ISO-10303-21;
HEADER;
/* Generated by software containing ST-Developer
 * from STEP Tools, Inc. (www.steptools.com) 
 */

FILE_DESCRIPTION(
/* description */ (''),
/* implementation_level */ '2;1');

FILE_NAME(
/* name */ '15_Bracket_Screw_ISO_4762_M10x30.step',
/* time_stamp */ '2026-10-26T04:15:57-07:00',
/* author */ (''),
/* organization */ (''),
/* preprocessor_version */ 'ST-DEVELOPER v20.2',
/* originating_system */ 'Autodesk Translation Framework v15.15.0.0',
/* authorisation */ '');

FILE_SCHEMA (('AUTOMOTIVE_DESIGN { 1 0 10303 214 3 1 1 }'));
ENDSEC;

DATA;
#10=MECHANICAL_DESIGN_GEOMETRIC_PRESENTATION_REPRESENTATION('',(#469),#55737);
#408=CONICAL_SURFACE('',#29836,4.75,0.78539816339745);
#409=CONICAL_SURFACE('',#29843,7.75,0.785398163397448);
#429=SHAPE_REPRESENTATION_RELATIONSHIP('SRR','None',#55838,#449);
#449=ADVANCED_BREP_SHAPE_REPRESENTATION('',(#489),#55734);
#469=STYLED_ITEM('',(#55998),#489);
#489=MANIFOLD_SOLID_BREP('Body1',#27238);
#580=B_SPLINE_SURFACE_WITH_KNOTS('',3,3,((#51175,#51176,#51177,#51178,#51179,
#51180,#51181,#51182,#51183,#51184,#51185,#51186,#51187,#51188,#51189,#51190,
#51191,#51192,#51193,#51194,#51195,#51196,#51197,#51198,#51199,#51200,#51201,
#51202,#51203,#51204,#51205,#51206,#51207,#51208,#51209,#51210,#51211,#51212,
#51213,#51214,#51215,#51216,#51217,#51218,#51219,#51220,#51221,#51222,#51223,
#51224,#51225,#51226,#51227,#51228,#51229,#51230,#51231,#51232,#51233,#51234,
#51235,#51236,#51237,#51238,#51239,#51240,#51241,#51242,#51243,#51244,#51245,
#51246,#51247,#51248,#51249,#51250,#51251,#51252,#51253,#51254,#51255,#51256,
#51257,#51258,#51259,#51260,#51261,#51262,#51263,#51264,#51265,#51266,#51267,
#51268,#51269,#51270,#51271,#51272,#51273,#51274,#51275,#51276,#51277,#51278,
#51279,#51280,#51281,#51282,#51283,#51284,#51285,#51286,#51287,#51288,#51289,
#51290,#51291,#51292,#51293,#51294,#51295,#51296,#51297,#51298,#51299,#51300,
#51301,#51302,#51303,#51304,#51305),(#51306,#51307,#51308,#51309,#51310,
#51311,#51312,#51313,#51314,#51315,#51316,#51317,#51318,#51319,#51320,#51321,
#51322,#51323,#51324,#51325,#51326,#51327,#51328,#51329,#51330,#51331,#51332,
#51333,#51334,#51335,#51336,#51337,#51338,#51339,#51340,#51341,#51342,#51343,
#51344,#51345,#51346,#51347,#51348,#51349,#51350,#51351,#51352,#51353,#51354,
#51355,#51356,#51357,#51358,#51359,#51360,#51361,#51362,#51363,#51364,#51365,
#51366,#51367,#51368,#51369,#51370,#51371,#51372,#51373,#51374,#51375,#51376,
#51377,#51378,#51379,#51380,#51381,#51382,#51383,#51384,#51385,#51386,#51387,
#51388,#51389,#51390,#51391,#51392,#51393,#51394,#51395,#51396,#51397,#51398,
#51399,#51400,#51401,#51402,#51403,#51404,#51405,#51406,#51407,#51408,#51409,
#51410,#51411,#51412,#51413,#51414,#51415,#51416,#51417,#51418,#51419,#51420,
#51421,#51422,#51423,#51424,#51425,#51426,#51427,#51428,#51429,#51430,#51431,
#51432,#51433,#51434,#51435,#51436),(#51437,#51438,#51439,#51440,#51441,
#51442,#51443,#51444,#51445,#51446,#51447,#51448,#51449,#51450,#51451,#51452,
#51453,#51454,#51455,#51456,#51457,#51458,#51459,#51460,#51461,#51462,#51463,
#51464,#51465,#51466,#51467,#51468,#51469,#51470,#51471,#51472,#51473,#51474,
#51475,#51476,#51477,#51478,#51479,#51480,#51481,#51482,#51483,#51484,#51485,
#51486,#51487,#51488,#51489,#51490,#51491,#51492,#51493,#51494,#51495,#51496,
#51497,#51498,#51499,#51500,#51501,#51502,#51503,#51504,#51505,#51506,#51507,
#51508,#51509,#51510,#51511,#51512,#51513,#51514,#51515,#51516,#51517,#51518,
#51519,#51520,#51521,#51522,#51523,#51524,#51525,#51526,#51527,#51528,#51529,
#51530,#51531,#51532,#51533,#51534,#51535,#51536,#51537,#51538,#51539,#51540,
#51541,#51542,#51543,#51544,#51545,#51546,#51547,#51548,#51549,#51550,#51551,
#51552,#51553,#51554,#51555,#51556,#51557,#51558,#51559,#51560,#51561,#51562,
#51563,#51564,#51565,#51566,#51567),(#51568,#51569,#51570,#51571,#51572,
#51573,#51574,#51575,#51576,#51577,#51578,#51579,#51580,#51581,#51582,#51583,
#51584,#51585,#51586,#51587,#51588,#51589,#51590,#51591,#51592,#51593,#51594,
#51595,#51596,#51597,#51598,#51599,#51600,#51601,#51602,#51603,#51604,#51605,
#51606,#51607,#51608,#51609,#51610,#51611,#51612,#51613,#51614,#51615,#51616,
#51617,#51618,#51619,#51620,#51621,#51622,#51623,#51624,#51625,#51626,#51627,
#51628,#51629,#51630,#51631,#51632,#51633,#51634,#51635,#51636,#51637,#51638,
#51639,#51640,#51641,#51642,#51643,#51644,#51645,#51646,#51647,#51648,#51649,
#51650,#51651,#51652,#51653,#51654,#51655,#51656,#51657,#51658,#51659,#51660,
#51661,#51662,#51663,#51664,#51665,#51666,#51667,#51668,#51669,#51670,#51671,
#51672,#51673,#51674,#51675,#51676,#51677,#51678,#51679,#51680,#51681,#51682,
#51683,#51684,#51685,#51686,#51687,#51688,#51689,#51690,#51691,#51692,#51693,
#51694,#51695,#51696,#51697,#51698)),.UNSPECIFIED.,.F.,.F.,.F.,(4,4),(4,
1,1,1,1,1,1,1,1,1,1,1,1,1,1,1,1,1,1,1,1,1,1,1,1,1,1,1,1,1,1,1,1,1,1,1,1,
1,1,1,1,1,1,1,1,1,1,1,1,1,1,1,1,1,1,1,1,1,1,1,1,1,1,1,1,1,1,1,1,1,1,1,1,
1,1,1,1,1,1,1,1,1,1,1,1,1,1,1,1,1,1,1,1,1,1,1,1,1,1,1,1,1,1,1,1,1,1,1,1,
1,1,1,1,1,1,1,1,1,1,1,1,1,1,1,1,1,1,1,4),(0.,0.0986691610045069),(8.3098959515533,
8.80969750862556,9.30949906569782,10.3091021798423,11.3087052939868,12.3083084081313,
13.3079115222759,14.3075146364204,15.3071177505649,16.3067208647094,17.3063239788539,
18.3059270929984,19.3055302071429,20.3051333212874,21.3047364354319,22.3043395495765,
23.303942663721,24.3035457778655,25.30314889201,26.3027520061545,27.302355120299,
28.3019582344435,29.301561348588,30.3011644627325,31.3007675768771,32.3003706910216,
33.2999738051661,34.2995769193106,35.2991800334551,36.2987831475996,37.2983862617441,
38.2979893758886,39.2975924900331,40.2971956041777,41.2967987183222,42.2964018324667,
43.2960049466112,44.2956080607557,45.2952111749002,46.2948142890447,47.2944174031892,
48.2940205173337,49.2936236314783,50.2932267456228,51.2928298597673,52.2924329739118,
53.2920360880563,54.2916392022008,55.2912423163453,56.2908454304898,57.2904485446343,
58.2900516587789,59.2896547729234,60.2892578870679,61.2888610012124,62.2884641153569,
63.2880672295014,64.2876703436459,65.2872734577904,66.2868765719349,67.2864796860794,
68.286082800224,69.2856859143685,70.285289028513,71.2848921426575,72.284495256802,
73.2840983709465,74.283701485091,75.2833045992355,76.28290771338,77.2825108275245,
78.2821139416691,79.2817170558136,80.2813201699581,81.2809232841026,82.2805263982471,
83.2801295123916,84.2797326265361,85.2793357406806,86.2789388548251,87.2785419689697,
88.2781450831142,89.2777481972587,90.2773513114032,91.2769544255477,92.2765575396922,
93.2761606538367,94.2757637679812,95.2753668821258,96.2749699962703,97.2745731104148,
98.2741762245593,99.2737793387038,100.273382452848,101.272985566993,102.272588681137,
103.272191795282,104.271794909426,105.271398023571,106.271001137715,107.27060425186,
108.270207366004,109.269810480149,110.269413594293,111.269016708438,112.268619822582,
113.268222936727,114.267826050871,115.267429165016,116.26703227916,117.266635393305,
118.26623850745,119.265841621594,120.265444735739,121.265047849883,122.264650964028,
123.264254078172,124.263857192317,125.263460306461,126.263063420606,127.26266653475,
128.262269648895,129.261872763039,130.261475877184,131.261078991328,132.260682105473,
133.260285219617,133.760086776689,134.259888333762),.UNSPECIFIED.);
#581=B_SPLINE_SURFACE_WITH_KNOTS('',3,3,((#52048,#52049,#52050,#52051,#52052,
#52053,#52054,#52055,#52056,#52057,#52058,#52059,#52060,#52061,#52062,#52063,
#52064,#52065,#52066,#52067,#52068,#52069,#52070,#52071,#52072,#52073,#52074,
#52075,#52076,#52077,#52078,#52079,#52080,#52081,#52082,#52083,#52084,#52085,
#52086,#52087,#52088,#52089,#52090,#52091,#52092,#52093,#52094,#52095,#52096,
#52097,#52098,#52099,#52100,#52101,#52102,#52103,#52104,#52105,#52106,#52107,
#52108,#52109,#52110,#52111,#52112,#52113,#52114,#52115,#52116,#52117,#52118,
#52119,#52120,#52121,#52122,#52123,#52124,#52125,#52126,#52127,#52128,#52129,
#52130,#52131,#52132,#52133,#52134,#52135,#52136,#52137,#52138,#52139,#52140,
#52141,#52142,#52143,#52144,#52145,#52146,#52147,#52148,#52149,#52150,#52151,
#52152,#52153,#52154,#52155,#52156,#52157,#52158,#52159,#52160,#52161,#52162,
#52163,#52164,#52165,#52166,#52167,#52168,#52169,#52170,#52171,#52172,#52173,
#52174,#52175,#52176,#52177,#52178),(#52179,#52180,#52181,#52182,#52183,
#52184,#52185,#52186,#52187,#52188,#52189,#52190,#52191,#52192,#52193,#52194,
#52195,#52196,#52197,#52198,#52199,#52200,#52201,#52202,#52203,#52204,#52205,
#52206,#52207,#52208,#52209,#52210,#52211,#52212,#52213,#52214,#52215,#52216,
#52217,#52218,#52219,#52220,#52221,#52222,#52223,#52224,#52225,#52226,#52227,
#52228,#52229,#52230,#52231,#52232,#52233,#52234,#52235,#52236,#52237,#52238,
#52239,#52240,#52241,#52242,#52243,#52244,#52245,#52246,#52247,#52248,#52249,
#52250,#52251,#52252,#52253,#52254,#52255,#52256,#52257,#52258,#52259,#52260,
#52261,#52262,#52263,#52264,#52265,#52266,#52267,#52268,#52269,#52270,#52271,
#52272,#52273,#52274,#52275,#52276,#52277,#52278,#52279,#52280,#52281,#52282,
#52283,#52284,#52285,#52286,#52287,#52288,#52289,#52290,#52291,#52292,#52293,
#52294,#52295,#52296,#52297,#52298,#52299,#52300,#52301,#52302,#52303,#52304,
#52305,#52306,#52307,#52308,#52309),(#52310,#52311,#52312,#52313,#52314,
#52315,#52316,#52317,#52318,#52319,#52320,#52321,#52322,#52323,#52324,#52325,
#52326,#52327,#52328,#52329,#52330,#52331,#52332,#52333,#52334,#52335,#52336,
#52337,#52338,#52339,#52340,#52341,#52342,#52343,#52344,#52345,#52346,#52347,
#52348,#52349,#52350,#52351,#52352,#52353,#52354,#52355,#52356,#52357,#52358,
#52359,#52360,#52361,#52362,#52363,#52364,#52365,#52366,#52367,#52368,#52369,
#52370,#52371,#52372,#52373,#52374,#52375,#52376,#52377,#52378,#52379,#52380,
#52381,#52382,#52383,#52384,#52385,#52386,#52387,#52388,#52389,#52390,#52391,
#52392,#52393,#52394,#52395,#52396,#52397,#52398,#52399,#52400,#52401,#52402,
#52403,#52404,#52405,#52406,#52407,#52408,#52409,#52410,#52411,#52412,#52413,
#52414,#52415,#52416,#52417,#52418,#52419,#52420,#52421,#52422,#52423,#52424,
#52425,#52426,#52427,#52428,#52429,#52430,#52431,#52432,#52433,#52434,#52435,
#52436,#52437,#52438,#52439,#52440),(#52441,#52442,#52443,#52444,#52445,
#52446,#52447,#52448,#52449,#52450,#52451,#52452,#52453,#52454,#52455,#52456,
#52457,#52458,#52459,#52460,#52461,#52462,#52463,#52464,#52465,#52466,#52467,
#52468,#52469,#52470,#52471,#52472,#52473,#52474,#52475,#52476,#52477,#52478,
#52479,#52480,#52481,#52482,#52483,#52484,#52485,#52486,#52487,#52488,#52489,
#52490,#52491,#52492,#52493,#52494,#52495,#52496,#52497,#52498,#52499,#52500,
#52501,#52502,#52503,#52504,#52505,#52506,#52507,#52508,#52509,#52510,#52511,
#52512,#52513,#52514,#52515,#52516,#52517,#52518,#52519,#52520,#52521,#52522,
#52523,#52524,#52525,#52526,#52527,#52528,#52529,#52530,#52531,#52532,#52533,
#52534,#52535,#52536,#52537,#52538,#52539,#52540,#52541,#52542,#52543,#52544,
#52545,#52546,#52547,#52548,#52549,#52550,#52551,#52552,#52553,#52554,#52555,
#52556,#52557,#52558,#52559,#52560,#52561,#52562,#52563,#52564,#52565,#52566,
#52567,#52568,#52569,#52570,#52571)),.UNSPECIFIED.,.F.,.F.,.F.,(4,4),(4,
1,1,1,1,1,1,1,1,1,1,1,1,1,1,1,1,1,1,1,1,1,1,1,1,1,1,1,1,1,1,1,1,1,1,1,1,
1,1,1,1,1,1,1,1,1,1,1,1,1,1,1,1,1,1,1,1,1,1,1,1,1,1,1,1,1,1,1,1,1,1,1,1,
1,1,1,1,1,1,1,1,1,1,1,1,1,1,1,1,1,1,1,1,1,1,1,1,1,1,1,1,1,1,1,1,1,1,1,1,
1,1,1,1,1,1,1,1,1,1,1,1,1,1,1,1,1,1,1,4),(0.,0.0986691610045069),(11.6147305479242,
12.1145321049964,12.6143336620687,13.6139367762132,14.6135398903577,15.6131430045022,
16.6127461186467,17.6123492327912,18.6119523469357,19.6115554610803,20.6111585752248,
21.6107616893693,22.6103648035138,23.6099679176583,24.6095710318028,25.6091741459473,
26.6087772600918,27.6083803742363,28.6079834883808,29.6075866025254,30.6071897166699,
31.6067928308144,32.6063959449589,33.6059990591034,34.6056021732479,35.6052052873924,
36.6048084015369,37.6044115156814,38.604014629826,39.6036177439705,40.603220858115,
41.6028239722595,42.602427086404,43.6020302005485,44.601633314693,45.6012364288375,
46.600839542982,47.6004426571266,48.6000457712711,49.5996488854156,50.5992519995601,
51.5988551137046,52.5984582278491,53.5980613419936,54.5976644561381,55.5972675702826,
56.5968706844272,57.5964737985717,58.5960769127162,59.5956800268607,60.5952831410052,
61.5948862551497,62.5944893692942,63.5940924834387,64.5936955975832,65.5932987117278,
66.5929018258723,67.5925049400168,68.5921080541613,69.5917111683058,70.5913142824503,
71.5909173965948,72.5905205107393,73.5901236248838,74.5897267390284,75.5893298531729,
76.5889329673174,77.5885360814619,78.5881391956064,79.5877423097509,80.5873454238954,
81.5869485380399,82.5865516521845,83.586154766329,84.5857578804735,85.585360994618,
86.5849641087625,87.584567222907,88.5841703370515,89.583773451196,90.5833765653405,
91.582979679485,92.5825827936296,93.5821859077741,94.5817890219186,95.5813921360631,
96.5809952502076,97.5805983643521,98.5802014784966,99.5798045926411,100.579407706786,
101.57901082093,102.578613935075,103.578217049219,104.577820163364,105.577423277508,
106.577026391653,107.576629505797,108.576232619942,109.575835734086,110.575438848231,
111.575041962375,112.57464507652,113.574248190664,114.573851304809,115.573454418953,
116.573057533098,117.572660647242,118.572263761387,119.571866875531,120.571469989676,
121.57107310382,122.570676217965,123.570279332109,124.569882446254,125.569485560398,
126.569088674543,127.568691788687,128.568294902832,129.567898016976,130.567501131121,
131.567104245265,132.56670735941,133.566310473554,134.565913587699,135.565516701844,
136.565119815988,137.06492137306,137.564722930133),.UNSPECIFIED.);
#717=FACE_BOUND('',#9993,.T.);
#718=FACE_BOUND('',#9995,.T.);
#719=FACE_BOUND('',#9996,.T.);
#720=FACE_BOUND('',#9997,.T.);
#721=FACE_BOUND('',#9998,.T.);
#722=FACE_BOUND('',#9999,.T.);
#723=FACE_BOUND('',#10000,.T.);
#724=FACE_BOUND('',#10001,.T.);
#725=FACE_BOUND('',#10002,.T.);
#726=FACE_BOUND('',#10003,.T.);
#727=FACE_BOUND('',#10004,.T.);
#728=FACE_BOUND('',#10005,.T.);
#729=FACE_BOUND('',#10006,.T.);
#730=FACE_BOUND('',#10007,.T.);
#731=FACE_BOUND('',#10008,.T.);
#732=FACE_BOUND('',#10009,.T.);
#733=FACE_BOUND('',#10010,.T.);
#734=FACE_BOUND('',#10011,.T.);
#735=FACE_BOUND('',#10012,.T.);
#736=FACE_BOUND('',#10013,.T.);
#737=FACE_BOUND('',#10014,.T.);
#738=FACE_BOUND('',#10015,.T.);
#739=FACE_BOUND('',#10016,.T.);
#740=FACE_BOUND('',#10017,.T.);
#741=FACE_BOUND('',#10018,.T.);
#742=FACE_BOUND('',#10019,.T.);
#743=FACE_BOUND('',#10020,.T.);
#744=FACE_BOUND('',#10021,.T.);
#745=FACE_BOUND('',#10022,.T.);
#746=FACE_BOUND('',#10023,.T.);
#747=FACE_BOUND('',#10024,.T.);
#748=FACE_BOUND('',#10025,.T.);
#749=FACE_BOUND('',#10026,.T.);
#750=FACE_BOUND('',#10027,.T.);
#751=FACE_BOUND('',#10028,.T.);
#752=FACE_BOUND('',#10029,.T.);
#753=FACE_BOUND('',#10032,.T.);
#1553=PLANE('',#29604);
#1554=PLANE('',#29609);
#1555=PLANE('',#29610);
#1556=PLANE('',#29612);
#1557=PLANE('',#29613);
#1558=PLANE('',#29615);
#1559=PLANE('',#29616);
#1560=PLANE('',#29618);
#1561=PLANE('',#29619);
#1562=PLANE('',#29621);
#1563=PLANE('',#29622);
#1564=PLANE('',#29624);
#1565=PLANE('',#29625);
#1566=PLANE('',#29627);
#1567=PLANE('',#29628);
#1568=PLANE('',#29630);
#1569=PLANE('',#29631);
#1570=PLANE('',#29633);
#1571=PLANE('',#29634);
#1572=PLANE('',#29636);
#1573=PLANE('',#29637);
#1574=PLANE('',#29639);
#1575=PLANE('',#29640);
#1576=PLANE('',#29642);
#1577=PLANE('',#29643);
#1578=PLANE('',#29645);
#1579=PLANE('',#29646);
#1580=PLANE('',#29648);
#1581=PLANE('',#29649);
#1582=PLANE('',#29651);
#1583=PLANE('',#29652);
#1584=PLANE('',#29654);
#1585=PLANE('',#29655);
#1586=PLANE('',#29657);
#1587=PLANE('',#29658);
#1588=PLANE('',#29660);
#1589=PLANE('',#29661);
#1590=PLANE('',#29663);
#1591=PLANE('',#29664);
#1592=PLANE('',#29666);
#1593=PLANE('',#29667);
#1594=PLANE('',#29669);
#1595=PLANE('',#29670);
#1596=PLANE('',#29672);
#1597=PLANE('',#29673);
#1598=PLANE('',#29675);
#1599=PLANE('',#29676);
#1600=PLANE('',#29678);
#1601=PLANE('',#29679);
#1602=PLANE('',#29681);
#1603=PLANE('',#29682);
#1604=PLANE('',#29684);
#1605=PLANE('',#29685);
#1606=PLANE('',#29687);
#1607=PLANE('',#29688);
#1608=PLANE('',#29690);
#1609=PLANE('',#29691);
#1610=PLANE('',#29693);
#1611=PLANE('',#29694);
#1612=PLANE('',#29696);
#1613=PLANE('',#29697);
#1614=PLANE('',#29699);
#1615=PLANE('',#29700);
#1616=PLANE('',#29702);
#1617=PLANE('',#29703);
#1618=PLANE('',#29705);
#1619=PLANE('',#29706);
#1620=PLANE('',#29708);
#1621=PLANE('',#29709);
#1622=PLANE('',#29711);
#1623=PLANE('',#29712);
#1624=PLANE('',#29715);
#1625=PLANE('',#29716);
#1626=PLANE('',#29719);
#1627=PLANE('',#29720);
#1628=PLANE('',#29722);
#1629=PLANE('',#29723);
#1630=PLANE('',#29725);
#1631=PLANE('',#29726);
#1632=PLANE('',#29728);
#1633=PLANE('',#29729);
#1634=PLANE('',#29731);
#1635=PLANE('',#29732);
#1636=PLANE('',#29734);
#1637=PLANE('',#29735);
#1638=PLANE('',#29737);
#1639=PLANE('',#29738);
#1640=PLANE('',#29740);
#1641=PLANE('',#29741);
#1642=PLANE('',#29743);
#1643=PLANE('',#29744);
#1644=PLANE('',#29746);
#1645=PLANE('',#29747);
#1646=PLANE('',#29749);
#1647=PLANE('',#29750);
#1648=PLANE('',#29752);
#1649=PLANE('',#29753);
#1650=PLANE('',#29755);
#1651=PLANE('',#29756);
#1652=PLANE('',#29758);
#1653=PLANE('',#29759);
#1654=PLANE('',#29761);
#1655=PLANE('',#29762);
#1656=PLANE('',#29764);
#1657=PLANE('',#29765);
#1658=PLANE('',#29767);
#1659=PLANE('',#29768);
#1660=PLANE('',#29770);
#1661=PLANE('',#29771);
#1662=PLANE('',#29773);
#1663=PLANE('',#29774);
#1664=PLANE('',#29776);
#1665=PLANE('',#29777);
#1666=PLANE('',#29779);
#1667=PLANE('',#29780);
#1668=PLANE('',#29782);
#1669=PLANE('',#29783);
#1670=PLANE('',#29785);
#1671=PLANE('',#29786);
#1672=PLANE('',#29788);
#1673=PLANE('',#29789);
#1674=PLANE('',#29791);
#1675=PLANE('',#29792);
#1676=PLANE('',#29794);
#1677=PLANE('',#29795);
#1678=PLANE('',#29797);
#1679=PLANE('',#29798);
#1680=PLANE('',#29800);
#1681=PLANE('',#29801);
#1682=PLANE('',#29803);
#1683=PLANE('',#29804);
#1684=PLANE('',#29806);
#1685=PLANE('',#29807);
#1686=PLANE('',#29809);
#1687=PLANE('',#29810);
#1688=PLANE('',#29812);
#1689=PLANE('',#29813);
#1690=PLANE('',#29815);
#1691=PLANE('',#29816);
#1692=PLANE('',#29818);
#1693=PLANE('',#29819);
#1694=PLANE('',#29821);
#1695=PLANE('',#29822);
#1696=PLANE('',#29824);
#1697=PLANE('',#29825);
#1698=PLANE('',#29827);
#1699=PLANE('',#29828);
#1700=PLANE('',#29829);
#1701=PLANE('',#29830);
#1702=PLANE('',#29831);
#1703=PLANE('',#29832);
#1704=PLANE('',#29833);
#1705=PLANE('',#29834);
#1706=PLANE('',#29839);
#1707=PLANE('',#29845);
#3691=LINE('',#49731,#6062);
#3692=LINE('',#49758,#6063);
#3693=LINE('',#49806,#6064);
#3694=LINE('',#49854,#6065);
#3695=LINE('',#49902,#6066);
#3696=LINE('',#49956,#6067);
#3697=LINE('',#50004,#6068);
#3698=LINE('',#50052,#6069);
#3699=LINE('',#50106,#6070);
#3700=LINE('',#50154,#6071);
#3701=LINE('',#50202,#6072);
#3702=LINE('',#50250,#6073);
#3703=LINE('',#50304,#6074);
#3704=LINE('',#50352,#6075);
#3705=LINE('',#50400,#6076);
#3706=LINE('',#50454,#6077);
#3707=LINE('',#50502,#6078);
#3708=LINE('',#50550,#6079);
#3709=LINE('',#50598,#6080);
#3710=LINE('',#50652,#6081);
#3711=LINE('',#50700,#6082);
#3712=LINE('',#50710,#6083);
#3713=LINE('',#50736,#6084);
#3714=LINE('',#50761,#6085);
#3715=LINE('',#50786,#6086);
#3716=LINE('',#50810,#6087);
#3717=LINE('',#50834,#6088);
#3718=LINE('',#50859,#6089);
#3719=LINE('',#50884,#6090);
#3720=LINE('',#50908,#6091);
#3721=LINE('',#50933,#6092);
#3722=LINE('',#50958,#6093);
#3723=LINE('',#50982,#6094);
#3724=LINE('',#51006,#6095);
#3725=LINE('',#51031,#6096);
#3726=LINE('',#51056,#6097);
#3727=LINE('',#51080,#6098);
#3728=LINE('',#51105,#6099);
#3729=LINE('',#51130,#6100);
#3730=LINE('',#51154,#6101);
#3731=LINE('',#52692,#6102);
#3732=LINE('',#52694,#6103);
#3733=LINE('',#52696,#6104);
#3734=LINE('',#52697,#6105);
#3735=LINE('',#52701,#6106);
#3736=LINE('',#52704,#6107);
#3737=LINE('',#52705,#6108);
#3738=LINE('',#52711,#6109);
#3739=LINE('',#52713,#6110);
#3740=LINE('',#52715,#6111);
#3741=LINE('',#52716,#6112);
#3742=LINE('',#52720,#6113);
#3743=LINE('',#52723,#6114);
#3744=LINE('',#52724,#6115);
#3745=LINE('',#52730,#6116);
#3746=LINE('',#52732,#6117);
#3747=LINE('',#52734,#6118);
#3748=LINE('',#52735,#6119);
#3749=LINE('',#52739,#6120);
#3750=LINE('',#52742,#6121);
#3751=LINE('',#52743,#6122);
#3752=LINE('',#52749,#6123);
#3753=LINE('',#52751,#6124);
#3754=LINE('',#52753,#6125);
#3755=LINE('',#52754,#6126);
#3756=LINE('',#52758,#6127);
#3757=LINE('',#52761,#6128);
#3758=LINE('',#52762,#6129);
#3759=LINE('',#52768,#6130);
#3760=LINE('',#52770,#6131);
#3761=LINE('',#52772,#6132);
#3762=LINE('',#52773,#6133);
#3763=LINE('',#52777,#6134);
#3764=LINE('',#52780,#6135);
#3765=LINE('',#52781,#6136);
#3766=LINE('',#52787,#6137);
#3767=LINE('',#52789,#6138);
#3768=LINE('',#52791,#6139);
#3769=LINE('',#52792,#6140);
#3770=LINE('',#52796,#6141);
#3771=LINE('',#52799,#6142);
#3772=LINE('',#52800,#6143);
#3773=LINE('',#52806,#6144);
#3774=LINE('',#52808,#6145);
#3775=LINE('',#52810,#6146);
#3776=LINE('',#52811,#6147);
#3777=LINE('',#52815,#6148);
#3778=LINE('',#52818,#6149);
#3779=LINE('',#52819,#6150);
#3780=LINE('',#52825,#6151);
#3781=LINE('',#52827,#6152);
#3782=LINE('',#52829,#6153);
#3783=LINE('',#52830,#6154);
#3784=LINE('',#52834,#6155);
#3785=LINE('',#52837,#6156);
#3786=LINE('',#52838,#6157);
#3787=LINE('',#52844,#6158);
#3788=LINE('',#52846,#6159);
#3789=LINE('',#52848,#6160);
#3790=LINE('',#52849,#6161);
#3791=LINE('',#52853,#6162);
#3792=LINE('',#52856,#6163);
#3793=LINE('',#52857,#6164);
#3794=LINE('',#52863,#6165);
#3795=LINE('',#52865,#6166);
#3796=LINE('',#52867,#6167);
#3797=LINE('',#52868,#6168);
#3798=LINE('',#52872,#6169);
#3799=LINE('',#52875,#6170);
#3800=LINE('',#52876,#6171);
#3801=LINE('',#52882,#6172);
#3802=LINE('',#52884,#6173);
#3803=LINE('',#52886,#6174);
#3804=LINE('',#52887,#6175);
#3805=LINE('',#52891,#6176);
#3806=LINE('',#52894,#6177);
#3807=LINE('',#52895,#6178);
#3808=LINE('',#52901,#6179);
#3809=LINE('',#52903,#6180);
#3810=LINE('',#52905,#6181);
#3811=LINE('',#52906,#6182);
#3812=LINE('',#52910,#6183);
#3813=LINE('',#52913,#6184);
#3814=LINE('',#52914,#6185);
#3815=LINE('',#52920,#6186);
#3816=LINE('',#52922,#6187);
#3817=LINE('',#52924,#6188);
#3818=LINE('',#52925,#6189);
#3819=LINE('',#52929,#6190);
#3820=LINE('',#52932,#6191);
#3821=LINE('',#52933,#6192);
#3822=LINE('',#52939,#6193);
#3823=LINE('',#52941,#6194);
#3824=LINE('',#52943,#6195);
#3825=LINE('',#52944,#6196);
#3826=LINE('',#52948,#6197);
#3827=LINE('',#52951,#6198);
#3828=LINE('',#52952,#6199);
#3829=LINE('',#52958,#6200);
#3830=LINE('',#52960,#6201);
#3831=LINE('',#52962,#6202);
#3832=LINE('',#52963,#6203);
#3833=LINE('',#52967,#6204);
#3834=LINE('',#52970,#6205);
#3835=LINE('',#52971,#6206);
#3836=LINE('',#52977,#6207);
#3837=LINE('',#52979,#6208);
#3838=LINE('',#52981,#6209);
#3839=LINE('',#52982,#6210);
#3840=LINE('',#52986,#6211);
#3841=LINE('',#52989,#6212);
#3842=LINE('',#52990,#6213);
#3843=LINE('',#52996,#6214);
#3844=LINE('',#52998,#6215);
#3845=LINE('',#53000,#6216);
#3846=LINE('',#53001,#6217);
#3847=LINE('',#53005,#6218);
#3848=LINE('',#53008,#6219);
#3849=LINE('',#53009,#6220);
#3850=LINE('',#53015,#6221);
#3851=LINE('',#53017,#6222);
#3852=LINE('',#53019,#6223);
#3853=LINE('',#53020,#6224);
#3854=LINE('',#53025,#6225);
#3855=LINE('',#53029,#6226);
#3856=LINE('',#53030,#6227);
#3857=LINE('',#53038,#6228);
#3858=LINE('',#53040,#6229);
#3859=LINE('',#53042,#6230);
#3860=LINE('',#53043,#6231);
#3861=LINE('',#53047,#6232);
#3862=LINE('',#53050,#6233);
#3863=LINE('',#53051,#6234);
#3864=LINE('',#53057,#6235);
#3865=LINE('',#53059,#6236);
#3866=LINE('',#53061,#6237);
#3867=LINE('',#53062,#6238);
#3868=LINE('',#53066,#6239);
#3869=LINE('',#53069,#6240);
#3870=LINE('',#53070,#6241);
#3871=LINE('',#53076,#6242);
#3872=LINE('',#53078,#6243);
#3873=LINE('',#53080,#6244);
#3874=LINE('',#53081,#6245);
#3875=LINE('',#53085,#6246);
#3876=LINE('',#53088,#6247);
#3877=LINE('',#53089,#6248);
#3878=LINE('',#53095,#6249);
#3879=LINE('',#53097,#6250);
#3880=LINE('',#53099,#6251);
#3881=LINE('',#53100,#6252);
#3882=LINE('',#53104,#6253);
#3883=LINE('',#53107,#6254);
#3884=LINE('',#53108,#6255);
#3885=LINE('',#53114,#6256);
#3886=LINE('',#53116,#6257);
#3887=LINE('',#53118,#6258);
#3888=LINE('',#53119,#6259);
#3889=LINE('',#53123,#6260);
#3890=LINE('',#53126,#6261);
#3891=LINE('',#53127,#6262);
#3892=LINE('',#53133,#6263);
#3893=LINE('',#53135,#6264);
#3894=LINE('',#53137,#6265);
#3895=LINE('',#53138,#6266);
#3896=LINE('',#53142,#6267);
#3897=LINE('',#53145,#6268);
#3898=LINE('',#53146,#6269);
#3899=LINE('',#53152,#6270);
#3900=LINE('',#53154,#6271);
#3901=LINE('',#53156,#6272);
#3902=LINE('',#53157,#6273);
#3903=LINE('',#53161,#6274);
#3904=LINE('',#53164,#6275);
#3905=LINE('',#53165,#6276);
#3906=LINE('',#53171,#6277);
#3907=LINE('',#53173,#6278);
#3908=LINE('',#53175,#6279);
#3909=LINE('',#53176,#6280);
#3910=LINE('',#53180,#6281);
#3911=LINE('',#53183,#6282);
#3912=LINE('',#53184,#6283);
#3913=LINE('',#53190,#6284);
#3914=LINE('',#53192,#6285);
#3915=LINE('',#53194,#6286);
#3916=LINE('',#53195,#6287);
#3917=LINE('',#53199,#6288);
#3918=LINE('',#53202,#6289);
#3919=LINE('',#53203,#6290);
#3920=LINE('',#53209,#6291);
#3921=LINE('',#53211,#6292);
#3922=LINE('',#53213,#6293);
#3923=LINE('',#53214,#6294);
#3924=LINE('',#53218,#6295);
#3925=LINE('',#53221,#6296);
#3926=LINE('',#53222,#6297);
#3927=LINE('',#53228,#6298);
#3928=LINE('',#53230,#6299);
#3929=LINE('',#53232,#6300);
#3930=LINE('',#53233,#6301);
#3931=LINE('',#53237,#6302);
#3932=LINE('',#53240,#6303);
#3933=LINE('',#53241,#6304);
#3934=LINE('',#53247,#6305);
#3935=LINE('',#53249,#6306);
#3936=LINE('',#53251,#6307);
#3937=LINE('',#53252,#6308);
#3938=LINE('',#53256,#6309);
#3939=LINE('',#53259,#6310);
#3940=LINE('',#53260,#6311);
#3941=LINE('',#53266,#6312);
#3942=LINE('',#53268,#6313);
#3943=LINE('',#53270,#6314);
#3944=LINE('',#53271,#6315);
#3945=LINE('',#53275,#6316);
#3946=LINE('',#53278,#6317);
#3947=LINE('',#53279,#6318);
#3948=LINE('',#53285,#6319);
#3949=LINE('',#53287,#6320);
#3950=LINE('',#53289,#6321);
#3951=LINE('',#53290,#6322);
#3952=LINE('',#53294,#6323);
#3953=LINE('',#53297,#6324);
#3954=LINE('',#53298,#6325);
#3955=LINE('',#53304,#6326);
#3956=LINE('',#53306,#6327);
#3957=LINE('',#53308,#6328);
#3958=LINE('',#53309,#6329);
#3959=LINE('',#53313,#6330);
#3960=LINE('',#53316,#6331);
#3961=LINE('',#53317,#6332);
#3962=LINE('',#53323,#6333);
#3963=LINE('',#53325,#6334);
#3964=LINE('',#53327,#6335);
#3965=LINE('',#53328,#6336);
#3966=LINE('',#53332,#6337);
#3967=LINE('',#53335,#6338);
#3968=LINE('',#53336,#6339);
#3969=LINE('',#53342,#6340);
#3970=LINE('',#53344,#6341);
#3971=LINE('',#53346,#6342);
#3972=LINE('',#53347,#6343);
#3973=LINE('',#53351,#6344);
#3974=LINE('',#53354,#6345);
#3975=LINE('',#53355,#6346);
#3976=LINE('',#53361,#6347);
#3977=LINE('',#53363,#6348);
#3978=LINE('',#53365,#6349);
#3979=LINE('',#53366,#6350);
#3980=LINE('',#53370,#6351);
#3981=LINE('',#53373,#6352);
#3982=LINE('',#53374,#6353);
#3983=LINE('',#53380,#6354);
#3984=LINE('',#53382,#6355);
#3985=LINE('',#53384,#6356);
#3986=LINE('',#53385,#6357);
#3987=LINE('',#53388,#6358);
#3988=LINE('',#53390,#6359);
#3989=LINE('',#53391,#6360);
#3990=LINE('',#53394,#6361);
#3991=LINE('',#53396,#6362);
#3992=LINE('',#53397,#6363);
#3993=LINE('',#53400,#6364);
#3994=LINE('',#53402,#6365);
#3995=LINE('',#53403,#6366);
#3996=LINE('',#53406,#6367);
#3997=LINE('',#53408,#6368);
#3998=LINE('',#53409,#6369);
#3999=LINE('',#53411,#6370);
#4000=LINE('',#53412,#6371);
#4001=LINE('',#53418,#6372);
#4002=LINE('',#53427,#6373);
#4003=LINE('',#53428,#6374);
#4004=LINE('',#53432,#6375);
#6062=VECTOR('',#36109,5.);
#6063=VECTOR('',#36114,5.);
#6064=VECTOR('',#36117,5.);
#6065=VECTOR('',#36120,5.);
#6066=VECTOR('',#36123,5.);
#6067=VECTOR('',#36126,5.);
#6068=VECTOR('',#36129,5.);
#6069=VECTOR('',#36132,5.);
#6070=VECTOR('',#36135,5.);
#6071=VECTOR('',#36138,5.);
#6072=VECTOR('',#36141,5.);
#6073=VECTOR('',#36144,5.);
#6074=VECTOR('',#36147,5.);
#6075=VECTOR('',#36150,5.);
#6076=VECTOR('',#36153,5.);
#6077=VECTOR('',#36156,5.);
#6078=VECTOR('',#36159,5.);
#6079=VECTOR('',#36162,5.);
#6080=VECTOR('',#36165,5.);
#6081=VECTOR('',#36168,5.);
#6082=VECTOR('',#36171,4.0705);
#6083=VECTOR('',#36176,4.0705);
#6084=VECTOR('',#36181,4.0705);
#6085=VECTOR('',#36184,4.0705);
#6086=VECTOR('',#36187,4.0705);
#6087=VECTOR('',#36190,4.0705);
#6088=VECTOR('',#36193,4.0705);
#6089=VECTOR('',#36196,4.0705);
#6090=VECTOR('',#36199,4.0705);
#6091=VECTOR('',#36202,4.0705);
#6092=VECTOR('',#36205,4.0705);
#6093=VECTOR('',#36208,4.0705);
#6094=VECTOR('',#36211,4.0705);
#6095=VECTOR('',#36214,4.0705);
#6096=VECTOR('',#36217,4.0705);
#6097=VECTOR('',#36220,4.0705);
#6098=VECTOR('',#36223,4.0705);
#6099=VECTOR('',#36226,4.0705);
#6100=VECTOR('',#36229,4.0705);
#6101=VECTOR('',#36232,4.0705);
#6102=VECTOR('',#36245,10.);
#6103=VECTOR('',#36246,10.);
#6104=VECTOR('',#36247,10.);
#6105=VECTOR('',#36248,10.);
#6106=VECTOR('',#36253,10.);
#6107=VECTOR('',#36256,10.);
#6108=VECTOR('',#36257,10.);
#6109=VECTOR('',#36264,10.);
#6110=VECTOR('',#36265,10.);
#6111=VECTOR('',#36266,10.);
#6112=VECTOR('',#36267,10.);
#6113=VECTOR('',#36272,10.);
#6114=VECTOR('',#36275,10.);
#6115=VECTOR('',#36276,10.);
#6116=VECTOR('',#36283,10.);
#6117=VECTOR('',#36284,10.);
#6118=VECTOR('',#36285,10.);
#6119=VECTOR('',#36286,10.);
#6120=VECTOR('',#36291,10.);
#6121=VECTOR('',#36294,10.);
#6122=VECTOR('',#36295,10.);
#6123=VECTOR('',#36302,10.);
#6124=VECTOR('',#36303,10.);
#6125=VECTOR('',#36304,10.);
#6126=VECTOR('',#36305,10.);
#6127=VECTOR('',#36310,10.);
#6128=VECTOR('',#36313,10.);
#6129=VECTOR('',#36314,10.);
#6130=VECTOR('',#36321,10.);
#6131=VECTOR('',#36322,10.);
#6132=VECTOR('',#36323,10.);
#6133=VECTOR('',#36324,10.);
#6134=VECTOR('',#36329,10.);
#6135=VECTOR('',#36332,10.);
#6136=VECTOR('',#36333,10.);
#6137=VECTOR('',#36340,10.);
#6138=VECTOR('',#36341,10.);
#6139=VECTOR('',#36342,10.);
#6140=VECTOR('',#36343,10.);
#6141=VECTOR('',#36348,10.);
#6142=VECTOR('',#36351,10.);
#6143=VECTOR('',#36352,10.);
#6144=VECTOR('',#36359,10.);
#6145=VECTOR('',#36360,10.);
#6146=VECTOR('',#36361,10.);
#6147=VECTOR('',#36362,10.);
#6148=VECTOR('',#36367,10.);
#6149=VECTOR('',#36370,10.);
#6150=VECTOR('',#36371,10.);
#6151=VECTOR('',#36378,10.);
#6152=VECTOR('',#36379,10.);
#6153=VECTOR('',#36380,10.);
#6154=VECTOR('',#36381,10.);
#6155=VECTOR('',#36386,10.);
#6156=VECTOR('',#36389,10.);
#6157=VECTOR('',#36390,10.);
#6158=VECTOR('',#36397,10.);
#6159=VECTOR('',#36398,10.);
#6160=VECTOR('',#36399,10.);
#6161=VECTOR('',#36400,10.);
#6162=VECTOR('',#36405,10.);
#6163=VECTOR('',#36408,10.);
#6164=VECTOR('',#36409,10.);
#6165=VECTOR('',#36416,10.);
#6166=VECTOR('',#36417,10.);
#6167=VECTOR('',#36418,10.);
#6168=VECTOR('',#36419,10.);
#6169=VECTOR('',#36424,10.);
#6170=VECTOR('',#36427,10.);
#6171=VECTOR('',#36428,10.);
#6172=VECTOR('',#36435,10.);
#6173=VECTOR('',#36436,10.);
#6174=VECTOR('',#36437,10.);
#6175=VECTOR('',#36438,10.);
#6176=VECTOR('',#36443,10.);
#6177=VECTOR('',#36446,10.);
#6178=VECTOR('',#36447,10.);
#6179=VECTOR('',#36454,10.);
#6180=VECTOR('',#36455,10.);
#6181=VECTOR('',#36456,10.);
#6182=VECTOR('',#36457,10.);
#6183=VECTOR('',#36462,10.);
#6184=VECTOR('',#36465,10.);
#6185=VECTOR('',#36466,10.);
#6186=VECTOR('',#36473,10.);
#6187=VECTOR('',#36474,10.);
#6188=VECTOR('',#36475,10.);
#6189=VECTOR('',#36476,10.);
#6190=VECTOR('',#36481,10.);
#6191=VECTOR('',#36484,10.);
#6192=VECTOR('',#36485,10.);
#6193=VECTOR('',#36492,10.);
#6194=VECTOR('',#36493,10.);
#6195=VECTOR('',#36494,10.);
#6196=VECTOR('',#36495,10.);
#6197=VECTOR('',#36500,10.);
#6198=VECTOR('',#36503,10.);
#6199=VECTOR('',#36504,10.);
#6200=VECTOR('',#36511,10.);
#6201=VECTOR('',#36512,10.);
#6202=VECTOR('',#36513,10.);
#6203=VECTOR('',#36514,10.);
#6204=VECTOR('',#36519,10.);
#6205=VECTOR('',#36522,10.);
#6206=VECTOR('',#36523,10.);
#6207=VECTOR('',#36530,10.);
#6208=VECTOR('',#36531,10.);
#6209=VECTOR('',#36532,10.);
#6210=VECTOR('',#36533,10.);
#6211=VECTOR('',#36538,10.);
#6212=VECTOR('',#36541,10.);
#6213=VECTOR('',#36542,10.);
#6214=VECTOR('',#36549,10.);
#6215=VECTOR('',#36550,10.);
#6216=VECTOR('',#36551,10.);
#6217=VECTOR('',#36552,10.);
#6218=VECTOR('',#36557,10.);
#6219=VECTOR('',#36560,10.);
#6220=VECTOR('',#36561,10.);
#6221=VECTOR('',#36568,10.);
#6222=VECTOR('',#36569,10.);
#6223=VECTOR('',#36570,10.);
#6224=VECTOR('',#36571,10.);
#6225=VECTOR('',#36576,10.);
#6226=VECTOR('',#36581,10.);
#6227=VECTOR('',#36582,10.);
#6228=VECTOR('',#36591,10.);
#6229=VECTOR('',#36592,10.);
#6230=VECTOR('',#36593,10.);
#6231=VECTOR('',#36594,10.);
#6232=VECTOR('',#36599,10.);
#6233=VECTOR('',#36602,10.);
#6234=VECTOR('',#36603,10.);
#6235=VECTOR('',#36610,10.);
#6236=VECTOR('',#36611,10.);
#6237=VECTOR('',#36612,10.);
#6238=VECTOR('',#36613,10.);
#6239=VECTOR('',#36618,10.);
#6240=VECTOR('',#36621,10.);
#6241=VECTOR('',#36622,10.);
#6242=VECTOR('',#36629,10.);
#6243=VECTOR('',#36630,10.);
#6244=VECTOR('',#36631,10.);
#6245=VECTOR('',#36632,10.);
#6246=VECTOR('',#36637,10.);
#6247=VECTOR('',#36640,10.);
#6248=VECTOR('',#36641,10.);
#6249=VECTOR('',#36648,10.);
#6250=VECTOR('',#36649,10.);
#6251=VECTOR('',#36650,10.);
#6252=VECTOR('',#36651,10.);
#6253=VECTOR('',#36656,10.);
#6254=VECTOR('',#36659,10.);
#6255=VECTOR('',#36660,10.);
#6256=VECTOR('',#36667,10.);
#6257=VECTOR('',#36668,10.);
#6258=VECTOR('',#36669,10.);
#6259=VECTOR('',#36670,10.);
#6260=VECTOR('',#36675,10.);
#6261=VECTOR('',#36678,10.);
#6262=VECTOR('',#36679,10.);
#6263=VECTOR('',#36686,10.);
#6264=VECTOR('',#36687,10.);
#6265=VECTOR('',#36688,10.);
#6266=VECTOR('',#36689,10.);
#6267=VECTOR('',#36694,10.);
#6268=VECTOR('',#36697,10.);
#6269=VECTOR('',#36698,10.);
#6270=VECTOR('',#36705,10.);
#6271=VECTOR('',#36706,10.);
#6272=VECTOR('',#36707,10.);
#6273=VECTOR('',#36708,10.);
#6274=VECTOR('',#36713,10.);
#6275=VECTOR('',#36716,10.);
#6276=VECTOR('',#36717,10.);
#6277=VECTOR('',#36724,10.);
#6278=VECTOR('',#36725,10.);
#6279=VECTOR('',#36726,10.);
#6280=VECTOR('',#36727,10.);
#6281=VECTOR('',#36732,10.);
#6282=VECTOR('',#36735,10.);
#6283=VECTOR('',#36736,10.);
#6284=VECTOR('',#36743,10.);
#6285=VECTOR('',#36744,10.);
#6286=VECTOR('',#36745,10.);
#6287=VECTOR('',#36746,10.);
#6288=VECTOR('',#36751,10.);
#6289=VECTOR('',#36754,10.);
#6290=VECTOR('',#36755,10.);
#6291=VECTOR('',#36762,10.);
#6292=VECTOR('',#36763,10.);
#6293=VECTOR('',#36764,10.);
#6294=VECTOR('',#36765,10.);
#6295=VECTOR('',#36770,10.);
#6296=VECTOR('',#36773,10.);
#6297=VECTOR('',#36774,10.);
#6298=VECTOR('',#36781,10.);
#6299=VECTOR('',#36782,10.);
#6300=VECTOR('',#36783,10.);
#6301=VECTOR('',#36784,10.);
#6302=VECTOR('',#36789,10.);
#6303=VECTOR('',#36792,10.);
#6304=VECTOR('',#36793,10.);
#6305=VECTOR('',#36800,10.);
#6306=VECTOR('',#36801,10.);
#6307=VECTOR('',#36802,10.);
#6308=VECTOR('',#36803,10.);
#6309=VECTOR('',#36808,10.);
#6310=VECTOR('',#36811,10.);
#6311=VECTOR('',#36812,10.);
#6312=VECTOR('',#36819,10.);
#6313=VECTOR('',#36820,10.);
#6314=VECTOR('',#36821,10.);
#6315=VECTOR('',#36822,10.);
#6316=VECTOR('',#36827,10.);
#6317=VECTOR('',#36830,10.);
#6318=VECTOR('',#36831,10.);
#6319=VECTOR('',#36838,10.);
#6320=VECTOR('',#36839,10.);
#6321=VECTOR('',#36840,10.);
#6322=VECTOR('',#36841,10.);
#6323=VECTOR('',#36846,10.);
#6324=VECTOR('',#36849,10.);
#6325=VECTOR('',#36850,10.);
#6326=VECTOR('',#36857,10.);
#6327=VECTOR('',#36858,10.);
#6328=VECTOR('',#36859,10.);
#6329=VECTOR('',#36860,10.);
#6330=VECTOR('',#36865,10.);
#6331=VECTOR('',#36868,10.);
#6332=VECTOR('',#36869,10.);
#6333=VECTOR('',#36876,10.);
#6334=VECTOR('',#36877,10.);
#6335=VECTOR('',#36878,10.);
#6336=VECTOR('',#36879,10.);
#6337=VECTOR('',#36884,10.);
#6338=VECTOR('',#36887,10.);
#6339=VECTOR('',#36888,10.);
#6340=VECTOR('',#36895,10.);
#6341=VECTOR('',#36896,10.);
#6342=VECTOR('',#36897,10.);
#6343=VECTOR('',#36898,10.);
#6344=VECTOR('',#36903,10.);
#6345=VECTOR('',#36906,10.);
#6346=VECTOR('',#36907,10.);
#6347=VECTOR('',#36914,10.);
#6348=VECTOR('',#36915,10.);
#6349=VECTOR('',#36916,10.);
#6350=VECTOR('',#36917,10.);
#6351=VECTOR('',#36922,10.);
#6352=VECTOR('',#36925,10.);
#6353=VECTOR('',#36926,10.);
#6354=VECTOR('',#36933,10.);
#6355=VECTOR('',#36934,10.);
#6356=VECTOR('',#36935,10.);
#6357=VECTOR('',#36936,10.);
#6358=VECTOR('',#36939,10.);
#6359=VECTOR('',#36940,10.);
#6360=VECTOR('',#36941,10.);
#6361=VECTOR('',#36944,10.);
#6362=VECTOR('',#36945,10.);
#6363=VECTOR('',#36946,10.);
#6364=VECTOR('',#36949,10.);
#6365=VECTOR('',#36950,10.);
#6366=VECTOR('',#36951,10.);
#6367=VECTOR('',#36954,10.);
#6368=VECTOR('',#36955,10.);
#6369=VECTOR('',#36956,10.);
#6370=VECTOR('',#36959,10.);
#6371=VECTOR('',#36960,10.);
#6372=VECTOR('',#36969,4.75);
#6373=VECTOR('',#36982,8.);
#6374=VECTOR('',#36983,8.);
#6375=VECTOR('',#36988,7.75);
#6756=CYLINDRICAL_SURFACE('',#29561,4.925);
#6757=CYLINDRICAL_SURFACE('',#29563,4.925);
#6758=CYLINDRICAL_SURFACE('',#29564,4.925);
#6759=CYLINDRICAL_SURFACE('',#29565,4.925);
#6760=CYLINDRICAL_SURFACE('',#29566,4.925);
#6761=CYLINDRICAL_SURFACE('',#29567,4.925);
#6762=CYLINDRICAL_SURFACE('',#29568,4.925);
#6763=CYLINDRICAL_SURFACE('',#29569,4.925);
#6764=CYLINDRICAL_SURFACE('',#29570,4.925);
#6765=CYLINDRICAL_SURFACE('',#29571,4.925);
#6766=CYLINDRICAL_SURFACE('',#29572,4.925);
#6767=CYLINDRICAL_SURFACE('',#29573,4.925);
#6768=CYLINDRICAL_SURFACE('',#29574,4.925);
#6769=CYLINDRICAL_SURFACE('',#29575,4.925);
#6770=CYLINDRICAL_SURFACE('',#29576,4.925);
#6771=CYLINDRICAL_SURFACE('',#29577,4.925);
#6772=CYLINDRICAL_SURFACE('',#29578,4.925);
#6773=CYLINDRICAL_SURFACE('',#29579,4.925);
#6774=CYLINDRICAL_SURFACE('',#29580,4.925);
#6775=CYLINDRICAL_SURFACE('',#29581,4.925);
#6776=CYLINDRICAL_SURFACE('',#29582,4.0705);
#6777=CYLINDRICAL_SURFACE('',#29584,4.0705);
#6778=CYLINDRICAL_SURFACE('',#29586,4.0705);
#6779=CYLINDRICAL_SURFACE('',#29587,4.0705);
#6780=CYLINDRICAL_SURFACE('',#29588,4.0705);
#6781=CYLINDRICAL_SURFACE('',#29589,4.0705);
#6782=CYLINDRICAL_SURFACE('',#29590,4.0705);
#6783=CYLINDRICAL_SURFACE('',#29591,4.0705);
#6784=CYLINDRICAL_SURFACE('',#29592,4.0705);
#6785=CYLINDRICAL_SURFACE('',#29593,4.0705);
#6786=CYLINDRICAL_SURFACE('',#29594,4.0705);
#6787=CYLINDRICAL_SURFACE('',#29595,4.0705);
#6788=CYLINDRICAL_SURFACE('',#29596,4.0705);
#6789=CYLINDRICAL_SURFACE('',#29597,4.0705);
#6790=CYLINDRICAL_SURFACE('',#29598,4.0705);
#6791=CYLINDRICAL_SURFACE('',#29599,4.0705);
#6792=CYLINDRICAL_SURFACE('',#29600,4.0705);
#6793=CYLINDRICAL_SURFACE('',#29601,4.0705);
#6794=CYLINDRICAL_SURFACE('',#29602,4.0705);
#6795=CYLINDRICAL_SURFACE('',#29603,4.0705);
#6796=CYLINDRICAL_SURFACE('',#29608,4.0705);
#6797=CYLINDRICAL_SURFACE('',#29837,4.925);
#6798=CYLINDRICAL_SURFACE('',#29841,8.);
#8112=FACE_OUTER_BOUND('',#9794,.T.);
#8113=FACE_OUTER_BOUND('',#9795,.T.);
#8114=FACE_OUTER_BOUND('',#9796,.T.);
#8115=FACE_OUTER_BOUND('',#9797,.T.);
#8116=FACE_OUTER_BOUND('',#9798,.T.);
#8117=FACE_OUTER_BOUND('',#9799,.T.);
#8118=FACE_OUTER_BOUND('',#9800,.T.);
#8119=FACE_OUTER_BOUND('',#9801,.T.);
#8120=FACE_OUTER_BOUND('',#9802,.T.);
#8121=FACE_OUTER_BOUND('',#9803,.T.);
#8122=FACE_OUTER_BOUND('',#9804,.T.);
#8123=FACE_OUTER_BOUND('',#9805,.T.);
#8124=FACE_OUTER_BOUND('',#9806,.T.);
#8125=FACE_OUTER_BOUND('',#9807,.T.);
#8126=FACE_OUTER_BOUND('',#9808,.T.);
#8127=FACE_OUTER_BOUND('',#9809,.T.);
#8128=FACE_OUTER_BOUND('',#9810,.T.);
#8129=FACE_OUTER_BOUND('',#9811,.T.);
#8130=FACE_OUTER_BOUND('',#9812,.T.);
#8131=FACE_OUTER_BOUND('',#9813,.T.);
#8132=FACE_OUTER_BOUND('',#9814,.T.);
#8133=FACE_OUTER_BOUND('',#9815,.T.);
#8134=FACE_OUTER_BOUND('',#9816,.T.);
#8135=FACE_OUTER_BOUND('',#9817,.T.);
#8136=FACE_OUTER_BOUND('',#9818,.T.);
#8137=FACE_OUTER_BOUND('',#9819,.T.);
#8138=FACE_OUTER_BOUND('',#9820,.T.);
#8139=FACE_OUTER_BOUND('',#9821,.T.);
#8140=FACE_OUTER_BOUND('',#9822,.T.);
#8141=FACE_OUTER_BOUND('',#9823,.T.);
#8142=FACE_OUTER_BOUND('',#9824,.T.);
#8143=FACE_OUTER_BOUND('',#9825,.T.);
#8144=FACE_OUTER_BOUND('',#9826,.T.);
#8145=FACE_OUTER_BOUND('',#9827,.T.);
#8146=FACE_OUTER_BOUND('',#9828,.T.);
#8147=FACE_OUTER_BOUND('',#9829,.T.);
#8148=FACE_OUTER_BOUND('',#9830,.T.);
#8149=FACE_OUTER_BOUND('',#9831,.T.);
#8150=FACE_OUTER_BOUND('',#9832,.T.);
#8151=FACE_OUTER_BOUND('',#9833,.T.);
#8152=FACE_OUTER_BOUND('',#9834,.T.);
#8153=FACE_OUTER_BOUND('',#9835,.T.);
#8154=FACE_OUTER_BOUND('',#9836,.T.);
#8155=FACE_OUTER_BOUND('',#9837,.T.);
#8156=FACE_OUTER_BOUND('',#9838,.T.);
#8157=FACE_OUTER_BOUND('',#9839,.T.);
#8158=FACE_OUTER_BOUND('',#9840,.T.);
#8159=FACE_OUTER_BOUND('',#9841,.T.);
#8160=FACE_OUTER_BOUND('',#9842,.T.);
#8161=FACE_OUTER_BOUND('',#9843,.T.);
#8162=FACE_OUTER_BOUND('',#9844,.T.);
#8163=FACE_OUTER_BOUND('',#9845,.T.);
#8164=FACE_OUTER_BOUND('',#9846,.T.);
#8165=FACE_OUTER_BOUND('',#9847,.T.);
#8166=FACE_OUTER_BOUND('',#9848,.T.);
#8167=FACE_OUTER_BOUND('',#9849,.T.);
#8168=FACE_OUTER_BOUND('',#9850,.T.);
#8169=FACE_OUTER_BOUND('',#9851,.T.);
#8170=FACE_OUTER_BOUND('',#9852,.T.);
#8171=FACE_OUTER_BOUND('',#9853,.T.);
#8172=FACE_OUTER_BOUND('',#9854,.T.);
#8173=FACE_OUTER_BOUND('',#9855,.T.);
#8174=FACE_OUTER_BOUND('',#9856,.T.);
#8175=FACE_OUTER_BOUND('',#9857,.T.);
#8176=FACE_OUTER_BOUND('',#9858,.T.);
#8177=FACE_OUTER_BOUND('',#9859,.T.);
#8178=FACE_OUTER_BOUND('',#9860,.T.);
#8179=FACE_OUTER_BOUND('',#9861,.T.);
#8180=FACE_OUTER_BOUND('',#9862,.T.);
#8181=FACE_OUTER_BOUND('',#9863,.T.);
#8182=FACE_OUTER_BOUND('',#9864,.T.);
#8183=FACE_OUTER_BOUND('',#9865,.T.);
#8184=FACE_OUTER_BOUND('',#9866,.T.);
#8185=FACE_OUTER_BOUND('',#9867,.T.);
#8186=FACE_OUTER_BOUND('',#9868,.T.);
#8187=FACE_OUTER_BOUND('',#9869,.T.);
#8188=FACE_OUTER_BOUND('',#9870,.T.);
#8189=FACE_OUTER_BOUND('',#9871,.T.);
#8190=FACE_OUTER_BOUND('',#9872,.T.);
#8191=FACE_OUTER_BOUND('',#9873,.T.);
#8192=FACE_OUTER_BOUND('',#9874,.T.);
#8193=FACE_OUTER_BOUND('',#9875,.T.);
#8194=FACE_OUTER_BOUND('',#9876,.T.);
#8195=FACE_OUTER_BOUND('',#9877,.T.);
#8196=FACE_OUTER_BOUND('',#9878,.T.);
#8197=FACE_OUTER_BOUND('',#9879,.T.);
#8198=FACE_OUTER_BOUND('',#9880,.T.);
#8199=FACE_OUTER_BOUND('',#9881,.T.);
#8200=FACE_OUTER_BOUND('',#9882,.T.);
#8201=FACE_OUTER_BOUND('',#9883,.T.);
#8202=FACE_OUTER_BOUND('',#9884,.T.);
#8203=FACE_OUTER_BOUND('',#9885,.T.);
#8204=FACE_OUTER_BOUND('',#9886,.T.);
#8205=FACE_OUTER_BOUND('',#9887,.T.);
#8206=FACE_OUTER_BOUND('',#9888,.T.);
#8207=FACE_OUTER_BOUND('',#9889,.T.);
#8208=FACE_OUTER_BOUND('',#9890,.T.);
#8209=FACE_OUTER_BOUND('',#9891,.T.);
#8210=FACE_OUTER_BOUND('',#9892,.T.);
#8211=FACE_OUTER_BOUND('',#9893,.T.);
#8212=FACE_OUTER_BOUND('',#9894,.T.);
#8213=FACE_OUTER_BOUND('',#9895,.T.);
#8214=FACE_OUTER_BOUND('',#9896,.T.);
#8215=FACE_OUTER_BOUND('',#9897,.T.);
#8216=FACE_OUTER_BOUND('',#9898,.T.);
#8217=FACE_OUTER_BOUND('',#9899,.T.);
#8218=FACE_OUTER_BOUND('',#9900,.T.);
#8219=FACE_OUTER_BOUND('',#9901,.T.);
#8220=FACE_OUTER_BOUND('',#9902,.T.);
#8221=FACE_OUTER_BOUND('',#9903,.T.);
#8222=FACE_OUTER_BOUND('',#9904,.T.);
#8223=FACE_OUTER_BOUND('',#9905,.T.);
#8224=FACE_OUTER_BOUND('',#9906,.T.);
#8225=FACE_OUTER_BOUND('',#9907,.T.);
#8226=FACE_OUTER_BOUND('',#9908,.T.);
#8227=FACE_OUTER_BOUND('',#9909,.T.);
#8228=FACE_OUTER_BOUND('',#9910,.T.);
#8229=FACE_OUTER_BOUND('',#9911,.T.);
#8230=FACE_OUTER_BOUND('',#9912,.T.);
#8231=FACE_OUTER_BOUND('',#9913,.T.);
#8232=FACE_OUTER_BOUND('',#9914,.T.);
#8233=FACE_OUTER_BOUND('',#9915,.T.);
#8234=FACE_OUTER_BOUND('',#9916,.T.);
#8235=FACE_OUTER_BOUND('',#9917,.T.);
#8236=FACE_OUTER_BOUND('',#9918,.T.);
#8237=FACE_OUTER_BOUND('',#9919,.T.);
#8238=FACE_OUTER_BOUND('',#9920,.T.);
#8239=FACE_OUTER_BOUND('',#9921,.T.);
#8240=FACE_OUTER_BOUND('',#9922,.T.);
#8241=FACE_OUTER_BOUND('',#9923,.T.);
#8242=FACE_OUTER_BOUND('',#9924,.T.);
#8243=FACE_OUTER_BOUND('',#9925,.T.);
#8244=FACE_OUTER_BOUND('',#9926,.T.);
#8245=FACE_OUTER_BOUND('',#9927,.T.);
#8246=FACE_OUTER_BOUND('',#9928,.T.);
#8247=FACE_OUTER_BOUND('',#9929,.T.);
#8248=FACE_OUTER_BOUND('',#9930,.T.);
#8249=FACE_OUTER_BOUND('',#9931,.T.);
#8250=FACE_OUTER_BOUND('',#9932,.T.);
#8251=FACE_OUTER_BOUND('',#9933,.T.);
#8252=FACE_OUTER_BOUND('',#9934,.T.);
#8253=FACE_OUTER_BOUND('',#9935,.T.);
#8254=FACE_OUTER_BOUND('',#9936,.T.);
#8255=FACE_OUTER_BOUND('',#9937,.T.);
#8256=FACE_OUTER_BOUND('',#9938,.T.);
#8257=FACE_OUTER_BOUND('',#9939,.T.);
#8258=FACE_OUTER_BOUND('',#9940,.T.);
#8259=FACE_OUTER_BOUND('',#9941,.T.);
#8260=FACE_OUTER_BOUND('',#9942,.T.);
#8261=FACE_OUTER_BOUND('',#9943,.T.);
#8262=FACE_OUTER_BOUND('',#9944,.T.);
#8263=FACE_OUTER_BOUND('',#9945,.T.);
#8264=FACE_OUTER_BOUND('',#9946,.T.);
#8265=FACE_OUTER_BOUND('',#9947,.T.);
#8266=FACE_OUTER_BOUND('',#9948,.T.);
#8267=FACE_OUTER_BOUND('',#9949,.T.);
#8268=FACE_OUTER_BOUND('',#9950,.T.);
#8269=FACE_OUTER_BOUND('',#9951,.T.);
#8270=FACE_OUTER_BOUND('',#9952,.T.);
#8271=FACE_OUTER_BOUND('',#9953,.T.);
#8272=FACE_OUTER_BOUND('',#9954,.T.);
#8273=FACE_OUTER_BOUND('',#9955,.T.);
#8274=FACE_OUTER_BOUND('',#9956,.T.);
#8275=FACE_OUTER_BOUND('',#9957,.T.);
#8276=FACE_OUTER_BOUND('',#9958,.T.);
#8277=FACE_OUTER_BOUND('',#9959,.T.);
#8278=FACE_OUTER_BOUND('',#9960,.T.);
#8279=FACE_OUTER_BOUND('',#9961,.T.);
#8280=FACE_OUTER_BOUND('',#9962,.T.);
#8281=FACE_OUTER_BOUND('',#9963,.T.);
#8282=FACE_OUTER_BOUND('',#9964,.T.);
#8283=FACE_OUTER_BOUND('',#9965,.T.);
#8284=FACE_OUTER_BOUND('',#9966,.T.);
#8285=FACE_OUTER_BOUND('',#9967,.T.);
#8286=FACE_OUTER_BOUND('',#9968,.T.);
#8287=FACE_OUTER_BOUND('',#9969,.T.);
#8288=FACE_OUTER_BOUND('',#9970,.T.);
#8289=FACE_OUTER_BOUND('',#9971,.T.);
#8290=FACE_OUTER_BOUND('',#9972,.T.);
#8291=FACE_OUTER_BOUND('',#9973,.T.);
#8292=FACE_OUTER_BOUND('',#9974,.T.);
#8293=FACE_OUTER_BOUND('',#9975,.T.);
#8294=FACE_OUTER_BOUND('',#9976,.T.);
#8295=FACE_OUTER_BOUND('',#9977,.T.);
#8296=FACE_OUTER_BOUND('',#9978,.T.);
#8297=FACE_OUTER_BOUND('',#9979,.T.);
#8298=FACE_OUTER_BOUND('',#9980,.T.);
#8299=FACE_OUTER_BOUND('',#9981,.T.);
#8300=FACE_OUTER_BOUND('',#9982,.T.);
#8301=FACE_OUTER_BOUND('',#9983,.T.);
#8302=FACE_OUTER_BOUND('',#9984,.T.);
#8303=FACE_OUTER_BOUND('',#9985,.T.);
#8304=FACE_OUTER_BOUND('',#9986,.T.);
#8305=FACE_OUTER_BOUND('',#9987,.T.);
#8306=FACE_OUTER_BOUND('',#9988,.T.);
#8307=FACE_OUTER_BOUND('',#9989,.T.);
#8308=FACE_OUTER_BOUND('',#9990,.T.);
#8309=FACE_OUTER_BOUND('',#9991,.T.);
#8310=FACE_OUTER_BOUND('',#9992,.T.);
#8311=FACE_OUTER_BOUND('',#9994,.T.);
#8312=FACE_OUTER_BOUND('',#10030,.T.);
#8313=FACE_OUTER_BOUND('',#10031,.T.);
#9794=EDGE_LOOP('',(#24224,#24225,#24226,#24227));
#9795=EDGE_LOOP('',(#24228,#24229,#24230,#24231));
#9796=EDGE_LOOP('',(#24232,#24233,#24234,#24235));
#9797=EDGE_LOOP('',(#24236,#24237,#24238,#24239));
#9798=EDGE_LOOP('',(#24240,#24241,#24242,#24243));
#9799=EDGE_LOOP('',(#24244,#24245,#24246,#24247));
#9800=EDGE_LOOP('',(#24248,#24249,#24250,#24251));
#9801=EDGE_LOOP('',(#24252,#24253,#24254,#24255));
#9802=EDGE_LOOP('',(#24256,#24257,#24258,#24259));
#9803=EDGE_LOOP('',(#24260,#24261,#24262,#24263));
#9804=EDGE_LOOP('',(#24264,#24265,#24266,#24267));
#9805=EDGE_LOOP('',(#24268,#24269,#24270,#24271));
#9806=EDGE_LOOP('',(#24272,#24273,#24274,#24275));
#9807=EDGE_LOOP('',(#24276,#24277,#24278,#24279));
#9808=EDGE_LOOP('',(#24280,#24281,#24282,#24283));
#9809=EDGE_LOOP('',(#24284,#24285,#24286,#24287));
#9810=EDGE_LOOP('',(#24288,#24289,#24290,#24291));
#9811=EDGE_LOOP('',(#24292,#24293,#24294,#24295));
#9812=EDGE_LOOP('',(#24296,#24297,#24298,#24299));
#9813=EDGE_LOOP('',(#24300,#24301,#24302,#24303));
#9814=EDGE_LOOP('',(#24304,#24305,#24306));
#9815=EDGE_LOOP('',(#24307,#24308,#24309,#24310,#24311));
#9816=EDGE_LOOP('',(#24312,#24313,#24314,#24315));
#9817=EDGE_LOOP('',(#24316,#24317,#24318,#24319));
#9818=EDGE_LOOP('',(#24320,#24321,#24322,#24323));
#9819=EDGE_LOOP('',(#24324,#24325,#24326,#24327));
#9820=EDGE_LOOP('',(#24328,#24329,#24330,#24331));
#9821=EDGE_LOOP('',(#24332,#24333,#24334,#24335));
#9822=EDGE_LOOP('',(#24336,#24337,#24338,#24339));
#9823=EDGE_LOOP('',(#24340,#24341,#24342,#24343));
#9824=EDGE_LOOP('',(#24344,#24345,#24346,#24347));
#9825=EDGE_LOOP('',(#24348,#24349,#24350,#24351));
#9826=EDGE_LOOP('',(#24352,#24353,#24354,#24355));
#9827=EDGE_LOOP('',(#24356,#24357,#24358,#24359));
#9828=EDGE_LOOP('',(#24360,#24361,#24362,#24363));
#9829=EDGE_LOOP('',(#24364,#24365,#24366,#24367));
#9830=EDGE_LOOP('',(#24368,#24369,#24370,#24371));
#9831=EDGE_LOOP('',(#24372,#24373,#24374,#24375));
#9832=EDGE_LOOP('',(#24376,#24377,#24378,#24379));
#9833=EDGE_LOOP('',(#24380,#24381,#24382,#24383));
#9834=EDGE_LOOP('',(#24384,#24385,#24386,#24387,#24388,#24389,#24390,#24391,
#24392,#24393,#24394,#24395,#24396,#24397,#24398,#24399,#24400,#24401,#24402,
#24403,#24404,#24405,#24406,#24407,#24408,#24409,#24410,#24411,#24412,#24413,
#24414,#24415,#24416,#24417,#24418,#24419,#24420,#24421,#24422,#24423,#24424,
#24425,#24426));
#9835=EDGE_LOOP('',(#24427,#24428,#24429,#24430,#24431));
#9836=EDGE_LOOP('',(#24432,#24433,#24434,#24435));
#9837=EDGE_LOOP('',(#24436,#24437,#24438,#24439,#24440,#24441,#24442,#24443,
#24444,#24445,#24446,#24447,#24448,#24449,#24450,#24451,#24452,#24453,#24454,
#24455,#24456,#24457,#24458,#24459,#24460,#24461,#24462,#24463,#24464,#24465,
#24466,#24467,#24468,#24469,#24470,#24471,#24472,#24473,#24474,#24475,#24476,
#24477,#24478,#24479));
#9838=EDGE_LOOP('',(#24480,#24481,#24482,#24483));
#9839=EDGE_LOOP('',(#24484,#24485,#24486));
#9840=EDGE_LOOP('',(#24487,#24488,#24489,#24490));
#9841=EDGE_LOOP('',(#24491,#24492,#24493));
#9842=EDGE_LOOP('',(#24494,#24495,#24496,#24497));
#9843=EDGE_LOOP('',(#24498,#24499,#24500));
#9844=EDGE_LOOP('',(#24501,#24502,#24503,#24504));
#9845=EDGE_LOOP('',(#24505,#24506,#24507));
#9846=EDGE_LOOP('',(#24508,#24509,#24510,#24511));
#9847=EDGE_LOOP('',(#24512,#24513,#24514));
#9848=EDGE_LOOP('',(#24515,#24516,#24517,#24518));
#9849=EDGE_LOOP('',(#24519,#24520,#24521));
#9850=EDGE_LOOP('',(#24522,#24523,#24524,#24525));
#9851=EDGE_LOOP('',(#24526,#24527,#24528));
#9852=EDGE_LOOP('',(#24529,#24530,#24531,#24532));
#9853=EDGE_LOOP('',(#24533,#24534,#24535));
#9854=EDGE_LOOP('',(#24536,#24537,#24538,#24539));
#9855=EDGE_LOOP('',(#24540,#24541,#24542));
#9856=EDGE_LOOP('',(#24543,#24544,#24545,#24546));
#9857=EDGE_LOOP('',(#24547,#24548,#24549));
#9858=EDGE_LOOP('',(#24550,#24551,#24552,#24553));
#9859=EDGE_LOOP('',(#24554,#24555,#24556));
#9860=EDGE_LOOP('',(#24557,#24558,#24559,#24560));
#9861=EDGE_LOOP('',(#24561,#24562,#24563));
#9862=EDGE_LOOP('',(#24564,#24565,#24566,#24567));
#9863=EDGE_LOOP('',(#24568,#24569,#24570));
#9864=EDGE_LOOP('',(#24571,#24572,#24573,#24574));
#9865=EDGE_LOOP('',(#24575,#24576,#24577));
#9866=EDGE_LOOP('',(#24578,#24579,#24580,#24581));
#9867=EDGE_LOOP('',(#24582,#24583,#24584));
#9868=EDGE_LOOP('',(#24585,#24586,#24587,#24588));
#9869=EDGE_LOOP('',(#24589,#24590,#24591));
#9870=EDGE_LOOP('',(#24592,#24593,#24594,#24595));
#9871=EDGE_LOOP('',(#24596,#24597,#24598));
#9872=EDGE_LOOP('',(#24599,#24600,#24601,#24602));
#9873=EDGE_LOOP('',(#24603,#24604,#24605));
#9874=EDGE_LOOP('',(#24606,#24607,#24608,#24609));
#9875=EDGE_LOOP('',(#24610,#24611,#24612));
#9876=EDGE_LOOP('',(#24613,#24614,#24615,#24616));
#9877=EDGE_LOOP('',(#24617,#24618,#24619));
#9878=EDGE_LOOP('',(#24620,#24621,#24622,#24623));
#9879=EDGE_LOOP('',(#24624,#24625,#24626));
#9880=EDGE_LOOP('',(#24627,#24628,#24629,#24630));
#9881=EDGE_LOOP('',(#24631,#24632,#24633));
#9882=EDGE_LOOP('',(#24634,#24635,#24636,#24637));
#9883=EDGE_LOOP('',(#24638,#24639,#24640));
#9884=EDGE_LOOP('',(#24641,#24642,#24643,#24644));
#9885=EDGE_LOOP('',(#24645,#24646,#24647));
#9886=EDGE_LOOP('',(#24648,#24649,#24650,#24651));
#9887=EDGE_LOOP('',(#24652,#24653,#24654));
#9888=EDGE_LOOP('',(#24655,#24656,#24657,#24658));
#9889=EDGE_LOOP('',(#24659,#24660,#24661));
#9890=EDGE_LOOP('',(#24662,#24663,#24664,#24665));
#9891=EDGE_LOOP('',(#24666,#24667,#24668));
#9892=EDGE_LOOP('',(#24669,#24670,#24671,#24672));
#9893=EDGE_LOOP('',(#24673,#24674,#24675));
#9894=EDGE_LOOP('',(#24676,#24677,#24678,#24679));
#9895=EDGE_LOOP('',(#24680,#24681,#24682));
#9896=EDGE_LOOP('',(#24683,#24684,#24685,#24686));
#9897=EDGE_LOOP('',(#24687,#24688,#24689));
#9898=EDGE_LOOP('',(#24690,#24691,#24692,#24693));
#9899=EDGE_LOOP('',(#24694,#24695,#24696));
#9900=EDGE_LOOP('',(#24697,#24698,#24699,#24700));
#9901=EDGE_LOOP('',(#24701,#24702,#24703));
#9902=EDGE_LOOP('',(#24704,#24705,#24706,#24707));
#9903=EDGE_LOOP('',(#24708,#24709,#24710));
#9904=EDGE_LOOP('',(#24711,#24712,#24713,#24714));
#9905=EDGE_LOOP('',(#24715,#24716,#24717));
#9906=EDGE_LOOP('',(#24718,#24719,#24720,#24721));
#9907=EDGE_LOOP('',(#24722,#24723,#24724,#24725));
#9908=EDGE_LOOP('',(#24726,#24727,#24728,#24729));
#9909=EDGE_LOOP('',(#24730,#24731,#24732,#24733));
#9910=EDGE_LOOP('',(#24734,#24735,#24736,#24737));
#9911=EDGE_LOOP('',(#24738,#24739,#24740));
#9912=EDGE_LOOP('',(#24741,#24742,#24743,#24744));
#9913=EDGE_LOOP('',(#24745,#24746,#24747));
#9914=EDGE_LOOP('',(#24748,#24749,#24750,#24751));
#9915=EDGE_LOOP('',(#24752,#24753,#24754));
#9916=EDGE_LOOP('',(#24755,#24756,#24757,#24758));
#9917=EDGE_LOOP('',(#24759,#24760,#24761));
#9918=EDGE_LOOP('',(#24762,#24763,#24764,#24765));
#9919=EDGE_LOOP('',(#24766,#24767,#24768));
#9920=EDGE_LOOP('',(#24769,#24770,#24771,#24772));
#9921=EDGE_LOOP('',(#24773,#24774,#24775));
#9922=EDGE_LOOP('',(#24776,#24777,#24778,#24779));
#9923=EDGE_LOOP('',(#24780,#24781,#24782));
#9924=EDGE_LOOP('',(#24783,#24784,#24785,#24786));
#9925=EDGE_LOOP('',(#24787,#24788,#24789));
#9926=EDGE_LOOP('',(#24790,#24791,#24792,#24793));
#9927=EDGE_LOOP('',(#24794,#24795,#24796));
#9928=EDGE_LOOP('',(#24797,#24798,#24799,#24800));
#9929=EDGE_LOOP('',(#24801,#24802,#24803));
#9930=EDGE_LOOP('',(#24804,#24805,#24806,#24807));
#9931=EDGE_LOOP('',(#24808,#24809,#24810));
#9932=EDGE_LOOP('',(#24811,#24812,#24813,#24814));
#9933=EDGE_LOOP('',(#24815,#24816,#24817));
#9934=EDGE_LOOP('',(#24818,#24819,#24820,#24821));
#9935=EDGE_LOOP('',(#24822,#24823,#24824));
#9936=EDGE_LOOP('',(#24825,#24826,#24827,#24828));
#9937=EDGE_LOOP('',(#24829,#24830,#24831));
#9938=EDGE_LOOP('',(#24832,#24833,#24834,#24835));
#9939=EDGE_LOOP('',(#24836,#24837,#24838));
#9940=EDGE_LOOP('',(#24839,#24840,#24841,#24842));
#9941=EDGE_LOOP('',(#24843,#24844,#24845));
#9942=EDGE_LOOP('',(#24846,#24847,#24848,#24849));
#9943=EDGE_LOOP('',(#24850,#24851,#24852));
#9944=EDGE_LOOP('',(#24853,#24854,#24855,#24856));
#9945=EDGE_LOOP('',(#24857,#24858,#24859));
#9946=EDGE_LOOP('',(#24860,#24861,#24862,#24863));
#9947=EDGE_LOOP('',(#24864,#24865,#24866));
#9948=EDGE_LOOP('',(#24867,#24868,#24869,#24870));
#9949=EDGE_LOOP('',(#24871,#24872,#24873));
#9950=EDGE_LOOP('',(#24874,#24875,#24876,#24877));
#9951=EDGE_LOOP('',(#24878,#24879,#24880));
#9952=EDGE_LOOP('',(#24881,#24882,#24883,#24884));
#9953=EDGE_LOOP('',(#24885,#24886,#24887));
#9954=EDGE_LOOP('',(#24888,#24889,#24890,#24891));
#9955=EDGE_LOOP('',(#24892,#24893,#24894));
#9956=EDGE_LOOP('',(#24895,#24896,#24897,#24898));
#9957=EDGE_LOOP('',(#24899,#24900,#24901));
#9958=EDGE_LOOP('',(#24902,#24903,#24904,#24905));
#9959=EDGE_LOOP('',(#24906,#24907,#24908));
#9960=EDGE_LOOP('',(#24909,#24910,#24911,#24912));
#9961=EDGE_LOOP('',(#24913,#24914,#24915));
#9962=EDGE_LOOP('',(#24916,#24917,#24918,#24919));
#9963=EDGE_LOOP('',(#24920,#24921,#24922));
#9964=EDGE_LOOP('',(#24923,#24924,#24925,#24926));
#9965=EDGE_LOOP('',(#24927,#24928,#24929));
#9966=EDGE_LOOP('',(#24930,#24931,#24932,#24933));
#9967=EDGE_LOOP('',(#24934,#24935,#24936));
#9968=EDGE_LOOP('',(#24937,#24938,#24939,#24940));
#9969=EDGE_LOOP('',(#24941,#24942,#24943));
#9970=EDGE_LOOP('',(#24944,#24945,#24946,#24947));
#9971=EDGE_LOOP('',(#24948,#24949,#24950));
#9972=EDGE_LOOP('',(#24951,#24952,#24953,#24954));
#9973=EDGE_LOOP('',(#24955,#24956,#24957));
#9974=EDGE_LOOP('',(#24958,#24959,#24960,#24961));
#9975=EDGE_LOOP('',(#24962,#24963,#24964));
#9976=EDGE_LOOP('',(#24965,#24966,#24967,#24968));
#9977=EDGE_LOOP('',(#24969,#24970,#24971));
#9978=EDGE_LOOP('',(#24972,#24973,#24974,#24975));
#9979=EDGE_LOOP('',(#24976,#24977,#24978));
#9980=EDGE_LOOP('',(#24979,#24980,#24981,#24982));
#9981=EDGE_LOOP('',(#24983,#24984,#24985));
#9982=EDGE_LOOP('',(#24986,#24987,#24988,#24989));
#9983=EDGE_LOOP('',(#24990,#24991,#24992,#24993));
#9984=EDGE_LOOP('',(#24994,#24995,#24996,#24997));
#9985=EDGE_LOOP('',(#24998,#24999,#25000,#25001));
#9986=EDGE_LOOP('',(#25002,#25003,#25004,#25005));
#9987=EDGE_LOOP('',(#25006,#25007,#25008,#25009));
#9988=EDGE_LOOP('',(#25010,#25011,#25012,#25013,#25014,#25015));
#9989=EDGE_LOOP('',(#25016));
#9990=EDGE_LOOP('',(#25017,#25018,#25019,#25020,#25021,#25022));
#9991=EDGE_LOOP('',(#25023,#25024,#25025,#25026));
#9992=EDGE_LOOP('',(#25027));
#9993=EDGE_LOOP('',(#25028,#25029,#25030,#25031,#25032));
#9994=EDGE_LOOP('',(#25033,#25034,#25035,#25036,#25037,#25038,#25039,#25040,
#25041,#25042,#25043,#25044));
#9995=EDGE_LOOP('',(#25045,#25046,#25047,#25048));
#9996=EDGE_LOOP('',(#25049,#25050,#25051,#25052));
#9997=EDGE_LOOP('',(#25053,#25054,#25055,#25056));
#9998=EDGE_LOOP('',(#25057,#25058,#25059,#25060));
#9999=EDGE_LOOP('',(#25061,#25062,#25063,#25064));
#10000=EDGE_LOOP('',(#25065,#25066,#25067,#25068));
#10001=EDGE_LOOP('',(#25069,#25070,#25071,#25072));
#10002=EDGE_LOOP('',(#25073,#25074,#25075,#25076));
#10003=EDGE_LOOP('',(#25077,#25078,#25079,#25080));
#10004=EDGE_LOOP('',(#25081,#25082,#25083,#25084));
#10005=EDGE_LOOP('',(#25085,#25086,#25087,#25088));
#10006=EDGE_LOOP('',(#25089,#25090,#25091,#25092));
#10007=EDGE_LOOP('',(#25093,#25094,#25095,#25096));
#10008=EDGE_LOOP('',(#25097,#25098,#25099,#25100));
#10009=EDGE_LOOP('',(#25101,#25102,#25103,#25104));
#10010=EDGE_LOOP('',(#25105,#25106,#25107,#25108));
#10011=EDGE_LOOP('',(#25109,#25110,#25111,#25112));
#10012=EDGE_LOOP('',(#25113,#25114,#25115,#25116));
#10013=EDGE_LOOP('',(#25117,#25118,#25119,#25120));
#10014=EDGE_LOOP('',(#25121,#25122,#25123,#25124));
#10015=EDGE_LOOP('',(#25125,#25126,#25127,#25128));
#10016=EDGE_LOOP('',(#25129,#25130,#25131,#25132));
#10017=EDGE_LOOP('',(#25133,#25134,#25135,#25136));
#10018=EDGE_LOOP('',(#25137,#25138,#25139,#25140));
#10019=EDGE_LOOP('',(#25141,#25142,#25143,#25144));
#10020=EDGE_LOOP('',(#25145,#25146,#25147,#25148));
#10021=EDGE_LOOP('',(#25149,#25150,#25151,#25152));
#10022=EDGE_LOOP('',(#25153,#25154,#25155,#25156));
#10023=EDGE_LOOP('',(#25157,#25158,#25159,#25160));
#10024=EDGE_LOOP('',(#25161,#25162,#25163,#25164));
#10025=EDGE_LOOP('',(#25165,#25166,#25167,#25168));
#10026=EDGE_LOOP('',(#25169,#25170,#25171,#25172));
#10027=EDGE_LOOP('',(#25173,#25174,#25175,#25176));
#10028=EDGE_LOOP('',(#25177,#25178,#25179,#25180));
#10029=EDGE_LOOP('',(#25181,#25182,#25183,#25184));
#10030=EDGE_LOOP('',(#25185,#25186,#25187,#25188));
#10031=EDGE_LOOP('',(#25189));
#10032=EDGE_LOOP('',(#25190,#25191,#25192,#25193,#25194,#25195));
#10881=CIRCLE('',#29562,4.925);
#10882=CIRCLE('',#29583,4.0705);
#10883=CIRCLE('',#29585,4.0705);
#10884=CIRCLE('',#29605,4.925);
#10885=CIRCLE('',#29606,4.925);
#10886=CIRCLE('',#29607,4.0705);
#10887=CIRCLE('',#29611,8.);
#10888=CIRCLE('',#29614,8.);
#10889=CIRCLE('',#29617,8.);
#10890=CIRCLE('',#29620,8.);
#10891=CIRCLE('',#29623,8.);
#10892=CIRCLE('',#29626,8.);
#10893=CIRCLE('',#29629,8.);
#10894=CIRCLE('',#29632,8.);
#10895=CIRCLE('',#29635,8.);
#10896=CIRCLE('',#29638,8.);
#10897=CIRCLE('',#29641,8.);
#10898=CIRCLE('',#29644,8.);
#10899=CIRCLE('',#29647,8.);
#10900=CIRCLE('',#29650,8.);
#10901=CIRCLE('',#29653,8.);
#10902=CIRCLE('',#29656,8.);
#10903=CIRCLE('',#29659,8.);
#10904=CIRCLE('',#29662,8.);
#10905=CIRCLE('',#29665,8.);
#10906=CIRCLE('',#29668,8.);
#10907=CIRCLE('',#29671,8.);
#10908=CIRCLE('',#29674,8.);
#10909=CIRCLE('',#29677,8.);
#10910=CIRCLE('',#29680,8.);
#10911=CIRCLE('',#29683,8.);
#10912=CIRCLE('',#29686,8.);
#10913=CIRCLE('',#29689,8.);
#10914=CIRCLE('',#29692,8.);
#10915=CIRCLE('',#29695,8.);
#10916=CIRCLE('',#29698,8.);
#10917=CIRCLE('',#29701,8.);
#10918=CIRCLE('',#29704,8.);
#10919=CIRCLE('',#29707,8.);
#10920=CIRCLE('',#29710,8.);
#10921=CIRCLE('',#29713,8.);
#10922=CIRCLE('',#29714,8.);
#10923=CIRCLE('',#29717,8.);
#10924=CIRCLE('',#29718,8.);
#10925=CIRCLE('',#29721,8.);
#10926=CIRCLE('',#29724,8.);
#10927=CIRCLE('',#29727,8.);
#10928=CIRCLE('',#29730,8.);
#10929=CIRCLE('',#29733,8.);
#10930=CIRCLE('',#29736,8.);
#10931=CIRCLE('',#29739,8.);
#10932=CIRCLE('',#29742,8.);
#10933=CIRCLE('',#29745,8.);
#10934=CIRCLE('',#29748,8.);
#10935=CIRCLE('',#29751,8.);
#10936=CIRCLE('',#29754,8.);
#10937=CIRCLE('',#29757,8.);
#10938=CIRCLE('',#29760,8.);
#10939=CIRCLE('',#29763,8.);
#10940=CIRCLE('',#29766,8.);
#10941=CIRCLE('',#29769,8.);
#10942=CIRCLE('',#29772,8.);
#10943=CIRCLE('',#29775,8.);
#10944=CIRCLE('',#29778,8.);
#10945=CIRCLE('',#29781,8.);
#10946=CIRCLE('',#29784,8.);
#10947=CIRCLE('',#29787,8.);
#10948=CIRCLE('',#29790,8.);
#10949=CIRCLE('',#29793,8.);
#10950=CIRCLE('',#29796,8.);
#10951=CIRCLE('',#29799,8.);
#10952=CIRCLE('',#29802,8.);
#10953=CIRCLE('',#29805,8.);
#10954=CIRCLE('',#29808,8.);
#10955=CIRCLE('',#29811,8.);
#10956=CIRCLE('',#29814,8.);
#10957=CIRCLE('',#29817,8.);
#10958=CIRCLE('',#29820,8.);
#10959=CIRCLE('',#29823,8.);
#10960=CIRCLE('',#29826,8.);
#10961=CIRCLE('',#29835,4.5);
#10962=CIRCLE('',#29838,4.925);
#10963=CIRCLE('',#29840,8.);
#10964=CIRCLE('',#29842,8.);
#10965=CIRCLE('',#29844,7.5);
#11312=B_SPLINE_CURVE_WITH_KNOTS('',3,(#49733,#49734,#49735,#49736,#49737,
#49738,#49739,#49740,#49741,#49742),.UNSPECIFIED.,.F.,.F.,(4,3,3,4),(-4.0932327200247,
-3.99841245657804,-2.99880934243353,-2.06652207565086),.UNSPECIFIED.);
#11313=B_SPLINE_CURVE_WITH_KNOTS('',3,(#49745,#49746,#49747,#49748,#49749,
#49750,#49751,#49752,#49753,#49754),.UNSPECIFIED.,.F.,.F.,(4,3,3,4),(0.,
0.499801557072245,0.999603114144509,1.11488200921585),.UNSPECIFIED.);
#11314=B_SPLINE_CURVE_WITH_KNOTS('',3,(#49759,#49760,#49761,#49762,#49763,
#49764,#49765,#49766,#49767,#49768,#49769,#49770,#49771,#49772,#49773,#49774,
#49775,#49776,#49777,#49778,#49779,#49780),.UNSPECIFIED.,.F.,.F.,(4,3,3,
3,3,3,3,4),(-10.3764180272043,-9.99603114144511,-8.9964280273006,-7.99682491315609,
-6.99722179901157,-5.99761868486707,-4.99801557072256,-4.0932327200247),
 .UNSPECIFIED.);
#11315=B_SPLINE_CURVE_WITH_KNOTS('',3,(#49781,#49782,#49783,#49784,#49785,
#49786,#49787,#49788,#49789,#49790,#49791,#49792,#49793,#49794,#49795,#49796,
#49797,#49798,#49799,#49800,#49801,#49802),.UNSPECIFIED.,.F.,.F.,(4,3,3,
3,3,3,3,4),(1.11488200921585,1.99920622828902,2.99880934243353,3.99841245657804,
4.99801557072255,5.99761868486706,6.99722179901157,7.39806731639545),
 .UNSPECIFIED.);
#11316=B_SPLINE_CURVE_WITH_KNOTS('',3,(#49807,#49808,#49809,#49810,#49811,
#49812,#49813,#49814,#49815,#49816,#49817,#49818,#49819,#49820,#49821,#49822,
#49823,#49824,#49825,#49826,#49827,#49828),.UNSPECIFIED.,.F.,.F.,(4,3,3,
3,3,3,3,4),(-16.6596033343839,-15.9936498263122,-14.9940467121677,-13.9944435980232,
-12.9948404838786,-11.9952373697341,-10.9956342555896,-10.3764180272043),
 .UNSPECIFIED.);
#11317=B_SPLINE_CURVE_WITH_KNOTS('',3,(#49829,#49830,#49831,#49832,#49833,
#49834,#49835,#49836,#49837,#49838,#49839,#49840,#49841,#49842,#49843,#49844,
#49845,#49846,#49847,#49848,#49849,#49850),.UNSPECIFIED.,.F.,.F.,(4,3,3,
3,3,3,3,4),(7.39806731639545,7.99682491315608,8.9964280273006,9.99603114144511,
10.9956342555896,11.9952373697341,12.9948404838786,13.681252623575),
 .UNSPECIFIED.);
#11318=B_SPLINE_CURVE_WITH_KNOTS('',3,(#49855,#49856,#49857,#49858,#49859,
#49860,#49861,#49862,#49863,#49864,#49865,#49866,#49867,#49868,#49869,#49870,
#49871,#49872,#49873,#49874,#49875,#49876),.UNSPECIFIED.,.F.,.F.,(4,3,3,
3,3,3,3,4),(-22.9427886415635,-21.9912685111792,-20.9916653970347,-19.9920622828902,
-18.9924591687457,-17.9928560546012,-16.9932529404567,-16.6596033343839),
 .UNSPECIFIED.);
#11319=B_SPLINE_CURVE_WITH_KNOTS('',3,(#49877,#49878,#49879,#49880,#49881,
#49882,#49883,#49884,#49885,#49886,#49887,#49888,#49889,#49890,#49891,#49892,
#49893,#49894,#49895,#49896,#49897,#49898),.UNSPECIFIED.,.F.,.F.,(4,3,3,
3,3,3,3,4),(13.681252623575,13.9944435980232,14.9940467121677,15.9936498263122,
16.9932529404567,17.9928560546012,18.9924591687457,19.9644379307546),
 .UNSPECIFIED.);
#11320=B_SPLINE_CURVE_WITH_KNOTS('',3,(#49903,#49904,#49905,#49906,#49907,
#49908,#49909,#49910,#49911,#49912,#49913,#49914,#49915,#49916,#49917,#49918,
#49919,#49920,#49921,#49922,#49923,#49924,#49925,#49926,#49927),
 .UNSPECIFIED.,.F.,.F.,(4,3,3,3,3,3,3,3,4),(-29.225973948743,-28.9884903101908,
-27.9888871960463,-26.9892840819018,-25.9896809677573,-24.9900778536128,
-23.9904747394683,-22.9908716253238,-22.9427886415635),.UNSPECIFIED.);
#11321=B_SPLINE_CURVE_WITH_KNOTS('',3,(#49928,#49929,#49930,#49931,#49932,
#49933,#49934,#49935,#49936,#49937,#49938,#49939,#49940,#49941,#49942,#49943,
#49944,#49945,#49946,#49947,#49948,#49949,#49950,#49951,#49952),
 .UNSPECIFIED.,.F.,.F.,(4,3,3,3,3,3,3,3,4),(19.9644379307546,19.9920622828902,
20.9916653970347,21.9912685111792,22.9908716253238,23.9904747394683,24.9900778536128,
25.9896809677573,26.2476232379342),.UNSPECIFIED.);
#11322=B_SPLINE_CURVE_WITH_KNOTS('',3,(#49957,#49958,#49959,#49960,#49961,
#49962,#49963,#49964,#49965,#49966,#49967,#49968,#49969,#49970,#49971,#49972,
#49973,#49974,#49975,#49976,#49977,#49978),.UNSPECIFIED.,.F.,.F.,(4,3,3,
3,3,3,3,4),(-35.5091592559226,-34.9861089950579,-33.9865058809134,-32.9869027667689,
-31.9872996526244,-30.9876965384798,-29.9880934243353,-29.225973948743),
 .UNSPECIFIED.);
#11323=B_SPLINE_CURVE_WITH_KNOTS('',3,(#49979,#49980,#49981,#49982,#49983,
#49984,#49985,#49986,#49987,#49988,#49989,#49990,#49991,#49992,#49993,#49994,
#49995,#49996,#49997,#49998,#49999,#50000),.UNSPECIFIED.,.F.,.F.,(4,3,3,
3,3,3,3,4),(26.2476232379342,26.9892840819018,27.9888871960463,28.9884903101908,
29.9880934243353,30.9876965384798,31.9872996526244,32.5308085451138),
 .UNSPECIFIED.);
#11324=B_SPLINE_CURVE_WITH_KNOTS('',3,(#50005,#50006,#50007,#50008,#50009,
#50010,#50011,#50012,#50013,#50014,#50015,#50016,#50017,#50018,#50019,#50020,
#50021,#50022,#50023,#50024,#50025,#50026),.UNSPECIFIED.,.F.,.F.,(4,3,3,
3,3,3,3,4),(-41.7923445631022,-40.9837276799249,-39.9841245657804,-38.9845214516359,
-37.9849183374914,-36.9853152233469,-35.9857121092024,-35.5091592559226),
 .UNSPECIFIED.);
#11325=B_SPLINE_CURVE_WITH_KNOTS('',3,(#50027,#50028,#50029,#50030,#50031,
#50032,#50033,#50034,#50035,#50036,#50037,#50038,#50039,#50040,#50041,#50042,
#50043,#50044,#50045,#50046,#50047,#50048),.UNSPECIFIED.,.F.,.F.,(4,3,3,
3,3,3,3,4),(32.5308085451138,32.9869027667689,33.9865058809134,34.9861089950579,
35.9857121092024,36.9853152233469,37.9849183374914,38.8139938522934),
 .UNSPECIFIED.);
#11326=B_SPLINE_CURVE_WITH_KNOTS('',3,(#50053,#50054,#50055,#50056,#50057,
#50058,#50059,#50060,#50061,#50062,#50063,#50064,#50065,#50066,#50067,#50068,
#50069,#50070,#50071,#50072,#50073,#50074,#50075,#50076,#50077),
 .UNSPECIFIED.,.F.,.F.,(4,3,3,3,3,3,3,3,4),(-48.0755298702818,-47.9809494789365,
-46.981346364792,-45.9817432506475,-44.982140136503,-43.9825370223585,-42.982933908214,
-41.9833307940695,-41.7923445631022),.UNSPECIFIED.);
#11327=B_SPLINE_CURVE_WITH_KNOTS('',3,(#50078,#50079,#50080,#50081,#50082,
#50083,#50084,#50085,#50086,#50087,#50088,#50089,#50090,#50091,#50092,#50093,
#50094,#50095,#50096,#50097,#50098,#50099,#50100,#50101,#50102),
 .UNSPECIFIED.,.F.,.F.,(4,3,3,3,3,3,3,3,4),(38.8139938522934,38.9845214516359,
39.9841245657804,40.983727679925,41.9833307940695,42.982933908214,43.9825370223585,
44.982140136503,45.097179159473),.UNSPECIFIED.);
#11328=B_SPLINE_CURVE_WITH_KNOTS('',3,(#50107,#50108,#50109,#50110,#50111,
#50112,#50113,#50114,#50115,#50116,#50117,#50118,#50119,#50120,#50121,#50122,
#50123,#50124,#50125,#50126,#50127,#50128),.UNSPECIFIED.,.F.,.F.,(4,3,3,
3,3,3,3,4),(-54.3587151774614,-53.9785681638036,-52.9789650496591,-51.9793619355146,
-50.9797588213701,-49.9801557072255,-48.980552593081,-48.0755298702818),
 .UNSPECIFIED.);
#11329=B_SPLINE_CURVE_WITH_KNOTS('',3,(#50129,#50130,#50131,#50132,#50133,
#50134,#50135,#50136,#50137,#50138,#50139,#50140,#50141,#50142,#50143,#50144,
#50145,#50146,#50147,#50148,#50149,#50150),.UNSPECIFIED.,.F.,.F.,(4,3,3,
3,3,3,3,4),(45.097179159473,45.9817432506475,46.981346364792,47.9809494789365,
48.980552593081,49.9801557072255,50.97975882137,51.3803644666526),
 .UNSPECIFIED.);
#11330=B_SPLINE_CURVE_WITH_KNOTS('',3,(#50155,#50156,#50157,#50158,#50159,
#50160,#50161,#50162,#50163,#50164,#50165,#50166,#50167,#50168,#50169,#50170,
#50171,#50172,#50173,#50174,#50175,#50176),.UNSPECIFIED.,.F.,.F.,(4,3,3,
3,3,3,3,4),(-60.641900484641,-59.9761868486707,-58.9765837345262,-57.9769806203817,
-56.9773775062371,-55.9777743920926,-54.9781712779481,-54.3587151774614),
 .UNSPECIFIED.);
#11331=B_SPLINE_CURVE_WITH_KNOTS('',3,(#50177,#50178,#50179,#50180,#50181,
#50182,#50183,#50184,#50185,#50186,#50187,#50188,#50189,#50190,#50191,#50192,
#50193,#50194,#50195,#50196,#50197,#50198),.UNSPECIFIED.,.F.,.F.,(4,3,3,
3,3,3,3,4),(51.3803644666526,51.9793619355146,52.9789650496591,53.9785681638036,
54.9781712779481,55.9777743920926,56.9773775062371,57.6635497738322),
 .UNSPECIFIED.);
#11332=B_SPLINE_CURVE_WITH_KNOTS('',3,(#50203,#50204,#50205,#50206,#50207,
#50208,#50209,#50210,#50211,#50212,#50213,#50214,#50215,#50216,#50217,#50218,
#50219,#50220,#50221,#50222,#50223,#50224),.UNSPECIFIED.,.F.,.F.,(4,3,3,
3,3,3,3,4),(-66.9250857918206,-65.9738055335377,-64.9742024193932,-63.9745993052487,
-62.9749961911042,-61.9753930769597,-60.9757899628152,-60.641900484641),
 .UNSPECIFIED.);
#11333=B_SPLINE_CURVE_WITH_KNOTS('',3,(#50225,#50226,#50227,#50228,#50229,
#50230,#50231,#50232,#50233,#50234,#50235,#50236,#50237,#50238,#50239,#50240,
#50241,#50242,#50243,#50244,#50245,#50246),.UNSPECIFIED.,.F.,.F.,(4,3,3,
3,3,3,3,4),(57.6635497738322,57.9769806203816,58.9765837345261,59.9761868486707,
60.9757899628152,61.9753930769597,62.9749961911042,63.9467350810118),
 .UNSPECIFIED.);
#11334=B_SPLINE_CURVE_WITH_KNOTS('',3,(#50251,#50252,#50253,#50254,#50255,
#50256,#50257,#50258,#50259,#50260,#50261,#50262,#50263,#50264,#50265,#50266,
#50267,#50268,#50269,#50270,#50271,#50272,#50273,#50274,#50275),
 .UNSPECIFIED.,.F.,.F.,(4,3,3,3,3,3,3,3,4),(-73.2082710990002,-72.9710273325493,
-71.9714242184048,-70.9718211042603,-69.9722179901158,-68.9726148759713,
-67.9730117618268,-66.9734086476822,-66.9250857918206),.UNSPECIFIED.);
#11335=B_SPLINE_CURVE_WITH_KNOTS('',3,(#50276,#50277,#50278,#50279,#50280,
#50281,#50282,#50283,#50284,#50285,#50286,#50287,#50288,#50289,#50290,#50291,
#50292,#50293,#50294,#50295,#50296,#50297,#50298,#50299,#50300),
 .UNSPECIFIED.,.F.,.F.,(4,3,3,3,3,3,3,3,4),(63.9467350810118,63.9745993052487,
64.9742024193932,65.9738055335377,66.9734086476822,67.9730117618267,68.9726148759712,
69.9722179901158,70.2299203881913),.UNSPECIFIED.);
#11336=B_SPLINE_CURVE_WITH_KNOTS('',3,(#50305,#50306,#50307,#50308,#50309,
#50310,#50311,#50312,#50313,#50314,#50315,#50316,#50317,#50318,#50319,#50320,
#50321,#50322,#50323,#50324,#50325,#50326),.UNSPECIFIED.,.F.,.F.,(4,3,3,
3,3,3,3,4),(-79.4914564061798,-78.9686460174164,-77.9690429032719,-76.9694397891273,
-75.9698366749828,-74.9702335608383,-73.9706304466938,-73.2082710990002),
 .UNSPECIFIED.);
#11337=B_SPLINE_CURVE_WITH_KNOTS('',3,(#50327,#50328,#50329,#50330,#50331,
#50332,#50333,#50334,#50335,#50336,#50337,#50338,#50339,#50340,#50341,#50342,
#50343,#50344,#50345,#50346,#50347,#50348),.UNSPECIFIED.,.F.,.F.,(4,3,3,
3,3,3,3,4),(70.2299203881913,70.9718211042603,71.9714242184048,72.9710273325493,
73.9706304466938,74.9702335608383,75.9698366749828,76.5131056953709),
 .UNSPECIFIED.);
#11338=B_SPLINE_CURVE_WITH_KNOTS('',3,(#50353,#50354,#50355,#50356,#50357,
#50358,#50359,#50360,#50361,#50362,#50363,#50364,#50365,#50366,#50367,#50368,
#50369,#50370,#50371,#50372,#50373,#50374),.UNSPECIFIED.,.F.,.F.,(4,3,3,
3,3,3,3,4),(-85.7746417133594,-84.9662647022835,-83.9666615881389,-82.9670584739944,
-81.9674553598499,-80.9678522457054,-79.9682491315609,-79.4914564061798),
 .UNSPECIFIED.);
#11339=B_SPLINE_CURVE_WITH_KNOTS('',3,(#50375,#50376,#50377,#50378,#50379,
#50380,#50381,#50382,#50383,#50384,#50385,#50386,#50387,#50388,#50389,#50390,
#50391,#50392,#50393,#50394,#50395,#50396),.UNSPECIFIED.,.F.,.F.,(4,3,3,
3,3,3,3,4),(76.5131056953709,76.9694397891273,77.9690429032718,78.9686460174164,
79.9682491315609,80.9678522457054,81.9674553598499,82.7962910025505),
 .UNSPECIFIED.);
#11340=B_SPLINE_CURVE_WITH_KNOTS('',3,(#50401,#50402,#50403,#50404,#50405,
#50406,#50407,#50408,#50409,#50410,#50411,#50412,#50413,#50414,#50415,#50416,
#50417,#50418,#50419,#50420,#50421,#50422,#50423,#50424,#50425),
 .UNSPECIFIED.,.F.,.F.,(4,3,3,3,3,3,3,3,4),(-92.057827020539,-91.963486501295,
-90.9638833871505,-89.964280273006,-88.9646771588615,-87.965074044717,-86.9654709305725,
-85.965867816428,-85.7746417133594),.UNSPECIFIED.);
#11341=B_SPLINE_CURVE_WITH_KNOTS('',3,(#50426,#50427,#50428,#50429,#50430,
#50431,#50432,#50433,#50434,#50435,#50436,#50437,#50438,#50439,#50440,#50441,
#50442,#50443,#50444,#50445,#50446,#50447,#50448,#50449,#50450),
 .UNSPECIFIED.,.F.,.F.,(4,3,3,3,3,3,3,3,4),(82.7962910025505,82.9670584739944,
83.9666615881389,84.9662647022834,85.9658678164279,86.9654709305725,87.965074044717,
88.9646771588615,89.0794763097301),.UNSPECIFIED.);
#11342=B_SPLINE_CURVE_WITH_KNOTS('',3,(#50455,#50456,#50457,#50458,#50459,
#50460,#50461,#50462,#50463,#50464,#50465,#50466,#50467,#50468,#50469,#50470,
#50471,#50472,#50473,#50474,#50475,#50476),.UNSPECIFIED.,.F.,.F.,(4,3,3,
3,3,3,3,4),(-98.3410123277186,-97.9611051861621,-96.9615020720176,-95.961898957873,
-94.9622958437285,-93.962692729584,-92.9630896154395,-92.057827020539),
 .UNSPECIFIED.);
#11343=B_SPLINE_CURVE_WITH_KNOTS('',3,(#50477,#50478,#50479,#50480,#50481,
#50482,#50483,#50484,#50485,#50486,#50487,#50488,#50489,#50490,#50491,#50492,
#50493,#50494,#50495,#50496,#50497,#50498),.UNSPECIFIED.,.F.,.F.,(4,3,3,
3,3,3,3,4),(89.0794763097301,89.964280273006,90.9638833871505,91.963486501295,
92.9630896154395,93.962692729584,94.9622958437285,95.3626616169097),
 .UNSPECIFIED.);
#11344=B_SPLINE_CURVE_WITH_KNOTS('',3,(#50503,#50504,#50505,#50506,#50507,
#50508,#50509,#50510,#50511,#50512,#50513,#50514,#50515,#50516,#50517,#50518,
#50519,#50520,#50521,#50522,#50523,#50524),.UNSPECIFIED.,.F.,.F.,(4,3,3,
3,3,3,3,4),(-104.624197634898,-103.958723871029,-102.959120756885,-101.95951764274,
-100.959914528596,-99.9603114144511,-98.9607083003066,-98.3410123277186),
 .UNSPECIFIED.);
#11345=B_SPLINE_CURVE_WITH_KNOTS('',3,(#50525,#50526,#50527,#50528,#50529,
#50530,#50531,#50532,#50533,#50534,#50535,#50536,#50537,#50538,#50539,#50540,
#50541,#50542,#50543,#50544,#50545,#50546),.UNSPECIFIED.,.F.,.F.,(4,3,3,
3,3,3,3,4),(95.3626616169097,95.961898957873,96.9615020720176,97.9611051861621,
98.9607083003066,99.9603114144511,100.959914528596,101.645846924089),
 .UNSPECIFIED.);
#11346=B_SPLINE_CURVE_WITH_KNOTS('',3,(#50551,#50552,#50553,#50554,#50555,
#50556,#50557,#50558,#50559,#50560,#50561,#50562,#50563,#50564,#50565,#50566,
#50567,#50568,#50569,#50570,#50571,#50572),.UNSPECIFIED.,.F.,.F.,(4,3,3,
3,3,3,3,4),(-110.907382942078,-109.956342555896,-108.956739441752,-107.957136327607,
-106.957533213463,-105.957930099318,-104.958326985174,-104.624197634898),
 .UNSPECIFIED.);
#11347=B_SPLINE_CURVE_WITH_KNOTS('',3,(#50573,#50574,#50575,#50576,#50577,
#50578,#50579,#50580,#50581,#50582,#50583,#50584,#50585,#50586,#50587,#50588,
#50589,#50590,#50591,#50592,#50593,#50594),.UNSPECIFIED.,.F.,.F.,(4,3,3,
3,3,3,3,4),(101.645846924089,101.95951764274,102.959120756885,103.958723871029,
104.958326985174,105.957930099318,106.957533213463,107.929032231269),
 .UNSPECIFIED.);
#11348=B_SPLINE_CURVE_WITH_KNOTS('',3,(#50599,#50600,#50601,#50602,#50603,
#50604,#50605,#50606,#50607,#50608,#50609,#50610,#50611,#50612,#50613,#50614,
#50615,#50616,#50617,#50618,#50619,#50620,#50621,#50622,#50623),
 .UNSPECIFIED.,.F.,.F.,(4,3,3,3,3,3,3,3,4),(-117.190568249257,-116.953564354908,
-115.953961240763,-114.954358126619,-113.954755012474,-112.95515189833,
-111.955548784185,-110.955945670041,-110.907382942078),.UNSPECIFIED.);
#11349=B_SPLINE_CURVE_WITH_KNOTS('',3,(#50624,#50625,#50626,#50627,#50628,
#50629,#50630,#50631,#50632,#50633,#50634,#50635,#50636,#50637,#50638,#50639,
#50640,#50641,#50642,#50643,#50644,#50645,#50646,#50647,#50648),
 .UNSPECIFIED.,.F.,.F.,(4,3,3,3,3,3,3,3,4),(107.929032231269,107.957136327607,
108.956739441752,109.956342555896,110.955945670041,111.955548784185,112.95515189833,
113.954755012474,114.212217538448),.UNSPECIFIED.);
#11350=B_SPLINE_CURVE_WITH_KNOTS('',3,(#50653,#50654,#50655,#50656,#50657,
#50658,#50659,#50660,#50661,#50662,#50663,#50664,#50665,#50666,#50667,#50668,
#50669,#50670,#50671,#50672,#50673,#50674),.UNSPECIFIED.,.F.,.F.,(4,3,3,
3,3,3,3,4),(-123.473753556437,-122.951183039775,-121.95157992563,-120.951976811486,
-119.952373697341,-118.952770583197,-117.953167469052,-117.190568249257),
 .UNSPECIFIED.);
#11351=B_SPLINE_CURVE_WITH_KNOTS('',3,(#50675,#50676,#50677,#50678,#50679,
#50680,#50681,#50682,#50683,#50684,#50685,#50686,#50687,#50688,#50689,#50690,
#50691,#50692,#50693,#50694,#50695,#50696),.UNSPECIFIED.,.F.,.F.,(4,3,3,
3,3,3,3,4),(114.212217538448,114.954358126619,115.953961240763,116.953564354908,
117.953167469052,118.952770583197,119.952373697341,120.495402845628),
 .UNSPECIFIED.);
#11352=B_SPLINE_CURVE_WITH_KNOTS('',3,(#50702,#50703,#50704,#50705),
 .UNSPECIFIED.,.F.,.F.,(4,4),(135.088484104361,135.498200854482),
 .UNSPECIFIED.);
#11353=B_SPLINE_CURVE_WITH_KNOTS('',3,(#50711,#50712,#50713,#50714,#50715,
#50716,#50717,#50718,#50719,#50720),.UNSPECIFIED.,.F.,.F.,(4,1,1,1,1,1,
1,4),(128.805298797182,129.567898016976,130.567501131121,131.567104245265,
132.56670735941,133.566310473554,134.565913587699,135.088484104361),
 .UNSPECIFIED.);
#11354=B_SPLINE_CURVE_WITH_KNOTS('',3,(#50723,#50724,#50725,#50726,#50727,
#50728,#50729,#50730,#50731,#50732),.UNSPECIFIED.,.F.,.F.,(4,1,1,1,1,1,
1,4),(128.805298797182,129.261872763039,130.261475877184,131.261078991328,
132.260682105473,133.260285219617,133.760086776689,134.259888333762),
 .UNSPECIFIED.);
#11355=B_SPLINE_CURVE_WITH_KNOTS('',3,(#50737,#50738,#50739,#50740,#50741,
#50742,#50743,#50744,#50745,#50746,#50747),.UNSPECIFIED.,.F.,.F.,(4,1,1,
1,1,1,1,1,4),(122.522113490002,122.570676217965,123.570279332109,124.569882446254,
125.569485560398,126.569088674543,127.568691788687,128.568294902832,128.805298797182),
 .UNSPECIFIED.);
#11356=B_SPLINE_CURVE_WITH_KNOTS('',3,(#50748,#50749,#50750,#50751,#50752,
#50753,#50754,#50755,#50756,#50757),.UNSPECIFIED.,.F.,.F.,(4,1,1,1,1,1,
1,4),(122.522113490002,123.264254078172,124.263857192317,125.263460306461,
126.263063420606,127.26266653475,128.262269648895,128.805298797182),
 .UNSPECIFIED.);
#11357=B_SPLINE_CURVE_WITH_KNOTS('',3,(#50762,#50763,#50764,#50765,#50766,
#50767,#50768,#50769,#50770,#50771),.UNSPECIFIED.,.F.,.F.,(4,1,1,1,1,1,
1,4),(116.238928182822,116.573057533098,117.572660647242,118.572263761387,
119.571866875531,120.571469989676,121.57107310382,122.522113490002),
 .UNSPECIFIED.);
#11358=B_SPLINE_CURVE_WITH_KNOTS('',3,(#50772,#50773,#50774,#50775,#50776,
#50777,#50778,#50779,#50780,#50781,#50782),.UNSPECIFIED.,.F.,.F.,(4,1,1,
1,1,1,1,1,4),(116.238928182822,116.26703227916,117.266635393305,118.26623850745,
119.265841621594,120.265444735739,121.265047849883,122.264650964028,122.522113490002),
 .UNSPECIFIED.);
#11359=B_SPLINE_CURVE_WITH_KNOTS('',3,(#50787,#50788,#50789,#50790,#50791,
#50792,#50793,#50794,#50795,#50796),.UNSPECIFIED.,.F.,.F.,(4,1,1,1,1,1,
1,4),(109.955742875643,110.575438848231,111.575041962375,112.57464507652,
113.574248190664,114.573851304809,115.573454418953,116.238928182822),
 .UNSPECIFIED.);
#11360=B_SPLINE_CURVE_WITH_KNOTS('',3,(#50797,#50798,#50799,#50800,#50801,
#50802,#50803,#50804,#50805,#50806),.UNSPECIFIED.,.F.,.F.,(4,1,1,1,1,1,
1,4),(109.955742875643,110.269413594293,111.269016708438,112.268619822582,
113.268222936727,114.267826050871,115.267429165016,116.238928182822),
 .UNSPECIFIED.);
#11361=B_SPLINE_CURVE_WITH_KNOTS('',3,(#50811,#50812,#50813,#50814,#50815,
#50816,#50817,#50818,#50819,#50820),.UNSPECIFIED.,.F.,.F.,(4,1,1,1,1,1,
1,4),(103.672557568463,104.577820163364,105.577423277508,106.577026391653,
107.576629505797,108.576232619942,109.575835734086,109.955742875643),
 .UNSPECIFIED.);
#11362=B_SPLINE_CURVE_WITH_KNOTS('',3,(#50821,#50822,#50823,#50824,#50825,
#50826,#50827,#50828,#50829,#50830),.UNSPECIFIED.,.F.,.F.,(4,1,1,1,1,1,
1,4),(103.672557568463,104.271794909426,105.271398023571,106.271001137715,
107.27060425186,108.270207366004,109.269810480149,109.955742875643),
 .UNSPECIFIED.);
#11363=B_SPLINE_CURVE_WITH_KNOTS('',3,(#50835,#50836,#50837,#50838,#50839,
#50840,#50841,#50842,#50843,#50844,#50845),.UNSPECIFIED.,.F.,.F.,(4,1,1,
1,1,1,1,1,4),(97.3893722612836,97.5805983643521,98.5802014784966,99.5798045926411,
100.579407706786,101.57901082093,102.578613935075,103.578217049219,103.672557568463),
 .UNSPECIFIED.);
#11364=B_SPLINE_CURVE_WITH_KNOTS('',3,(#50846,#50847,#50848,#50849,#50850,
#50851,#50852,#50853,#50854,#50855),.UNSPECIFIED.,.F.,.F.,(4,1,1,1,1,1,
1,4),(97.3893722612836,98.2741762245593,99.2737793387038,100.273382452848,
101.272985566993,102.272588681137,103.272191795282,103.672557568463),
 .UNSPECIFIED.);
#11365=B_SPLINE_CURVE_WITH_KNOTS('',3,(#50860,#50861,#50862,#50863,#50864,
#50865,#50866,#50867,#50868,#50869),.UNSPECIFIED.,.F.,.F.,(4,1,1,1,1,1,
1,4),(91.106186954104,91.582979679485,92.5825827936296,93.5821859077741,
94.5817890219186,95.5813921360631,96.5809952502076,97.3893722612836),
 .UNSPECIFIED.);
#11366=B_SPLINE_CURVE_WITH_KNOTS('',3,(#50870,#50871,#50872,#50873,#50874,
#50875,#50876,#50877,#50878,#50879,#50880),.UNSPECIFIED.,.F.,.F.,(4,1,1,
1,1,1,1,1,4),(91.106186954104,91.2769544255477,92.2765575396922,93.2761606538367,
94.2757637679812,95.2753668821258,96.2749699962703,97.2745731104148,97.3893722612836),
 .UNSPECIFIED.);
#11367=B_SPLINE_CURVE_WITH_KNOTS('',3,(#50885,#50886,#50887,#50888,#50889,
#50890,#50891,#50892,#50893,#50894),.UNSPECIFIED.,.F.,.F.,(4,1,1,1,1,1,
1,4),(84.8230016469244,85.585360994618,86.5849641087625,87.584567222907,
88.5841703370515,89.583773451196,90.5833765653405,91.106186954104),
 .UNSPECIFIED.);
#11368=B_SPLINE_CURVE_WITH_KNOTS('',3,(#50895,#50896,#50897,#50898,#50899,
#50900,#50901,#50902,#50903,#50904),.UNSPECIFIED.,.F.,.F.,(4,1,1,1,1,1,
1,4),(84.8230016469244,85.2793357406806,86.2789388548251,87.2785419689697,
88.2781450831142,89.2777481972587,90.2773513114032,91.106186954104),
 .UNSPECIFIED.);
#11369=B_SPLINE_CURVE_WITH_KNOTS('',3,(#50909,#50910,#50911,#50912,#50913,
#50914,#50915,#50916,#50917,#50918,#50919),.UNSPECIFIED.,.F.,.F.,(4,1,1,
1,1,1,1,1,4),(78.5398163397448,78.5881391956064,79.5877423097509,80.5873454238954,
81.5869485380399,82.5865516521845,83.586154766329,84.5857578804735,84.8230016469244),
 .UNSPECIFIED.);
#11370=B_SPLINE_CURVE_WITH_KNOTS('',3,(#50920,#50921,#50922,#50923,#50924,
#50925,#50926,#50927,#50928,#50929),.UNSPECIFIED.,.F.,.F.,(4,1,1,1,1,1,
1,4),(78.5398163397448,79.2817170558136,80.2813201699581,81.2809232841026,
82.2805263982471,83.2801295123916,84.2797326265361,84.8230016469244),
 .UNSPECIFIED.);
#11371=B_SPLINE_CURVE_WITH_KNOTS('',3,(#50934,#50935,#50936,#50937,#50938,
#50939,#50940,#50941,#50942,#50943),.UNSPECIFIED.,.F.,.F.,(4,1,1,1,1,1,
1,4),(72.2566310325652,72.5905205107393,73.5901236248838,74.5897267390284,
75.5893298531729,76.5889329673174,77.5885360814619,78.5398163397448),
 .UNSPECIFIED.);
#11372=B_SPLINE_CURVE_WITH_KNOTS('',3,(#50944,#50945,#50946,#50947,#50948,
#50949,#50950,#50951,#50952,#50953,#50954),.UNSPECIFIED.,.F.,.F.,(4,1,1,
1,1,1,1,1,4),(72.2566310325652,72.284495256802,73.2840983709465,74.283701485091,
75.2833045992355,76.28290771338,77.2825108275245,78.2821139416691,78.5398163397448),
 .UNSPECIFIED.);
#11373=B_SPLINE_CURVE_WITH_KNOTS('',3,(#50959,#50960,#50961,#50962,#50963,
#50964,#50965,#50966,#50967,#50968),.UNSPECIFIED.,.F.,.F.,(4,1,1,1,1,1,
1,4),(65.9734457253856,66.5929018258723,67.5925049400168,68.5921080541613,
69.5917111683058,70.5913142824503,71.5909173965948,72.2566310325652),
 .UNSPECIFIED.);
#11374=B_SPLINE_CURVE_WITH_KNOTS('',3,(#50969,#50970,#50971,#50972,#50973,
#50974,#50975,#50976,#50977,#50978),.UNSPECIFIED.,.F.,.F.,(4,1,1,1,1,1,
1,4),(65.9734457253856,66.2868765719349,67.2864796860794,68.286082800224,
69.2856859143685,70.285289028513,71.2848921426575,72.2566310325652),
 .UNSPECIFIED.);
#11375=B_SPLINE_CURVE_WITH_KNOTS('',3,(#50983,#50984,#50985,#50986,#50987,
#50988,#50989,#50990,#50991,#50992),.UNSPECIFIED.,.F.,.F.,(4,1,1,1,1,1,
1,4),(59.690260418206,60.5952831410052,61.5948862551497,62.5944893692942,
63.5940924834387,64.5936955975832,65.5932987117278,65.9734457253856),
 .UNSPECIFIED.);
#11376=B_SPLINE_CURVE_WITH_KNOTS('',3,(#50993,#50994,#50995,#50996,#50997,
#50998,#50999,#51000,#51001,#51002),.UNSPECIFIED.,.F.,.F.,(4,1,1,1,1,1,
1,4),(59.690260418206,60.2892578870679,61.2888610012124,62.2884641153569,
63.2880672295014,64.2876703436459,65.2872734577904,65.9734457253856),
 .UNSPECIFIED.);
#11377=B_SPLINE_CURVE_WITH_KNOTS('',3,(#51007,#51008,#51009,#51010,#51011,
#51012,#51013,#51014,#51015,#51016,#51017),.UNSPECIFIED.,.F.,.F.,(4,1,1,
1,1,1,1,1,4),(53.4070751110264,53.5980613419936,54.5976644561381,55.5972675702826,
56.5968706844272,57.5964737985717,58.5960769127162,59.5956800268607,59.690260418206),
 .UNSPECIFIED.);
#11378=B_SPLINE_CURVE_WITH_KNOTS('',3,(#51018,#51019,#51020,#51021,#51022,
#51023,#51024,#51025,#51026,#51027),.UNSPECIFIED.,.F.,.F.,(4,1,1,1,1,1,
1,4),(53.4070751110264,54.2916392022008,55.2912423163453,56.2908454304898,
57.2904485446343,58.2900516587789,59.2896547729234,59.690260418206),
 .UNSPECIFIED.);
#11379=B_SPLINE_CURVE_WITH_KNOTS('',3,(#51032,#51033,#51034,#51035,#51036,
#51037,#51038,#51039,#51040,#51041),.UNSPECIFIED.,.F.,.F.,(4,1,1,1,1,1,
1,4),(47.1238898038469,47.6004426571266,48.6000457712711,49.5996488854156,
50.5992519995601,51.5988551137046,52.5984582278491,53.4070751110264),
 .UNSPECIFIED.);
#11380=B_SPLINE_CURVE_WITH_KNOTS('',3,(#51042,#51043,#51044,#51045,#51046,
#51047,#51048,#51049,#51050,#51051,#51052),.UNSPECIFIED.,.F.,.F.,(4,1,1,
1,1,1,1,1,4),(47.1238898038468,47.2944174031892,48.2940205173337,49.2936236314783,
50.2932267456228,51.2928298597673,52.2924329739118,53.2920360880563,53.4070751110264),
 .UNSPECIFIED.);
#11381=B_SPLINE_CURVE_WITH_KNOTS('',3,(#51057,#51058,#51059,#51060,#51061,
#51062,#51063,#51064,#51065,#51066),.UNSPECIFIED.,.F.,.F.,(4,1,1,1,1,1,
1,4),(40.8407044966673,41.6028239722595,42.602427086404,43.6020302005485,
44.601633314693,45.6012364288375,46.600839542982,47.1238898038469),
 .UNSPECIFIED.);
#11382=B_SPLINE_CURVE_WITH_KNOTS('',3,(#51067,#51068,#51069,#51070,#51071,
#51072,#51073,#51074,#51075,#51076),.UNSPECIFIED.,.F.,.F.,(4,1,1,1,1,1,
1,4),(40.8407044966672,41.2967987183222,42.2964018324667,43.2960049466112,
44.2956080607557,45.2952111749002,46.2948142890447,47.1238898038468),
 .UNSPECIFIED.);
#11383=B_SPLINE_CURVE_WITH_KNOTS('',3,(#51081,#51082,#51083,#51084,#51085,
#51086,#51087,#51088,#51089,#51090,#51091),.UNSPECIFIED.,.F.,.F.,(4,1,1,
1,1,1,1,1,4),(34.5575191894877,34.6056021732479,35.6052052873924,36.6048084015369,
37.6044115156814,38.604014629826,39.6036177439705,40.603220858115,40.8407044966673),
 .UNSPECIFIED.);
#11384=B_SPLINE_CURVE_WITH_KNOTS('',3,(#51092,#51093,#51094,#51095,#51096,
#51097,#51098,#51099,#51100,#51101),.UNSPECIFIED.,.F.,.F.,(4,1,1,1,1,1,
1,4),(34.5575191894876,35.2991800334551,36.2987831475996,37.2983862617441,
38.2979893758886,39.2975924900331,40.2971956041777,40.8407044966672),
 .UNSPECIFIED.);
#11385=B_SPLINE_CURVE_WITH_KNOTS('',3,(#51106,#51107,#51108,#51109,#51110,
#51111,#51112,#51113,#51114,#51115),.UNSPECIFIED.,.F.,.F.,(4,1,1,1,1,1,
1,4),(28.2743338823081,28.6079834883808,29.6075866025254,30.6071897166699,
31.6067928308144,32.6063959449589,33.6059990591034,34.5575191894877),
 .UNSPECIFIED.);
#11386=B_SPLINE_CURVE_WITH_KNOTS('',3,(#51116,#51117,#51118,#51119,#51120,
#51121,#51122,#51123,#51124,#51125,#51126),.UNSPECIFIED.,.F.,.F.,(4,1,1,
1,1,1,1,1,4),(28.274333882308,28.3019582344435,29.301561348588,30.3011644627325,
31.3007675768771,32.3003706910216,33.2999738051661,34.2995769193106,34.5575191894876),
 .UNSPECIFIED.);
#11387=B_SPLINE_CURVE_WITH_KNOTS('',3,(#51131,#51132,#51133,#51134,#51135,
#51136,#51137,#51138,#51139,#51140),.UNSPECIFIED.,.F.,.F.,(4,1,1,1,1,1,
1,4),(21.9911485751285,22.6103648035138,23.6099679176583,24.6095710318028,
25.6091741459473,26.6087772600918,27.6083803742363,28.2743338823081),
 .UNSPECIFIED.);
#11388=B_SPLINE_CURVE_WITH_KNOTS('',3,(#51141,#51142,#51143,#51144,#51145,
#51146,#51147,#51148,#51149,#51150),.UNSPECIFIED.,.F.,.F.,(4,1,1,1,1,1,
1,4),(21.9911485751285,22.3043395495765,23.303942663721,24.3035457778655,
25.30314889201,26.3027520061545,27.302355120299,28.274333882308),
 .UNSPECIFIED.);
#11389=B_SPLINE_CURVE_WITH_KNOTS('',3,(#51155,#51156,#51157,#51158,#51159,
#51160,#51161,#51162,#51163,#51164),.UNSPECIFIED.,.F.,.F.,(4,1,1,1,1,1,
1,4),(15.7079632679489,16.6127461186467,17.6123492327912,18.6119523469357,
19.6115554610803,20.6111585752248,21.6107616893693,21.9911485751285),
 .UNSPECIFIED.);
#11390=B_SPLINE_CURVE_WITH_KNOTS('',3,(#51165,#51166,#51167,#51168,#51169,
#51170,#51171,#51172,#51173,#51174),.UNSPECIFIED.,.F.,.F.,(4,1,1,1,1,1,
1,4),(15.7079632679489,16.3067208647094,17.3063239788539,18.3059270929984,
19.3055302071429,20.3051333212874,21.3047364354319,21.9911485751285),
 .UNSPECIFIED.);
#11391=B_SPLINE_CURVE_WITH_KNOTS('',3,(#51700,#51701,#51702,#51703,#51704,
#51705,#51706,#51707,#51708,#51709,#51710,#51711,#51712,#51713,#51714,#51715,
#51716,#51717,#51718,#51719,#51720,#51721,#51722,#51723,#51724,#51725,#51726,
#51727,#51728,#51729,#51730,#51731,#51732,#51733,#51734,#51735,#51736,#51737,
#51738,#51739,#51740,#51741,#51742,#51743,#51744,#51745,#51746,#51747,#51748,
#51749,#51750,#51751,#51752,#51753,#51754,#51755,#51756,#51757,#51758,#51759,
#51760,#51761,#51762,#51763,#51764,#51765,#51766,#51767,#51768,#51769,#51770,
#51771,#51772,#51773,#51774,#51775,#51776,#51777,#51778,#51779,#51780,#51781,
#51782,#51783,#51784,#51785,#51786,#51787,#51788,#51789,#51790,#51791,#51792,
#51793,#51794,#51795,#51796,#51797,#51798,#51799,#51800,#51801,#51802),
 .UNSPECIFIED.,.F.,.F.,(4,3,3,3,3,3,3,3,3,3,3,3,3,3,3,3,3,3,3,3,3,3,3,3,
3,3,3,3,3,3,3,3,3,3,4),(-0.933975894023114,-0.900886022956469,-0.857613677956334,
-0.830917467558831,-0.811990732117496,-0.805266958984206,-0.762537705919167,
-0.721029781628806,-0.68471034787474,-0.677426067872528,-0.635390348422708,
-0.593572252555102,-0.552797767315397,-0.522216903385619,-0.510030154625355,
-0.502729037187648,-0.496839898567668,-0.456766765593561,-0.430474311596282,
-0.389892426332242,-0.34937929636466,-0.329910151917754,-0.324685557329147,
-0.285203392664255,-0.245885205074442,-0.210138932487817,-0.18387156592684,
-0.169358115925774,-0.161848011397128,-0.156162121436153,-0.117121591077115,
-0.0788937454479904,-0.0394468727239952,-0.00242854395559244,0.),
 .UNSPECIFIED.);
#11392=B_SPLINE_CURVE_WITH_KNOTS('',3,(#51803,#51804,#51805,#51806,#51807,
#51808,#51809,#51810,#51811,#51812,#51813,#51814,#51815),.UNSPECIFIED.,
 .F.,.F.,(4,3,3,3,4),(120.495402845628,120.951976811486,121.95157992563,
122.951183039775,123.883470306557),.UNSPECIFIED.);
#11393=B_SPLINE_CURVE_WITH_KNOTS('',3,(#51817,#51818,#51819,#51820,#51821,
#51822,#51823,#51824,#51825,#51826,#51827,#51828,#51829,#51830,#51831,#51832,
#51833,#51834,#51835,#51836,#51837,#51838,#51839,#51840,#51841,#51842,#51843,
#51844,#51845,#51846,#51847,#51848,#51849,#51850,#51851,#51852,#51853,#51854,
#51855,#51856,#51857,#51858,#51859,#51860,#51861,#51862,#51863,#51864,#51865,
#51866,#51867,#51868,#51869,#51870,#51871,#51872,#51873,#51874,#51875,#51876,
#51877,#51878,#51879,#51880,#51881,#51882,#51883,#51884,#51885,#51886,#51887,
#51888,#51889,#51890,#51891,#51892,#51893,#51894,#51895,#51896,#51897,#51898,
#51899,#51900,#51901,#51902,#51903,#51904,#51905,#51906,#51907,#51908,#51909,
#51910,#51911,#51912,#51913,#51914,#51915,#51916,#51917,#51918,#51919),
 .UNSPECIFIED.,.F.,.F.,(4,3,3,3,3,3,3,3,3,3,3,3,3,3,3,3,3,3,3,3,3,3,3,3,
3,3,3,3,3,3,3,3,3,3,4),(-0.937740963081769,-0.909984679133564,-0.872833882725954,
-0.847996397065448,-0.833928218367593,-0.824785785263065,-0.78663373762343,
-0.747733784440234,-0.730715054922586,-0.721961762671648,-0.713934774220468,
-0.674204019543976,-0.633909683375831,-0.593656192357265,-0.564100672307414,
-0.551648204867746,-0.54396197545851,-0.502501117350991,-0.475434112157862,
-0.435310758308129,-0.394542023824858,-0.374961735244211,-0.367483120962523,
-0.326359080771091,-0.284254421333978,-0.242709754795601,-0.212371035446151,
-0.198407867967393,-0.190923667635028,-0.185034664212022,-0.142232442426345,
-0.0988549974710058,-0.0555174255396185,-0.0127493435743661,0.),
 .UNSPECIFIED.);
#11394=B_SPLINE_CURVE_WITH_KNOTS('',3,(#51920,#51921,#51922,#51923,#51924,
#51925,#51926,#51927,#51928),.UNSPECIFIED.,.F.,.F.,(4,1,1,1,1,1,4),(10.3764180272042,
11.3087052939868,12.3083084081313,13.3079115222759,14.3075146364204,15.3071177505649,
15.7079632679489),.UNSPECIFIED.);
#11395=B_SPLINE_CURVE_WITH_KNOTS('',3,(#51934,#51935,#51936,#51937,#51938,
#51939,#51940,#51941,#51942,#51943,#51944,#51945,#51946,#51947,#51948,#51949,
#51950,#51951,#51952,#51953,#51954,#51955,#51956,#51957,#51958,#51959,#51960,
#51961,#51962,#51963,#51964,#51965,#51966,#51967,#51968,#51969,#51970,#51971,
#51972,#51973,#51974,#51975,#51976,#51977,#51978,#51979,#51980,#51981,#51982,
#51983,#51984,#51985,#51986,#51987,#51988,#51989,#51990,#51991,#51992,#51993,
#51994,#51995,#51996,#51997,#51998,#51999,#52000,#52001,#52002,#52003,#52004,
#52005,#52006,#52007,#52008,#52009,#52010,#52011,#52012,#52013,#52014,#52015,
#52016,#52017,#52018,#52019,#52020,#52021,#52022,#52023,#52024,#52025,#52026,
#52027,#52028,#52029,#52030,#52031,#52032,#52033,#52034,#52035,#52036),
 .UNSPECIFIED.,.F.,.F.,(4,3,3,3,3,3,3,3,3,3,3,3,3,3,3,3,3,3,3,3,3,3,3,3,
3,3,3,3,3,3,3,3,3,3,4),(-0.933975894023115,-0.90088602295648,-0.857613686561679,
-0.830917475626341,-0.811990735770248,-0.805266957540168,-0.762537700650808,
-0.72102977701899,-0.684710343841149,-0.67742606502949,-0.635390295376529,
-0.593572109506116,-0.552797660028653,-0.522216822920556,-0.510030127654026,
-0.502728981266388,-0.496839893719554,-0.456766643291822,-0.430474311596264,
-0.389892498153584,-0.349379548247307,-0.329910675083222,-0.324686090829592,
-0.285204009769594,-0.24588601906745,-0.210138932487834,-0.183871565926854,
-0.169358141411446,-0.161848180179082,-0.156162148451424,-0.117121611338568,
-0.0788936961114827,-0.0394468480557413,-0.00242847333026767,0.),
 .UNSPECIFIED.);
#11396=B_SPLINE_CURVE_WITH_KNOTS('',3,(#52039,#52040,#52041,#52042,#52043,
#52044,#52045,#52046,#52047),.UNSPECIFIED.,.F.,.F.,(4,1,1,1,1,1,4),(11.6147305479242,
12.1145321049964,12.6143336620687,13.6139367762132,14.6135398903577,15.6131430045022,
15.7079632679489),.UNSPECIFIED.);
#11397=B_SPLINE_CURVE_WITH_KNOTS('',3,(#52573,#52574,#52575,#52576,#52577,
#52578,#52579,#52580,#52581,#52582,#52583,#52584,#52585,#52586,#52587,#52588,
#52589,#52590,#52591,#52592,#52593,#52594,#52595,#52596,#52597,#52598,#52599,
#52600,#52601,#52602,#52603,#52604,#52605,#52606,#52607,#52608,#52609,#52610,
#52611,#52612,#52613,#52614,#52615,#52616,#52617,#52618,#52619,#52620,#52621,
#52622,#52623,#52624,#52625,#52626,#52627,#52628,#52629,#52630,#52631,#52632,
#52633,#52634,#52635,#52636,#52637,#52638,#52639,#52640,#52641,#52642,#52643,
#52644,#52645,#52646,#52647,#52648,#52649,#52650,#52651,#52652,#52653,#52654,
#52655,#52656,#52657,#52658,#52659,#52660,#52661,#52662,#52663,#52664,#52665,
#52666,#52667,#52668,#52669,#52670,#52671,#52672,#52673,#52674,#52675),
 .UNSPECIFIED.,.F.,.F.,(4,3,3,3,3,3,3,3,3,3,3,3,3,3,3,3,3,3,3,3,3,3,3,3,
3,3,3,3,3,3,3,3,3,3,4),(-0.93774096308164,-0.909984679133421,-0.872833901724178,
-0.847996414876281,-0.833928216062254,-0.824785782258315,-0.786633754260955,
-0.747733798998064,-0.730715068570549,-0.721961765812645,-0.713934771789967,
-0.674204030030189,-0.633909683853084,-0.593656117964,-0.564100616512456,
-0.551648127597297,-0.543961983767159,-0.502501076596855,-0.475434112157824,
-0.43531058957835,-0.394541812627602,-0.374961344140611,-0.367483133322358,
-0.326358922649391,-0.284254298812646,-0.24270975479558,-0.212371035446133,
-0.198407868112275,-0.190923678285126,-0.185034666341196,-0.142232895600103,
-0.0988556198980695,-0.0555180472647553,-0.0127497906429885,0.),
 .UNSPECIFIED.);
#11398=B_SPLINE_CURVE_WITH_KNOTS('',3,(#52676,#52677,#52678,#52679,#52680,
#52681,#52682,#52683,#52684,#52685,#52686,#52687,#52688),.UNSPECIFIED.,
 .F.,.F.,(4,3,3,3,4),(-125.949992382208,-125.450190825136,-124.950389268064,
-123.950786153919,-123.473753556437),.UNSPECIFIED.);
#13458=VERTEX_POINT('',#49729);
#13459=VERTEX_POINT('',#49730);
#13460=VERTEX_POINT('',#49732);
#13461=VERTEX_POINT('',#49743);
#13462=VERTEX_POINT('',#49756);
#13463=VERTEX_POINT('',#49757);
#13464=VERTEX_POINT('',#49804);
#13465=VERTEX_POINT('',#49805);
#13466=VERTEX_POINT('',#49852);
#13467=VERTEX_POINT('',#49853);
#13468=VERTEX_POINT('',#49900);
#13469=VERTEX_POINT('',#49901);
#13470=VERTEX_POINT('',#49954);
#13471=VERTEX_POINT('',#49955);
#13472=VERTEX_POINT('',#50002);
#13473=VERTEX_POINT('',#50003);
#13474=VERTEX_POINT('',#50050);
#13475=VERTEX_POINT('',#50051);
#13476=VERTEX_POINT('',#50104);
#13477=VERTEX_POINT('',#50105);
#13478=VERTEX_POINT('',#50152);
#13479=VERTEX_POINT('',#50153);
#13480=VERTEX_POINT('',#50200);
#13481=VERTEX_POINT('',#50201);
#13482=VERTEX_POINT('',#50248);
#13483=VERTEX_POINT('',#50249);
#13484=VERTEX_POINT('',#50302);
#13485=VERTEX_POINT('',#50303);
#13486=VERTEX_POINT('',#50350);
#13487=VERTEX_POINT('',#50351);
#13488=VERTEX_POINT('',#50398);
#13489=VERTEX_POINT('',#50399);
#13490=VERTEX_POINT('',#50452);
#13491=VERTEX_POINT('',#50453);
#13492=VERTEX_POINT('',#50500);
#13493=VERTEX_POINT('',#50501);
#13494=VERTEX_POINT('',#50548);
#13495=VERTEX_POINT('',#50549);
#13496=VERTEX_POINT('',#50596);
#13497=VERTEX_POINT('',#50597);
#13498=VERTEX_POINT('',#50650);
#13499=VERTEX_POINT('',#50651);
#13500=VERTEX_POINT('',#50698);
#13501=VERTEX_POINT('',#50699);
#13502=VERTEX_POINT('',#50701);
#13503=VERTEX_POINT('',#50708);
#13504=VERTEX_POINT('',#50709);
#13505=VERTEX_POINT('',#50721);
#13506=VERTEX_POINT('',#50734);
#13507=VERTEX_POINT('',#50735);
#13508=VERTEX_POINT('',#50759);
#13509=VERTEX_POINT('',#50760);
#13510=VERTEX_POINT('',#50784);
#13511=VERTEX_POINT('',#50785);
#13512=VERTEX_POINT('',#50808);
#13513=VERTEX_POINT('',#50809);
#13514=VERTEX_POINT('',#50832);
#13515=VERTEX_POINT('',#50833);
#13516=VERTEX_POINT('',#50857);
#13517=VERTEX_POINT('',#50858);
#13518=VERTEX_POINT('',#50882);
#13519=VERTEX_POINT('',#50883);
#13520=VERTEX_POINT('',#50906);
#13521=VERTEX_POINT('',#50907);
#13522=VERTEX_POINT('',#50931);
#13523=VERTEX_POINT('',#50932);
#13524=VERTEX_POINT('',#50956);
#13525=VERTEX_POINT('',#50957);
#13526=VERTEX_POINT('',#50980);
#13527=VERTEX_POINT('',#50981);
#13528=VERTEX_POINT('',#51004);
#13529=VERTEX_POINT('',#51005);
#13530=VERTEX_POINT('',#51029);
#13531=VERTEX_POINT('',#51030);
#13532=VERTEX_POINT('',#51054);
#13533=VERTEX_POINT('',#51055);
#13534=VERTEX_POINT('',#51078);
#13535=VERTEX_POINT('',#51079);
#13536=VERTEX_POINT('',#51103);
#13537=VERTEX_POINT('',#51104);
#13538=VERTEX_POINT('',#51128);
#13539=VERTEX_POINT('',#51129);
#13540=VERTEX_POINT('',#51152);
#13541=VERTEX_POINT('',#51153);
#13542=VERTEX_POINT('',#51699);
#13543=VERTEX_POINT('',#51816);
#13544=VERTEX_POINT('',#51930);
#13545=VERTEX_POINT('',#51933);
#13546=VERTEX_POINT('',#52572);
#13547=VERTEX_POINT('',#52690);
#13548=VERTEX_POINT('',#52691);
#13549=VERTEX_POINT('',#52693);
#13550=VERTEX_POINT('',#52695);
#13551=VERTEX_POINT('',#52699);
#13552=VERTEX_POINT('',#52703);
#13553=VERTEX_POINT('',#52709);
#13554=VERTEX_POINT('',#52710);
#13555=VERTEX_POINT('',#52712);
#13556=VERTEX_POINT('',#52714);
#13557=VERTEX_POINT('',#52718);
#13558=VERTEX_POINT('',#52722);
#13559=VERTEX_POINT('',#52728);
#13560=VERTEX_POINT('',#52729);
#13561=VERTEX_POINT('',#52731);
#13562=VERTEX_POINT('',#52733);
#13563=VERTEX_POINT('',#52737);
#13564=VERTEX_POINT('',#52741);
#13565=VERTEX_POINT('',#52747);
#13566=VERTEX_POINT('',#52748);
#13567=VERTEX_POINT('',#52750);
#13568=VERTEX_POINT('',#52752);
#13569=VERTEX_POINT('',#52756);
#13570=VERTEX_POINT('',#52760);
#13571=VERTEX_POINT('',#52766);
#13572=VERTEX_POINT('',#52767);
#13573=VERTEX_POINT('',#52769);
#13574=VERTEX_POINT('',#52771);
#13575=VERTEX_POINT('',#52775);
#13576=VERTEX_POINT('',#52779);
#13577=VERTEX_POINT('',#52785);
#13578=VERTEX_POINT('',#52786);
#13579=VERTEX_POINT('',#52788);
#13580=VERTEX_POINT('',#52790);
#13581=VERTEX_POINT('',#52794);
#13582=VERTEX_POINT('',#52798);
#13583=VERTEX_POINT('',#52804);
#13584=VERTEX_POINT('',#52805);
#13585=VERTEX_POINT('',#52807);
#13586=VERTEX_POINT('',#52809);
#13587=VERTEX_POINT('',#52813);
#13588=VERTEX_POINT('',#52817);
#13589=VERTEX_POINT('',#52823);
#13590=VERTEX_POINT('',#52824);
#13591=VERTEX_POINT('',#52826);
#13592=VERTEX_POINT('',#52828);
#13593=VERTEX_POINT('',#52832);
#13594=VERTEX_POINT('',#52836);
#13595=VERTEX_POINT('',#52842);
#13596=VERTEX_POINT('',#52843);
#13597=VERTEX_POINT('',#52845);
#13598=VERTEX_POINT('',#52847);
#13599=VERTEX_POINT('',#52851);
#13600=VERTEX_POINT('',#52855);
#13601=VERTEX_POINT('',#52861);
#13602=VERTEX_POINT('',#52862);
#13603=VERTEX_POINT('',#52864);
#13604=VERTEX_POINT('',#52866);
#13605=VERTEX_POINT('',#52870);
#13606=VERTEX_POINT('',#52874);
#13607=VERTEX_POINT('',#52880);
#13608=VERTEX_POINT('',#52881);
#13609=VERTEX_POINT('',#52883);
#13610=VERTEX_POINT('',#52885);
#13611=VERTEX_POINT('',#52889);
#13612=VERTEX_POINT('',#52893);
#13613=VERTEX_POINT('',#52899);
#13614=VERTEX_POINT('',#52900);
#13615=VERTEX_POINT('',#52902);
#13616=VERTEX_POINT('',#52904);
#13617=VERTEX_POINT('',#52908);
#13618=VERTEX_POINT('',#52912);
#13619=VERTEX_POINT('',#52918);
#13620=VERTEX_POINT('',#52919);
#13621=VERTEX_POINT('',#52921);
#13622=VERTEX_POINT('',#52923);
#13623=VERTEX_POINT('',#52927);
#13624=VERTEX_POINT('',#52931);
#13625=VERTEX_POINT('',#52937);
#13626=VERTEX_POINT('',#52938);
#13627=VERTEX_POINT('',#52940);
#13628=VERTEX_POINT('',#52942);
#13629=VERTEX_POINT('',#52946);
#13630=VERTEX_POINT('',#52950);
#13631=VERTEX_POINT('',#52956);
#13632=VERTEX_POINT('',#52957);
#13633=VERTEX_POINT('',#52959);
#13634=VERTEX_POINT('',#52961);
#13635=VERTEX_POINT('',#52965);
#13636=VERTEX_POINT('',#52969);
#13637=VERTEX_POINT('',#52975);
#13638=VERTEX_POINT('',#52976);
#13639=VERTEX_POINT('',#52978);
#13640=VERTEX_POINT('',#52980);
#13641=VERTEX_POINT('',#52984);
#13642=VERTEX_POINT('',#52988);
#13643=VERTEX_POINT('',#52994);
#13644=VERTEX_POINT('',#52995);
#13645=VERTEX_POINT('',#52997);
#13646=VERTEX_POINT('',#52999);
#13647=VERTEX_POINT('',#53003);
#13648=VERTEX_POINT('',#53007);
#13649=VERTEX_POINT('',#53013);
#13650=VERTEX_POINT('',#53014);
#13651=VERTEX_POINT('',#53016);
#13652=VERTEX_POINT('',#53018);
#13653=VERTEX_POINT('',#53022);
#13654=VERTEX_POINT('',#53024);
#13655=VERTEX_POINT('',#53028);
#13656=VERTEX_POINT('',#53032);
#13657=VERTEX_POINT('',#53036);
#13658=VERTEX_POINT('',#53037);
#13659=VERTEX_POINT('',#53039);
#13660=VERTEX_POINT('',#53041);
#13661=VERTEX_POINT('',#53045);
#13662=VERTEX_POINT('',#53049);
#13663=VERTEX_POINT('',#53055);
#13664=VERTEX_POINT('',#53056);
#13665=VERTEX_POINT('',#53058);
#13666=VERTEX_POINT('',#53060);
#13667=VERTEX_POINT('',#53064);
#13668=VERTEX_POINT('',#53068);
#13669=VERTEX_POINT('',#53074);
#13670=VERTEX_POINT('',#53075);
#13671=VERTEX_POINT('',#53077);
#13672=VERTEX_POINT('',#53079);
#13673=VERTEX_POINT('',#53083);
#13674=VERTEX_POINT('',#53087);
#13675=VERTEX_POINT('',#53093);
#13676=VERTEX_POINT('',#53094);
#13677=VERTEX_POINT('',#53096);
#13678=VERTEX_POINT('',#53098);
#13679=VERTEX_POINT('',#53102);
#13680=VERTEX_POINT('',#53106);
#13681=VERTEX_POINT('',#53112);
#13682=VERTEX_POINT('',#53113);
#13683=VERTEX_POINT('',#53115);
#13684=VERTEX_POINT('',#53117);
#13685=VERTEX_POINT('',#53121);
#13686=VERTEX_POINT('',#53125);
#13687=VERTEX_POINT('',#53131);
#13688=VERTEX_POINT('',#53132);
#13689=VERTEX_POINT('',#53134);
#13690=VERTEX_POINT('',#53136);
#13691=VERTEX_POINT('',#53140);
#13692=VERTEX_POINT('',#53144);
#13693=VERTEX_POINT('',#53150);
#13694=VERTEX_POINT('',#53151);
#13695=VERTEX_POINT('',#53153);
#13696=VERTEX_POINT('',#53155);
#13697=VERTEX_POINT('',#53159);
#13698=VERTEX_POINT('',#53163);
#13699=VERTEX_POINT('',#53169);
#13700=VERTEX_POINT('',#53170);
#13701=VERTEX_POINT('',#53172);
#13702=VERTEX_POINT('',#53174);
#13703=VERTEX_POINT('',#53178);
#13704=VERTEX_POINT('',#53182);
#13705=VERTEX_POINT('',#53188);
#13706=VERTEX_POINT('',#53189);
#13707=VERTEX_POINT('',#53191);
#13708=VERTEX_POINT('',#53193);
#13709=VERTEX_POINT('',#53197);
#13710=VERTEX_POINT('',#53201);
#13711=VERTEX_POINT('',#53207);
#13712=VERTEX_POINT('',#53208);
#13713=VERTEX_POINT('',#53210);
#13714=VERTEX_POINT('',#53212);
#13715=VERTEX_POINT('',#53216);
#13716=VERTEX_POINT('',#53220);
#13717=VERTEX_POINT('',#53226);
#13718=VERTEX_POINT('',#53227);
#13719=VERTEX_POINT('',#53229);
#13720=VERTEX_POINT('',#53231);
#13721=VERTEX_POINT('',#53235);
#13722=VERTEX_POINT('',#53239);
#13723=VERTEX_POINT('',#53245);
#13724=VERTEX_POINT('',#53246);
#13725=VERTEX_POINT('',#53248);
#13726=VERTEX_POINT('',#53250);
#13727=VERTEX_POINT('',#53254);
#13728=VERTEX_POINT('',#53258);
#13729=VERTEX_POINT('',#53264);
#13730=VERTEX_POINT('',#53265);
#13731=VERTEX_POINT('',#53267);
#13732=VERTEX_POINT('',#53269);
#13733=VERTEX_POINT('',#53273);
#13734=VERTEX_POINT('',#53277);
#13735=VERTEX_POINT('',#53283);
#13736=VERTEX_POINT('',#53284);
#13737=VERTEX_POINT('',#53286);
#13738=VERTEX_POINT('',#53288);
#13739=VERTEX_POINT('',#53292);
#13740=VERTEX_POINT('',#53296);
#13741=VERTEX_POINT('',#53302);
#13742=VERTEX_POINT('',#53303);
#13743=VERTEX_POINT('',#53305);
#13744=VERTEX_POINT('',#53307);
#13745=VERTEX_POINT('',#53311);
#13746=VERTEX_POINT('',#53315);
#13747=VERTEX_POINT('',#53321);
#13748=VERTEX_POINT('',#53322);
#13749=VERTEX_POINT('',#53324);
#13750=VERTEX_POINT('',#53326);
#13751=VERTEX_POINT('',#53330);
#13752=VERTEX_POINT('',#53334);
#13753=VERTEX_POINT('',#53340);
#13754=VERTEX_POINT('',#53341);
#13755=VERTEX_POINT('',#53343);
#13756=VERTEX_POINT('',#53345);
#13757=VERTEX_POINT('',#53349);
#13758=VERTEX_POINT('',#53353);
#13759=VERTEX_POINT('',#53359);
#13760=VERTEX_POINT('',#53360);
#13761=VERTEX_POINT('',#53362);
#13762=VERTEX_POINT('',#53364);
#13763=VERTEX_POINT('',#53368);
#13764=VERTEX_POINT('',#53372);
#13765=VERTEX_POINT('',#53378);
#13766=VERTEX_POINT('',#53379);
#13767=VERTEX_POINT('',#53381);
#13768=VERTEX_POINT('',#53383);
#13769=VERTEX_POINT('',#53387);
#13770=VERTEX_POINT('',#53389);
#13771=VERTEX_POINT('',#53393);
#13772=VERTEX_POINT('',#53395);
#13773=VERTEX_POINT('',#53399);
#13774=VERTEX_POINT('',#53401);
#13775=VERTEX_POINT('',#53405);
#13776=VERTEX_POINT('',#53407);
#13777=VERTEX_POINT('',#53415);
#13778=VERTEX_POINT('',#53422);
#13779=VERTEX_POINT('',#53425);
#13780=VERTEX_POINT('',#53430);
#17116=EDGE_CURVE('',#13458,#13459,#3691,.T.);
#17117=EDGE_CURVE('',#13458,#13460,#11312,.T.);
#17118=EDGE_CURVE('',#13460,#13461,#10881,.T.);
#17119=EDGE_CURVE('',#13461,#13459,#11313,.T.);
#17120=EDGE_CURVE('',#13462,#13463,#3692,.T.);
#17121=EDGE_CURVE('',#13462,#13458,#11314,.T.);
#17122=EDGE_CURVE('',#13459,#13463,#11315,.T.);
#17123=EDGE_CURVE('',#13464,#13465,#3693,.T.);
#17124=EDGE_CURVE('',#13464,#13462,#11316,.T.);
#17125=EDGE_CURVE('',#13463,#13465,#11317,.T.);
#17126=EDGE_CURVE('',#13466,#13467,#3694,.T.);
#17127=EDGE_CURVE('',#13466,#13464,#11318,.T.);
#17128=EDGE_CURVE('',#13465,#13467,#11319,.T.);
#17129=EDGE_CURVE('',#13468,#13469,#3695,.T.);
#17130=EDGE_CURVE('',#13468,#13466,#11320,.T.);
#17131=EDGE_CURVE('',#13467,#13469,#11321,.T.);
#17132=EDGE_CURVE('',#13470,#13471,#3696,.T.);
#17133=EDGE_CURVE('',#13470,#13468,#11322,.T.);
#17134=EDGE_CURVE('',#13469,#13471,#11323,.T.);
#17135=EDGE_CURVE('',#13472,#13473,#3697,.T.);
#17136=EDGE_CURVE('',#13472,#13470,#11324,.T.);
#17137=EDGE_CURVE('',#13471,#13473,#11325,.T.);
#17138=EDGE_CURVE('',#13474,#13475,#3698,.T.);
#17139=EDGE_CURVE('',#13474,#13472,#11326,.T.);
#17140=EDGE_CURVE('',#13473,#13475,#11327,.T.);
#17141=EDGE_CURVE('',#13476,#13477,#3699,.T.);
#17142=EDGE_CURVE('',#13476,#13474,#11328,.T.);
#17143=EDGE_CURVE('',#13475,#13477,#11329,.T.);
#17144=EDGE_CURVE('',#13478,#13479,#3700,.T.);
#17145=EDGE_CURVE('',#13478,#13476,#11330,.T.);
#17146=EDGE_CURVE('',#13477,#13479,#11331,.T.);
#17147=EDGE_CURVE('',#13480,#13481,#3701,.T.);
#17148=EDGE_CURVE('',#13480,#13478,#11332,.T.);
#17149=EDGE_CURVE('',#13479,#13481,#11333,.T.);
#17150=EDGE_CURVE('',#13482,#13483,#3702,.T.);
#17151=EDGE_CURVE('',#13482,#13480,#11334,.T.);
#17152=EDGE_CURVE('',#13481,#13483,#11335,.T.);
#17153=EDGE_CURVE('',#13484,#13485,#3703,.T.);
#17154=EDGE_CURVE('',#13484,#13482,#11336,.T.);
#17155=EDGE_CURVE('',#13483,#13485,#11337,.T.);
#17156=EDGE_CURVE('',#13486,#13487,#3704,.T.);
#17157=EDGE_CURVE('',#13486,#13484,#11338,.T.);
#17158=EDGE_CURVE('',#13485,#13487,#11339,.T.);
#17159=EDGE_CURVE('',#13488,#13489,#3705,.T.);
#17160=EDGE_CURVE('',#13488,#13486,#11340,.T.);
#17161=EDGE_CURVE('',#13487,#13489,#11341,.T.);
#17162=EDGE_CURVE('',#13490,#13491,#3706,.T.);
#17163=EDGE_CURVE('',#13490,#13488,#11342,.T.);
#17164=EDGE_CURVE('',#13489,#13491,#11343,.T.);
#17165=EDGE_CURVE('',#13492,#13493,#3707,.T.);
#17166=EDGE_CURVE('',#13492,#13490,#11344,.T.);
#17167=EDGE_CURVE('',#13491,#13493,#11345,.T.);
#17168=EDGE_CURVE('',#13494,#13495,#3708,.T.);
#17169=EDGE_CURVE('',#13494,#13492,#11346,.T.);
#17170=EDGE_CURVE('',#13493,#13495,#11347,.T.);
#17171=EDGE_CURVE('',#13496,#13497,#3709,.T.);
#17172=EDGE_CURVE('',#13496,#13494,#11348,.T.);
#17173=EDGE_CURVE('',#13495,#13497,#11349,.T.);
#17174=EDGE_CURVE('',#13498,#13499,#3710,.T.);
#17175=EDGE_CURVE('',#13498,#13496,#11350,.T.);
#17176=EDGE_CURVE('',#13497,#13499,#11351,.T.);
#17177=EDGE_CURVE('',#13500,#13501,#3711,.T.);
#17178=EDGE_CURVE('',#13500,#13502,#11352,.T.);
#17179=EDGE_CURVE('',#13501,#13502,#10882,.T.);
#17180=EDGE_CURVE('',#13503,#13504,#3712,.T.);
#17181=EDGE_CURVE('',#13503,#13500,#11353,.T.);
#17182=EDGE_CURVE('',#13505,#13501,#10883,.T.);
#17183=EDGE_CURVE('',#13504,#13505,#11354,.T.);
#17184=EDGE_CURVE('',#13506,#13507,#3713,.T.);
#17185=EDGE_CURVE('',#13506,#13503,#11355,.T.);
#17186=EDGE_CURVE('',#13507,#13504,#11356,.T.);
#17187=EDGE_CURVE('',#13508,#13509,#3714,.T.);
#17188=EDGE_CURVE('',#13508,#13506,#11357,.T.);
#17189=EDGE_CURVE('',#13509,#13507,#11358,.T.);
#17190=EDGE_CURVE('',#13510,#13511,#3715,.T.);
#17191=EDGE_CURVE('',#13510,#13508,#11359,.T.);
#17192=EDGE_CURVE('',#13511,#13509,#11360,.T.);
#17193=EDGE_CURVE('',#13512,#13513,#3716,.T.);
#17194=EDGE_CURVE('',#13512,#13510,#11361,.T.);
#17195=EDGE_CURVE('',#13513,#13511,#11362,.T.);
#17196=EDGE_CURVE('',#13514,#13515,#3717,.T.);
#17197=EDGE_CURVE('',#13514,#13512,#11363,.T.);
#17198=EDGE_CURVE('',#13515,#13513,#11364,.T.);
#17199=EDGE_CURVE('',#13516,#13517,#3718,.T.);
#17200=EDGE_CURVE('',#13516,#13514,#11365,.T.);
#17201=EDGE_CURVE('',#13517,#13515,#11366,.T.);
#17202=EDGE_CURVE('',#13518,#13519,#3719,.T.);
#17203=EDGE_CURVE('',#13518,#13516,#11367,.T.);
#17204=EDGE_CURVE('',#13519,#13517,#11368,.T.);
#17205=EDGE_CURVE('',#13520,#13521,#3720,.T.);
#17206=EDGE_CURVE('',#13520,#13518,#11369,.T.);
#17207=EDGE_CURVE('',#13521,#13519,#11370,.T.);
#17208=EDGE_CURVE('',#13522,#13523,#3721,.T.);
#17209=EDGE_CURVE('',#13522,#13520,#11371,.T.);
#17210=EDGE_CURVE('',#13523,#13521,#11372,.T.);
#17211=EDGE_CURVE('',#13524,#13525,#3722,.T.);
#17212=EDGE_CURVE('',#13524,#13522,#11373,.T.);
#17213=EDGE_CURVE('',#13525,#13523,#11374,.T.);
#17214=EDGE_CURVE('',#13526,#13527,#3723,.T.);
#17215=EDGE_CURVE('',#13526,#13524,#11375,.T.);
#17216=EDGE_CURVE('',#13527,#13525,#11376,.T.);
#17217=EDGE_CURVE('',#13528,#13529,#3724,.T.);
#17218=EDGE_CURVE('',#13528,#13526,#11377,.T.);
#17219=EDGE_CURVE('',#13529,#13527,#11378,.T.);
#17220=EDGE_CURVE('',#13530,#13531,#3725,.T.);
#17221=EDGE_CURVE('',#13530,#13528,#11379,.T.);
#17222=EDGE_CURVE('',#13531,#13529,#11380,.T.);
#17223=EDGE_CURVE('',#13532,#13533,#3726,.T.);
#17224=EDGE_CURVE('',#13532,#13530,#11381,.T.);
#17225=EDGE_CURVE('',#13533,#13531,#11382,.T.);
#17226=EDGE_CURVE('',#13534,#13535,#3727,.T.);
#17227=EDGE_CURVE('',#13534,#13532,#11383,.T.);
#17228=EDGE_CURVE('',#13535,#13533,#11384,.T.);
#17229=EDGE_CURVE('',#13536,#13537,#3728,.T.);
#17230=EDGE_CURVE('',#13536,#13534,#11385,.T.);
#17231=EDGE_CURVE('',#13537,#13535,#11386,.T.);
#17232=EDGE_CURVE('',#13538,#13539,#3729,.T.);
#17233=EDGE_CURVE('',#13538,#13536,#11387,.T.);
#17234=EDGE_CURVE('',#13539,#13537,#11388,.T.);
#17235=EDGE_CURVE('',#13540,#13541,#3730,.T.);
#17236=EDGE_CURVE('',#13540,#13538,#11389,.T.);
#17237=EDGE_CURVE('',#13541,#13539,#11390,.T.);
#17238=EDGE_CURVE('',#13542,#13505,#11391,.T.);
#17239=EDGE_CURVE('',#13499,#13542,#11392,.T.);
#17240=EDGE_CURVE('',#13543,#13461,#11393,.T.);
#17241=EDGE_CURVE('',#13543,#13541,#11394,.T.);
#17242=EDGE_CURVE('',#13461,#13544,#10884,.T.);
#17243=EDGE_CURVE('',#13544,#13460,#10885,.T.);
#17244=EDGE_CURVE('',#13460,#13545,#11395,.T.);
#17245=EDGE_CURVE('',#13545,#13543,#10886,.T.);
#17246=EDGE_CURVE('',#13545,#13540,#11396,.T.);
#17247=EDGE_CURVE('',#13502,#13546,#11397,.T.);
#17248=EDGE_CURVE('',#13546,#13498,#11398,.T.);
#17249=EDGE_CURVE('',#13547,#13548,#3731,.T.);
#17250=EDGE_CURVE('',#13547,#13549,#3732,.T.);
#17251=EDGE_CURVE('',#13550,#13549,#3733,.T.);
#17252=EDGE_CURVE('',#13548,#13550,#3734,.T.);
#17253=EDGE_CURVE('',#13548,#13551,#10887,.T.);
#17254=EDGE_CURVE('',#13550,#13551,#3735,.T.);
#17255=EDGE_CURVE('',#13551,#13552,#3736,.T.);
#17256=EDGE_CURVE('',#13549,#13552,#3737,.T.);
#17257=EDGE_CURVE('',#13552,#13547,#10888,.T.);
#17258=EDGE_CURVE('',#13553,#13554,#3738,.T.);
#17259=EDGE_CURVE('',#13553,#13555,#3739,.T.);
#17260=EDGE_CURVE('',#13556,#13555,#3740,.T.);
#17261=EDGE_CURVE('',#13554,#13556,#3741,.T.);
#17262=EDGE_CURVE('',#13554,#13557,#10889,.T.);
#17263=EDGE_CURVE('',#13556,#13557,#3742,.T.);
#17264=EDGE_CURVE('',#13557,#13558,#3743,.T.);
#17265=EDGE_CURVE('',#13555,#13558,#3744,.T.);
#17266=EDGE_CURVE('',#13558,#13553,#10890,.T.);
#17267=EDGE_CURVE('',#13559,#13560,#3745,.T.);
#17268=EDGE_CURVE('',#13559,#13561,#3746,.T.);
#17269=EDGE_CURVE('',#13562,#13561,#3747,.T.);
#17270=EDGE_CURVE('',#13560,#13562,#3748,.T.);
#17271=EDGE_CURVE('',#13560,#13563,#10891,.T.);
#17272=EDGE_CURVE('',#13562,#13563,#3749,.T.);
#17273=EDGE_CURVE('',#13563,#13564,#3750,.T.);
#17274=EDGE_CURVE('',#13561,#13564,#3751,.T.);
#17275=EDGE_CURVE('',#13564,#13559,#10892,.T.);
#17276=EDGE_CURVE('',#13565,#13566,#3752,.T.);
#17277=EDGE_CURVE('',#13565,#13567,#3753,.T.);
#17278=EDGE_CURVE('',#13568,#13567,#3754,.T.);
#17279=EDGE_CURVE('',#13566,#13568,#3755,.T.);
#17280=EDGE_CURVE('',#13566,#13569,#10893,.T.);
#17281=EDGE_CURVE('',#13568,#13569,#3756,.T.);
#17282=EDGE_CURVE('',#13569,#13570,#3757,.T.);
#17283=EDGE_CURVE('',#13567,#13570,#3758,.T.);
#17284=EDGE_CURVE('',#13570,#13565,#10894,.T.);
#17285=EDGE_CURVE('',#13571,#13572,#3759,.T.);
#17286=EDGE_CURVE('',#13571,#13573,#3760,.T.);
#17287=EDGE_CURVE('',#13574,#13573,#3761,.T.);
#17288=EDGE_CURVE('',#13572,#13574,#3762,.T.);
#17289=EDGE_CURVE('',#13572,#13575,#10895,.T.);
#17290=EDGE_CURVE('',#13574,#13575,#3763,.T.);
#17291=EDGE_CURVE('',#13575,#13576,#3764,.T.);
#17292=EDGE_CURVE('',#13573,#13576,#3765,.T.);
#17293=EDGE_CURVE('',#13576,#13571,#10896,.T.);
#17294=EDGE_CURVE('',#13577,#13578,#3766,.T.);
#17295=EDGE_CURVE('',#13577,#13579,#3767,.T.);
#17296=EDGE_CURVE('',#13580,#13579,#3768,.T.);
#17297=EDGE_CURVE('',#13578,#13580,#3769,.T.);
#17298=EDGE_CURVE('',#13578,#13581,#10897,.T.);
#17299=EDGE_CURVE('',#13580,#13581,#3770,.T.);
#17300=EDGE_CURVE('',#13581,#13582,#3771,.T.);
#17301=EDGE_CURVE('',#13579,#13582,#3772,.T.);
#17302=EDGE_CURVE('',#13582,#13577,#10898,.T.);
#17303=EDGE_CURVE('',#13583,#13584,#3773,.T.);
#17304=EDGE_CURVE('',#13583,#13585,#3774,.T.);
#17305=EDGE_CURVE('',#13586,#13585,#3775,.T.);
#17306=EDGE_CURVE('',#13584,#13586,#3776,.T.);
#17307=EDGE_CURVE('',#13584,#13587,#10899,.T.);
#17308=EDGE_CURVE('',#13586,#13587,#3777,.T.);
#17309=EDGE_CURVE('',#13587,#13588,#3778,.T.);
#17310=EDGE_CURVE('',#13585,#13588,#3779,.T.);
#17311=EDGE_CURVE('',#13588,#13583,#10900,.T.);
#17312=EDGE_CURVE('',#13589,#13590,#3780,.T.);
#17313=EDGE_CURVE('',#13589,#13591,#3781,.T.);
#17314=EDGE_CURVE('',#13592,#13591,#3782,.T.);
#17315=EDGE_CURVE('',#13590,#13592,#3783,.T.);
#17316=EDGE_CURVE('',#13590,#13593,#10901,.T.);
#17317=EDGE_CURVE('',#13592,#13593,#3784,.T.);
#17318=EDGE_CURVE('',#13593,#13594,#3785,.T.);
#17319=EDGE_CURVE('',#13591,#13594,#3786,.T.);
#17320=EDGE_CURVE('',#13594,#13589,#10902,.T.);
#17321=EDGE_CURVE('',#13595,#13596,#3787,.T.);
#17322=EDGE_CURVE('',#13595,#13597,#3788,.T.);
#17323=EDGE_CURVE('',#13598,#13597,#3789,.T.);
#17324=EDGE_CURVE('',#13596,#13598,#3790,.T.);
#17325=EDGE_CURVE('',#13596,#13599,#10903,.T.);
#17326=EDGE_CURVE('',#13598,#13599,#3791,.T.);
#17327=EDGE_CURVE('',#13599,#13600,#3792,.T.);
#17328=EDGE_CURVE('',#13597,#13600,#3793,.T.);
#17329=EDGE_CURVE('',#13600,#13595,#10904,.T.);
#17330=EDGE_CURVE('',#13601,#13602,#3794,.T.);
#17331=EDGE_CURVE('',#13601,#13603,#3795,.T.);
#17332=EDGE_CURVE('',#13604,#13603,#3796,.T.);
#17333=EDGE_CURVE('',#13602,#13604,#3797,.T.);
#17334=EDGE_CURVE('',#13602,#13605,#10905,.T.);
#17335=EDGE_CURVE('',#13604,#13605,#3798,.T.);
#17336=EDGE_CURVE('',#13605,#13606,#3799,.T.);
#17337=EDGE_CURVE('',#13603,#13606,#3800,.T.);
#17338=EDGE_CURVE('',#13606,#13601,#10906,.T.);
#17339=EDGE_CURVE('',#13607,#13608,#3801,.T.);
#17340=EDGE_CURVE('',#13607,#13609,#3802,.T.);
#17341=EDGE_CURVE('',#13610,#13609,#3803,.T.);
#17342=EDGE_CURVE('',#13608,#13610,#3804,.T.);
#17343=EDGE_CURVE('',#13608,#13611,#10907,.T.);
#17344=EDGE_CURVE('',#13610,#13611,#3805,.T.);
#17345=EDGE_CURVE('',#13611,#13612,#3806,.T.);
#17346=EDGE_CURVE('',#13609,#13612,#3807,.T.);
#17347=EDGE_CURVE('',#13612,#13607,#10908,.T.);
#17348=EDGE_CURVE('',#13613,#13614,#3808,.T.);
#17349=EDGE_CURVE('',#13613,#13615,#3809,.T.);
#17350=EDGE_CURVE('',#13616,#13615,#3810,.T.);
#17351=EDGE_CURVE('',#13614,#13616,#3811,.T.);
#17352=EDGE_CURVE('',#13614,#13617,#10909,.T.);
#17353=EDGE_CURVE('',#13616,#13617,#3812,.T.);
#17354=EDGE_CURVE('',#13617,#13618,#3813,.T.);
#17355=EDGE_CURVE('',#13615,#13618,#3814,.T.);
#17356=EDGE_CURVE('',#13618,#13613,#10910,.T.);
#17357=EDGE_CURVE('',#13619,#13620,#3815,.T.);
#17358=EDGE_CURVE('',#13619,#13621,#3816,.T.);
#17359=EDGE_CURVE('',#13622,#13621,#3817,.T.);
#17360=EDGE_CURVE('',#13620,#13622,#3818,.T.);
#17361=EDGE_CURVE('',#13620,#13623,#10911,.T.);
#17362=EDGE_CURVE('',#13622,#13623,#3819,.T.);
#17363=EDGE_CURVE('',#13623,#13624,#3820,.T.);
#17364=EDGE_CURVE('',#13621,#13624,#3821,.T.);
#17365=EDGE_CURVE('',#13624,#13619,#10912,.T.);
#17366=EDGE_CURVE('',#13625,#13626,#3822,.T.);
#17367=EDGE_CURVE('',#13625,#13627,#3823,.T.);
#17368=EDGE_CURVE('',#13628,#13627,#3824,.T.);
#17369=EDGE_CURVE('',#13626,#13628,#3825,.T.);
#17370=EDGE_CURVE('',#13626,#13629,#10913,.T.);
#17371=EDGE_CURVE('',#13628,#13629,#3826,.T.);
#17372=EDGE_CURVE('',#13629,#13630,#3827,.T.);
#17373=EDGE_CURVE('',#13627,#13630,#3828,.T.);
#17374=EDGE_CURVE('',#13630,#13625,#10914,.T.);
#17375=EDGE_CURVE('',#13631,#13632,#3829,.T.);
#17376=EDGE_CURVE('',#13631,#13633,#3830,.T.);
#17377=EDGE_CURVE('',#13634,#13633,#3831,.T.);
#17378=EDGE_CURVE('',#13632,#13634,#3832,.T.);
#17379=EDGE_CURVE('',#13632,#13635,#10915,.T.);
#17380=EDGE_CURVE('',#13634,#13635,#3833,.T.);
#17381=EDGE_CURVE('',#13635,#13636,#3834,.T.);
#17382=EDGE_CURVE('',#13633,#13636,#3835,.T.);
#17383=EDGE_CURVE('',#13636,#13631,#10916,.T.);
#17384=EDGE_CURVE('',#13637,#13638,#3836,.T.);
#17385=EDGE_CURVE('',#13637,#13639,#3837,.T.);
#17386=EDGE_CURVE('',#13640,#13639,#3838,.T.);
#17387=EDGE_CURVE('',#13638,#13640,#3839,.T.);
#17388=EDGE_CURVE('',#13638,#13641,#10917,.T.);
#17389=EDGE_CURVE('',#13640,#13641,#3840,.T.);
#17390=EDGE_CURVE('',#13641,#13642,#3841,.T.);
#17391=EDGE_CURVE('',#13639,#13642,#3842,.T.);
#17392=EDGE_CURVE('',#13642,#13637,#10918,.T.);
#17393=EDGE_CURVE('',#13643,#13644,#3843,.T.);
#17394=EDGE_CURVE('',#13643,#13645,#3844,.T.);
#17395=EDGE_CURVE('',#13646,#13645,#3845,.T.);
#17396=EDGE_CURVE('',#13644,#13646,#3846,.T.);
#17397=EDGE_CURVE('',#13644,#13647,#10919,.T.);
#17398=EDGE_CURVE('',#13646,#13647,#3847,.T.);
#17399=EDGE_CURVE('',#13647,#13648,#3848,.T.);
#17400=EDGE_CURVE('',#13645,#13648,#3849,.T.);
#17401=EDGE_CURVE('',#13648,#13643,#10920,.T.);
#17402=EDGE_CURVE('',#13649,#13650,#3850,.T.);
#17403=EDGE_CURVE('',#13649,#13651,#3851,.T.);
#17404=EDGE_CURVE('',#13652,#13651,#3852,.T.);
#17405=EDGE_CURVE('',#13650,#13652,#3853,.T.);
#17406=EDGE_CURVE('',#13650,#13653,#10921,.T.);
#17407=EDGE_CURVE('',#13652,#13654,#3854,.T.);
#17408=EDGE_CURVE('',#13653,#13654,#10922,.T.);
#17409=EDGE_CURVE('',#13654,#13655,#3855,.T.);
#17410=EDGE_CURVE('',#13651,#13655,#3856,.T.);
#17411=EDGE_CURVE('',#13655,#13656,#10923,.T.);
#17412=EDGE_CURVE('',#13656,#13649,#10924,.T.);
#17413=EDGE_CURVE('',#13657,#13658,#3857,.T.);
#17414=EDGE_CURVE('',#13657,#13659,#3858,.T.);
#17415=EDGE_CURVE('',#13660,#13659,#3859,.T.);
#17416=EDGE_CURVE('',#13658,#13660,#3860,.T.);
#17417=EDGE_CURVE('',#13658,#13661,#10925,.T.);
#17418=EDGE_CURVE('',#13660,#13661,#3861,.T.);
#17419=EDGE_CURVE('',#13661,#13662,#3862,.T.);
#17420=EDGE_CURVE('',#13659,#13662,#3863,.T.);
#17421=EDGE_CURVE('',#13662,#13657,#10926,.T.);
#17422=EDGE_CURVE('',#13663,#13664,#3864,.T.);
#17423=EDGE_CURVE('',#13663,#13665,#3865,.T.);
#17424=EDGE_CURVE('',#13666,#13665,#3866,.T.);
#17425=EDGE_CURVE('',#13664,#13666,#3867,.T.);
#17426=EDGE_CURVE('',#13664,#13667,#10927,.T.);
#17427=EDGE_CURVE('',#13666,#13667,#3868,.T.);
#17428=EDGE_CURVE('',#13667,#13668,#3869,.T.);
#17429=EDGE_CURVE('',#13665,#13668,#3870,.T.);
#17430=EDGE_CURVE('',#13668,#13663,#10928,.T.);
#17431=EDGE_CURVE('',#13669,#13670,#3871,.T.);
#17432=EDGE_CURVE('',#13669,#13671,#3872,.T.);
#17433=EDGE_CURVE('',#13672,#13671,#3873,.T.);
#17434=EDGE_CURVE('',#13670,#13672,#3874,.T.);
#17435=EDGE_CURVE('',#13670,#13673,#10929,.T.);
#17436=EDGE_CURVE('',#13672,#13673,#3875,.T.);
#17437=EDGE_CURVE('',#13673,#13674,#3876,.T.);
#17438=EDGE_CURVE('',#13671,#13674,#3877,.T.);
#17439=EDGE_CURVE('',#13674,#13669,#10930,.T.);
#17440=EDGE_CURVE('',#13675,#13676,#3878,.T.);
#17441=EDGE_CURVE('',#13675,#13677,#3879,.T.);
#17442=EDGE_CURVE('',#13678,#13677,#3880,.T.);
#17443=EDGE_CURVE('',#13676,#13678,#3881,.T.);
#17444=EDGE_CURVE('',#13676,#13679,#10931,.T.);
#17445=EDGE_CURVE('',#13678,#13679,#3882,.T.);
#17446=EDGE_CURVE('',#13679,#13680,#3883,.T.);
#17447=EDGE_CURVE('',#13677,#13680,#3884,.T.);
#17448=EDGE_CURVE('',#13680,#13675,#10932,.T.);
#17449=EDGE_CURVE('',#13681,#13682,#3885,.T.);
#17450=EDGE_CURVE('',#13681,#13683,#3886,.T.);
#17451=EDGE_CURVE('',#13684,#13683,#3887,.T.);
#17452=EDGE_CURVE('',#13682,#13684,#3888,.T.);
#17453=EDGE_CURVE('',#13682,#13685,#10933,.T.);
#17454=EDGE_CURVE('',#13684,#13685,#3889,.T.);
#17455=EDGE_CURVE('',#13685,#13686,#3890,.T.);
#17456=EDGE_CURVE('',#13683,#13686,#3891,.T.);
#17457=EDGE_CURVE('',#13686,#13681,#10934,.T.);
#17458=EDGE_CURVE('',#13687,#13688,#3892,.T.);
#17459=EDGE_CURVE('',#13687,#13689,#3893,.T.);
#17460=EDGE_CURVE('',#13690,#13689,#3894,.T.);
#17461=EDGE_CURVE('',#13688,#13690,#3895,.T.);
#17462=EDGE_CURVE('',#13688,#13691,#10935,.T.);
#17463=EDGE_CURVE('',#13690,#13691,#3896,.T.);
#17464=EDGE_CURVE('',#13691,#13692,#3897,.T.);
#17465=EDGE_CURVE('',#13689,#13692,#3898,.T.);
#17466=EDGE_CURVE('',#13692,#13687,#10936,.T.);
#17467=EDGE_CURVE('',#13693,#13694,#3899,.T.);
#17468=EDGE_CURVE('',#13693,#13695,#3900,.T.);
#17469=EDGE_CURVE('',#13696,#13695,#3901,.T.);
#17470=EDGE_CURVE('',#13694,#13696,#3902,.T.);
#17471=EDGE_CURVE('',#13694,#13697,#10937,.T.);
#17472=EDGE_CURVE('',#13696,#13697,#3903,.T.);
#17473=EDGE_CURVE('',#13697,#13698,#3904,.T.);
#17474=EDGE_CURVE('',#13695,#13698,#3905,.T.);
#17475=EDGE_CURVE('',#13698,#13693,#10938,.T.);
#17476=EDGE_CURVE('',#13699,#13700,#3906,.T.);
#17477=EDGE_CURVE('',#13699,#13701,#3907,.T.);
#17478=EDGE_CURVE('',#13702,#13701,#3908,.T.);
#17479=EDGE_CURVE('',#13700,#13702,#3909,.T.);
#17480=EDGE_CURVE('',#13700,#13703,#10939,.T.);
#17481=EDGE_CURVE('',#13702,#13703,#3910,.T.);
#17482=EDGE_CURVE('',#13703,#13704,#3911,.T.);
#17483=EDGE_CURVE('',#13701,#13704,#3912,.T.);
#17484=EDGE_CURVE('',#13704,#13699,#10940,.T.);
#17485=EDGE_CURVE('',#13705,#13706,#3913,.T.);
#17486=EDGE_CURVE('',#13705,#13707,#3914,.T.);
#17487=EDGE_CURVE('',#13708,#13707,#3915,.T.);
#17488=EDGE_CURVE('',#13706,#13708,#3916,.T.);
#17489=EDGE_CURVE('',#13706,#13709,#10941,.T.);
#17490=EDGE_CURVE('',#13708,#13709,#3917,.T.);
#17491=EDGE_CURVE('',#13709,#13710,#3918,.T.);
#17492=EDGE_CURVE('',#13707,#13710,#3919,.T.);
#17493=EDGE_CURVE('',#13710,#13705,#10942,.T.);
#17494=EDGE_CURVE('',#13711,#13712,#3920,.T.);
#17495=EDGE_CURVE('',#13711,#13713,#3921,.T.);
#17496=EDGE_CURVE('',#13714,#13713,#3922,.T.);
#17497=EDGE_CURVE('',#13712,#13714,#3923,.T.);
#17498=EDGE_CURVE('',#13712,#13715,#10943,.T.);
#17499=EDGE_CURVE('',#13714,#13715,#3924,.T.);
#17500=EDGE_CURVE('',#13715,#13716,#3925,.T.);
#17501=EDGE_CURVE('',#13713,#13716,#3926,.T.);
#17502=EDGE_CURVE('',#13716,#13711,#10944,.T.);
#17503=EDGE_CURVE('',#13717,#13718,#3927,.T.);
#17504=EDGE_CURVE('',#13717,#13719,#3928,.T.);
#17505=EDGE_CURVE('',#13720,#13719,#3929,.T.);
#17506=EDGE_CURVE('',#13718,#13720,#3930,.T.);
#17507=EDGE_CURVE('',#13718,#13721,#10945,.T.);
#17508=EDGE_CURVE('',#13720,#13721,#3931,.T.);
#17509=EDGE_CURVE('',#13721,#13722,#3932,.T.);
#17510=EDGE_CURVE('',#13719,#13722,#3933,.T.);
#17511=EDGE_CURVE('',#13722,#13717,#10946,.T.);
#17512=EDGE_CURVE('',#13723,#13724,#3934,.T.);
#17513=EDGE_CURVE('',#13723,#13725,#3935,.T.);
#17514=EDGE_CURVE('',#13726,#13725,#3936,.T.);
#17515=EDGE_CURVE('',#13724,#13726,#3937,.T.);
#17516=EDGE_CURVE('',#13724,#13727,#10947,.T.);
#17517=EDGE_CURVE('',#13726,#13727,#3938,.T.);
#17518=EDGE_CURVE('',#13727,#13728,#3939,.T.);
#17519=EDGE_CURVE('',#13725,#13728,#3940,.T.);
#17520=EDGE_CURVE('',#13728,#13723,#10948,.T.);
#17521=EDGE_CURVE('',#13729,#13730,#3941,.T.);
#17522=EDGE_CURVE('',#13729,#13731,#3942,.T.);
#17523=EDGE_CURVE('',#13732,#13731,#3943,.T.);
#17524=EDGE_CURVE('',#13730,#13732,#3944,.T.);
#17525=EDGE_CURVE('',#13730,#13733,#10949,.T.);
#17526=EDGE_CURVE('',#13732,#13733,#3945,.T.);
#17527=EDGE_CURVE('',#13733,#13734,#3946,.T.);
#17528=EDGE_CURVE('',#13731,#13734,#3947,.T.);
#17529=EDGE_CURVE('',#13734,#13729,#10950,.T.);
#17530=EDGE_CURVE('',#13735,#13736,#3948,.T.);
#17531=EDGE_CURVE('',#13735,#13737,#3949,.T.);
#17532=EDGE_CURVE('',#13738,#13737,#3950,.T.);
#17533=EDGE_CURVE('',#13736,#13738,#3951,.T.);
#17534=EDGE_CURVE('',#13736,#13739,#10951,.T.);
#17535=EDGE_CURVE('',#13738,#13739,#3952,.T.);
#17536=EDGE_CURVE('',#13739,#13740,#3953,.T.);
#17537=EDGE_CURVE('',#13737,#13740,#3954,.T.);
#17538=EDGE_CURVE('',#13740,#13735,#10952,.T.);
#17539=EDGE_CURVE('',#13741,#13742,#3955,.T.);
#17540=EDGE_CURVE('',#13741,#13743,#3956,.T.);
#17541=EDGE_CURVE('',#13744,#13743,#3957,.T.);
#17542=EDGE_CURVE('',#13742,#13744,#3958,.T.);
#17543=EDGE_CURVE('',#13742,#13745,#10953,.T.);
#17544=EDGE_CURVE('',#13744,#13745,#3959,.T.);
#17545=EDGE_CURVE('',#13745,#13746,#3960,.T.);
#17546=EDGE_CURVE('',#13743,#13746,#3961,.T.);
#17547=EDGE_CURVE('',#13746,#13741,#10954,.T.);
#17548=EDGE_CURVE('',#13747,#13748,#3962,.T.);
#17549=EDGE_CURVE('',#13747,#13749,#3963,.T.);
#17550=EDGE_CURVE('',#13750,#13749,#3964,.T.);
#17551=EDGE_CURVE('',#13748,#13750,#3965,.T.);
#17552=EDGE_CURVE('',#13748,#13751,#10955,.T.);
#17553=EDGE_CURVE('',#13750,#13751,#3966,.T.);
#17554=EDGE_CURVE('',#13751,#13752,#3967,.T.);
#17555=EDGE_CURVE('',#13749,#13752,#3968,.T.);
#17556=EDGE_CURVE('',#13752,#13747,#10956,.T.);
#17557=EDGE_CURVE('',#13753,#13754,#3969,.T.);
#17558=EDGE_CURVE('',#13753,#13755,#3970,.T.);
#17559=EDGE_CURVE('',#13756,#13755,#3971,.T.);
#17560=EDGE_CURVE('',#13754,#13756,#3972,.T.);
#17561=EDGE_CURVE('',#13754,#13757,#10957,.T.);
#17562=EDGE_CURVE('',#13756,#13757,#3973,.T.);
#17563=EDGE_CURVE('',#13757,#13758,#3974,.T.);
#17564=EDGE_CURVE('',#13755,#13758,#3975,.T.);
#17565=EDGE_CURVE('',#13758,#13753,#10958,.T.);
#17566=EDGE_CURVE('',#13759,#13760,#3976,.T.);
#17567=EDGE_CURVE('',#13759,#13761,#3977,.T.);
#17568=EDGE_CURVE('',#13762,#13761,#3978,.T.);
#17569=EDGE_CURVE('',#13760,#13762,#3979,.T.);
#17570=EDGE_CURVE('',#13760,#13763,#10959,.T.);
#17571=EDGE_CURVE('',#13762,#13763,#3980,.T.);
#17572=EDGE_CURVE('',#13763,#13764,#3981,.T.);
#17573=EDGE_CURVE('',#13761,#13764,#3982,.T.);
#17574=EDGE_CURVE('',#13764,#13759,#10960,.T.);
#17575=EDGE_CURVE('',#13765,#13766,#3983,.T.);
#17576=EDGE_CURVE('',#13765,#13767,#3984,.T.);
#17577=EDGE_CURVE('',#13767,#13768,#3985,.T.);
#17578=EDGE_CURVE('',#13766,#13768,#3986,.T.);
#17579=EDGE_CURVE('',#13769,#13765,#3987,.T.);
#17580=EDGE_CURVE('',#13769,#13770,#3988,.T.);
#17581=EDGE_CURVE('',#13770,#13767,#3989,.T.);
#17582=EDGE_CURVE('',#13771,#13769,#3990,.T.);
#17583=EDGE_CURVE('',#13771,#13772,#3991,.T.);
#17584=EDGE_CURVE('',#13772,#13770,#3992,.T.);
#17585=EDGE_CURVE('',#13773,#13771,#3993,.T.);
#17586=EDGE_CURVE('',#13773,#13774,#3994,.T.);
#17587=EDGE_CURVE('',#13774,#13772,#3995,.T.);
#17588=EDGE_CURVE('',#13775,#13773,#3996,.T.);
#17589=EDGE_CURVE('',#13775,#13776,#3997,.T.);
#17590=EDGE_CURVE('',#13776,#13774,#3998,.T.);
#17591=EDGE_CURVE('',#13766,#13775,#3999,.T.);
#17592=EDGE_CURVE('',#13768,#13776,#4000,.T.);
#17593=EDGE_CURVE('',#13777,#13777,#10961,.T.);
#17594=EDGE_CURVE('',#13544,#13777,#4001,.T.);
#17595=EDGE_CURVE('',#13546,#13542,#10962,.T.);
#17596=EDGE_CURVE('',#13778,#13778,#10963,.T.);
#17597=EDGE_CURVE('',#13779,#13779,#10964,.T.);
#17598=EDGE_CURVE('',#13779,#13656,#4002,.T.);
#17599=EDGE_CURVE('',#13653,#13778,#4003,.T.);
#17600=EDGE_CURVE('',#13780,#13780,#10965,.T.);
#17601=EDGE_CURVE('',#13780,#13779,#4004,.T.);
#24224=ORIENTED_EDGE('',*,*,#17116,.F.);
#24225=ORIENTED_EDGE('',*,*,#17117,.T.);
#24226=ORIENTED_EDGE('',*,*,#17118,.T.);
#24227=ORIENTED_EDGE('',*,*,#17119,.T.);
#24228=ORIENTED_EDGE('',*,*,#17120,.F.);
#24229=ORIENTED_EDGE('',*,*,#17121,.T.);
#24230=ORIENTED_EDGE('',*,*,#17116,.T.);
#24231=ORIENTED_EDGE('',*,*,#17122,.T.);
#24232=ORIENTED_EDGE('',*,*,#17123,.F.);
#24233=ORIENTED_EDGE('',*,*,#17124,.T.);
#24234=ORIENTED_EDGE('',*,*,#17120,.T.);
#24235=ORIENTED_EDGE('',*,*,#17125,.T.);
#24236=ORIENTED_EDGE('',*,*,#17126,.F.);
#24237=ORIENTED_EDGE('',*,*,#17127,.T.);
#24238=ORIENTED_EDGE('',*,*,#17123,.T.);
#24239=ORIENTED_EDGE('',*,*,#17128,.T.);
#24240=ORIENTED_EDGE('',*,*,#17129,.F.);
#24241=ORIENTED_EDGE('',*,*,#17130,.T.);
#24242=ORIENTED_EDGE('',*,*,#17126,.T.);
#24243=ORIENTED_EDGE('',*,*,#17131,.T.);
#24244=ORIENTED_EDGE('',*,*,#17132,.F.);
#24245=ORIENTED_EDGE('',*,*,#17133,.T.);
#24246=ORIENTED_EDGE('',*,*,#17129,.T.);
#24247=ORIENTED_EDGE('',*,*,#17134,.T.);
#24248=ORIENTED_EDGE('',*,*,#17135,.F.);
#24249=ORIENTED_EDGE('',*,*,#17136,.T.);
#24250=ORIENTED_EDGE('',*,*,#17132,.T.);
#24251=ORIENTED_EDGE('',*,*,#17137,.T.);
#24252=ORIENTED_EDGE('',*,*,#17138,.F.);
#24253=ORIENTED_EDGE('',*,*,#17139,.T.);
#24254=ORIENTED_EDGE('',*,*,#17135,.T.);
#24255=ORIENTED_EDGE('',*,*,#17140,.T.);
#24256=ORIENTED_EDGE('',*,*,#17141,.F.);
#24257=ORIENTED_EDGE('',*,*,#17142,.T.);
#24258=ORIENTED_EDGE('',*,*,#17138,.T.);
#24259=ORIENTED_EDGE('',*,*,#17143,.T.);
#24260=ORIENTED_EDGE('',*,*,#17144,.F.);
#24261=ORIENTED_EDGE('',*,*,#17145,.T.);
#24262=ORIENTED_EDGE('',*,*,#17141,.T.);
#24263=ORIENTED_EDGE('',*,*,#17146,.T.);
#24264=ORIENTED_EDGE('',*,*,#17147,.F.);
#24265=ORIENTED_EDGE('',*,*,#17148,.T.);
#24266=ORIENTED_EDGE('',*,*,#17144,.T.);
#24267=ORIENTED_EDGE('',*,*,#17149,.T.);
#24268=ORIENTED_EDGE('',*,*,#17150,.F.);
#24269=ORIENTED_EDGE('',*,*,#17151,.T.);
#24270=ORIENTED_EDGE('',*,*,#17147,.T.);
#24271=ORIENTED_EDGE('',*,*,#17152,.T.);
#24272=ORIENTED_EDGE('',*,*,#17153,.F.);
#24273=ORIENTED_EDGE('',*,*,#17154,.T.);
#24274=ORIENTED_EDGE('',*,*,#17150,.T.);
#24275=ORIENTED_EDGE('',*,*,#17155,.T.);
#24276=ORIENTED_EDGE('',*,*,#17156,.F.);
#24277=ORIENTED_EDGE('',*,*,#17157,.T.);
#24278=ORIENTED_EDGE('',*,*,#17153,.T.);
#24279=ORIENTED_EDGE('',*,*,#17158,.T.);
#24280=ORIENTED_EDGE('',*,*,#17159,.F.);
#24281=ORIENTED_EDGE('',*,*,#17160,.T.);
#24282=ORIENTED_EDGE('',*,*,#17156,.T.);
#24283=ORIENTED_EDGE('',*,*,#17161,.T.);
#24284=ORIENTED_EDGE('',*,*,#17162,.F.);
#24285=ORIENTED_EDGE('',*,*,#17163,.T.);
#24286=ORIENTED_EDGE('',*,*,#17159,.T.);
#24287=ORIENTED_EDGE('',*,*,#17164,.T.);
#24288=ORIENTED_EDGE('',*,*,#17165,.F.);
#24289=ORIENTED_EDGE('',*,*,#17166,.T.);
#24290=ORIENTED_EDGE('',*,*,#17162,.T.);
#24291=ORIENTED_EDGE('',*,*,#17167,.T.);
#24292=ORIENTED_EDGE('',*,*,#17168,.F.);
#24293=ORIENTED_EDGE('',*,*,#17169,.T.);
#24294=ORIENTED_EDGE('',*,*,#17165,.T.);
#24295=ORIENTED_EDGE('',*,*,#17170,.T.);
#24296=ORIENTED_EDGE('',*,*,#17171,.F.);
#24297=ORIENTED_EDGE('',*,*,#17172,.T.);
#24298=ORIENTED_EDGE('',*,*,#17168,.T.);
#24299=ORIENTED_EDGE('',*,*,#17173,.T.);
#24300=ORIENTED_EDGE('',*,*,#17174,.F.);
#24301=ORIENTED_EDGE('',*,*,#17175,.T.);
#24302=ORIENTED_EDGE('',*,*,#17171,.T.);
#24303=ORIENTED_EDGE('',*,*,#17176,.T.);
#24304=ORIENTED_EDGE('',*,*,#17177,.F.);
#24305=ORIENTED_EDGE('',*,*,#17178,.T.);
#24306=ORIENTED_EDGE('',*,*,#17179,.F.);
#24307=ORIENTED_EDGE('',*,*,#17180,.F.);
#24308=ORIENTED_EDGE('',*,*,#17181,.T.);
#24309=ORIENTED_EDGE('',*,*,#17177,.T.);
#24310=ORIENTED_EDGE('',*,*,#17182,.F.);
#24311=ORIENTED_EDGE('',*,*,#17183,.F.);
#24312=ORIENTED_EDGE('',*,*,#17184,.F.);
#24313=ORIENTED_EDGE('',*,*,#17185,.T.);
#24314=ORIENTED_EDGE('',*,*,#17180,.T.);
#24315=ORIENTED_EDGE('',*,*,#17186,.F.);
#24316=ORIENTED_EDGE('',*,*,#17187,.F.);
#24317=ORIENTED_EDGE('',*,*,#17188,.T.);
#24318=ORIENTED_EDGE('',*,*,#17184,.T.);
#24319=ORIENTED_EDGE('',*,*,#17189,.F.);
#24320=ORIENTED_EDGE('',*,*,#17190,.F.);
#24321=ORIENTED_EDGE('',*,*,#17191,.T.);
#24322=ORIENTED_EDGE('',*,*,#17187,.T.);
#24323=ORIENTED_EDGE('',*,*,#17192,.F.);
#24324=ORIENTED_EDGE('',*,*,#17193,.F.);
#24325=ORIENTED_EDGE('',*,*,#17194,.T.);
#24326=ORIENTED_EDGE('',*,*,#17190,.T.);
#24327=ORIENTED_EDGE('',*,*,#17195,.F.);
#24328=ORIENTED_EDGE('',*,*,#17196,.F.);
#24329=ORIENTED_EDGE('',*,*,#17197,.T.);
#24330=ORIENTED_EDGE('',*,*,#17193,.T.);
#24331=ORIENTED_EDGE('',*,*,#17198,.F.);
#24332=ORIENTED_EDGE('',*,*,#17199,.F.);
#24333=ORIENTED_EDGE('',*,*,#17200,.T.);
#24334=ORIENTED_EDGE('',*,*,#17196,.T.);
#24335=ORIENTED_EDGE('',*,*,#17201,.F.);
#24336=ORIENTED_EDGE('',*,*,#17202,.F.);
#24337=ORIENTED_EDGE('',*,*,#17203,.T.);
#24338=ORIENTED_EDGE('',*,*,#17199,.T.);
#24339=ORIENTED_EDGE('',*,*,#17204,.F.);
#24340=ORIENTED_EDGE('',*,*,#17205,.F.);
#24341=ORIENTED_EDGE('',*,*,#17206,.T.);
#24342=ORIENTED_EDGE('',*,*,#17202,.T.);
#24343=ORIENTED_EDGE('',*,*,#17207,.F.);
#24344=ORIENTED_EDGE('',*,*,#17208,.F.);
#24345=ORIENTED_EDGE('',*,*,#17209,.T.);
#24346=ORIENTED_EDGE('',*,*,#17205,.T.);
#24347=ORIENTED_EDGE('',*,*,#17210,.F.);
#24348=ORIENTED_EDGE('',*,*,#17211,.F.);
#24349=ORIENTED_EDGE('',*,*,#17212,.T.);
#24350=ORIENTED_EDGE('',*,*,#17208,.T.);
#24351=ORIENTED_EDGE('',*,*,#17213,.F.);
#24352=ORIENTED_EDGE('',*,*,#17214,.F.);
#24353=ORIENTED_EDGE('',*,*,#17215,.T.);
#24354=ORIENTED_EDGE('',*,*,#17211,.T.);
#24355=ORIENTED_EDGE('',*,*,#17216,.F.);
#24356=ORIENTED_EDGE('',*,*,#17217,.F.);
#24357=ORIENTED_EDGE('',*,*,#17218,.T.);
#24358=ORIENTED_EDGE('',*,*,#17214,.T.);
#24359=ORIENTED_EDGE('',*,*,#17219,.F.);
#24360=ORIENTED_EDGE('',*,*,#17220,.F.);
#24361=ORIENTED_EDGE('',*,*,#17221,.T.);
#24362=ORIENTED_EDGE('',*,*,#17217,.T.);
#24363=ORIENTED_EDGE('',*,*,#17222,.F.);
#24364=ORIENTED_EDGE('',*,*,#17223,.F.);
#24365=ORIENTED_EDGE('',*,*,#17224,.T.);
#24366=ORIENTED_EDGE('',*,*,#17220,.T.);
#24367=ORIENTED_EDGE('',*,*,#17225,.F.);
#24368=ORIENTED_EDGE('',*,*,#17226,.F.);
#24369=ORIENTED_EDGE('',*,*,#17227,.T.);
#24370=ORIENTED_EDGE('',*,*,#17223,.T.);
#24371=ORIENTED_EDGE('',*,*,#17228,.F.);
#24372=ORIENTED_EDGE('',*,*,#17229,.F.);
#24373=ORIENTED_EDGE('',*,*,#17230,.T.);
#24374=ORIENTED_EDGE('',*,*,#17226,.T.);
#24375=ORIENTED_EDGE('',*,*,#17231,.F.);
#24376=ORIENTED_EDGE('',*,*,#17232,.F.);
#24377=ORIENTED_EDGE('',*,*,#17233,.T.);
#24378=ORIENTED_EDGE('',*,*,#17229,.T.);
#24379=ORIENTED_EDGE('',*,*,#17234,.F.);
#24380=ORIENTED_EDGE('',*,*,#17235,.F.);
#24381=ORIENTED_EDGE('',*,*,#17236,.T.);
#24382=ORIENTED_EDGE('',*,*,#17232,.T.);
#24383=ORIENTED_EDGE('',*,*,#17237,.F.);
#24384=ORIENTED_EDGE('',*,*,#17238,.F.);
#24385=ORIENTED_EDGE('',*,*,#17239,.F.);
#24386=ORIENTED_EDGE('',*,*,#17176,.F.);
#24387=ORIENTED_EDGE('',*,*,#17173,.F.);
#24388=ORIENTED_EDGE('',*,*,#17170,.F.);
#24389=ORIENTED_EDGE('',*,*,#17167,.F.);
#24390=ORIENTED_EDGE('',*,*,#17164,.F.);
#24391=ORIENTED_EDGE('',*,*,#17161,.F.);
#24392=ORIENTED_EDGE('',*,*,#17158,.F.);
#24393=ORIENTED_EDGE('',*,*,#17155,.F.);
#24394=ORIENTED_EDGE('',*,*,#17152,.F.);
#24395=ORIENTED_EDGE('',*,*,#17149,.F.);
#24396=ORIENTED_EDGE('',*,*,#17146,.F.);
#24397=ORIENTED_EDGE('',*,*,#17143,.F.);
#24398=ORIENTED_EDGE('',*,*,#17140,.F.);
#24399=ORIENTED_EDGE('',*,*,#17137,.F.);
#24400=ORIENTED_EDGE('',*,*,#17134,.F.);
#24401=ORIENTED_EDGE('',*,*,#17131,.F.);
#24402=ORIENTED_EDGE('',*,*,#17128,.F.);
#24403=ORIENTED_EDGE('',*,*,#17125,.F.);
#24404=ORIENTED_EDGE('',*,*,#17122,.F.);
#24405=ORIENTED_EDGE('',*,*,#17119,.F.);
#24406=ORIENTED_EDGE('',*,*,#17240,.F.);
#24407=ORIENTED_EDGE('',*,*,#17241,.T.);
#24408=ORIENTED_EDGE('',*,*,#17237,.T.);
#24409=ORIENTED_EDGE('',*,*,#17234,.T.);
#24410=ORIENTED_EDGE('',*,*,#17231,.T.);
#24411=ORIENTED_EDGE('',*,*,#17228,.T.);
#24412=ORIENTED_EDGE('',*,*,#17225,.T.);
#24413=ORIENTED_EDGE('',*,*,#17222,.T.);
#24414=ORIENTED_EDGE('',*,*,#17219,.T.);
#24415=ORIENTED_EDGE('',*,*,#17216,.T.);
#24416=ORIENTED_EDGE('',*,*,#17213,.T.);
#24417=ORIENTED_EDGE('',*,*,#17210,.T.);
#24418=ORIENTED_EDGE('',*,*,#17207,.T.);
#24419=ORIENTED_EDGE('',*,*,#17204,.T.);
#24420=ORIENTED_EDGE('',*,*,#17201,.T.);
#24421=ORIENTED_EDGE('',*,*,#17198,.T.);
#24422=ORIENTED_EDGE('',*,*,#17195,.T.);
#24423=ORIENTED_EDGE('',*,*,#17192,.T.);
#24424=ORIENTED_EDGE('',*,*,#17189,.T.);
#24425=ORIENTED_EDGE('',*,*,#17186,.T.);
#24426=ORIENTED_EDGE('',*,*,#17183,.T.);
#24427=ORIENTED_EDGE('',*,*,#17242,.T.);
#24428=ORIENTED_EDGE('',*,*,#17243,.T.);
#24429=ORIENTED_EDGE('',*,*,#17244,.T.);
#24430=ORIENTED_EDGE('',*,*,#17245,.T.);
#24431=ORIENTED_EDGE('',*,*,#17240,.T.);
#24432=ORIENTED_EDGE('',*,*,#17235,.T.);
#24433=ORIENTED_EDGE('',*,*,#17241,.F.);
#24434=ORIENTED_EDGE('',*,*,#17245,.F.);
#24435=ORIENTED_EDGE('',*,*,#17246,.T.);
#24436=ORIENTED_EDGE('',*,*,#17247,.F.);
#24437=ORIENTED_EDGE('',*,*,#17178,.F.);
#24438=ORIENTED_EDGE('',*,*,#17181,.F.);
#24439=ORIENTED_EDGE('',*,*,#17185,.F.);
#24440=ORIENTED_EDGE('',*,*,#17188,.F.);
#24441=ORIENTED_EDGE('',*,*,#17191,.F.);
#24442=ORIENTED_EDGE('',*,*,#17194,.F.);
#24443=ORIENTED_EDGE('',*,*,#17197,.F.);
#24444=ORIENTED_EDGE('',*,*,#17200,.F.);
#24445=ORIENTED_EDGE('',*,*,#17203,.F.);
#24446=ORIENTED_EDGE('',*,*,#17206,.F.);
#24447=ORIENTED_EDGE('',*,*,#17209,.F.);
#24448=ORIENTED_EDGE('',*,*,#17212,.F.);
#24449=ORIENTED_EDGE('',*,*,#17215,.F.);
#24450=ORIENTED_EDGE('',*,*,#17218,.F.);
#24451=ORIENTED_EDGE('',*,*,#17221,.F.);
#24452=ORIENTED_EDGE('',*,*,#17224,.F.);
#24453=ORIENTED_EDGE('',*,*,#17227,.F.);
#24454=ORIENTED_EDGE('',*,*,#17230,.F.);
#24455=ORIENTED_EDGE('',*,*,#17233,.F.);
#24456=ORIENTED_EDGE('',*,*,#17236,.F.);
#24457=ORIENTED_EDGE('',*,*,#17246,.F.);
#24458=ORIENTED_EDGE('',*,*,#17244,.F.);
#24459=ORIENTED_EDGE('',*,*,#17117,.F.);
#24460=ORIENTED_EDGE('',*,*,#17121,.F.);
#24461=ORIENTED_EDGE('',*,*,#17124,.F.);
#24462=ORIENTED_EDGE('',*,*,#17127,.F.);
#24463=ORIENTED_EDGE('',*,*,#17130,.F.);
#24464=ORIENTED_EDGE('',*,*,#17133,.F.);
#24465=ORIENTED_EDGE('',*,*,#17136,.F.);
#24466=ORIENTED_EDGE('',*,*,#17139,.F.);
#24467=ORIENTED_EDGE('',*,*,#17142,.F.);
#24468=ORIENTED_EDGE('',*,*,#17145,.F.);
#24469=ORIENTED_EDGE('',*,*,#17148,.F.);
#24470=ORIENTED_EDGE('',*,*,#17151,.F.);
#24471=ORIENTED_EDGE('',*,*,#17154,.F.);
#24472=ORIENTED_EDGE('',*,*,#17157,.F.);
#24473=ORIENTED_EDGE('',*,*,#17160,.F.);
#24474=ORIENTED_EDGE('',*,*,#17163,.F.);
#24475=ORIENTED_EDGE('',*,*,#17166,.F.);
#24476=ORIENTED_EDGE('',*,*,#17169,.F.);
#24477=ORIENTED_EDGE('',*,*,#17172,.F.);
#24478=ORIENTED_EDGE('',*,*,#17175,.F.);
#24479=ORIENTED_EDGE('',*,*,#17248,.F.);
#24480=ORIENTED_EDGE('',*,*,#17249,.F.);
#24481=ORIENTED_EDGE('',*,*,#17250,.T.);
#24482=ORIENTED_EDGE('',*,*,#17251,.F.);
#24483=ORIENTED_EDGE('',*,*,#17252,.F.);
#24484=ORIENTED_EDGE('',*,*,#17253,.F.);
#24485=ORIENTED_EDGE('',*,*,#17252,.T.);
#24486=ORIENTED_EDGE('',*,*,#17254,.T.);
#24487=ORIENTED_EDGE('',*,*,#17255,.F.);
#24488=ORIENTED_EDGE('',*,*,#17254,.F.);
#24489=ORIENTED_EDGE('',*,*,#17251,.T.);
#24490=ORIENTED_EDGE('',*,*,#17256,.T.);
#24491=ORIENTED_EDGE('',*,*,#17257,.F.);
#24492=ORIENTED_EDGE('',*,*,#17256,.F.);
#24493=ORIENTED_EDGE('',*,*,#17250,.F.);
#24494=ORIENTED_EDGE('',*,*,#17258,.F.);
#24495=ORIENTED_EDGE('',*,*,#17259,.T.);
#24496=ORIENTED_EDGE('',*,*,#17260,.F.);
#24497=ORIENTED_EDGE('',*,*,#17261,.F.);
#24498=ORIENTED_EDGE('',*,*,#17262,.F.);
#24499=ORIENTED_EDGE('',*,*,#17261,.T.);
#24500=ORIENTED_EDGE('',*,*,#17263,.T.);
#24501=ORIENTED_EDGE('',*,*,#17264,.F.);
#24502=ORIENTED_EDGE('',*,*,#17263,.F.);
#24503=ORIENTED_EDGE('',*,*,#17260,.T.);
#24504=ORIENTED_EDGE('',*,*,#17265,.T.);
#24505=ORIENTED_EDGE('',*,*,#17266,.F.);
#24506=ORIENTED_EDGE('',*,*,#17265,.F.);
#24507=ORIENTED_EDGE('',*,*,#17259,.F.);
#24508=ORIENTED_EDGE('',*,*,#17267,.F.);
#24509=ORIENTED_EDGE('',*,*,#17268,.T.);
#24510=ORIENTED_EDGE('',*,*,#17269,.F.);
#24511=ORIENTED_EDGE('',*,*,#17270,.F.);
#24512=ORIENTED_EDGE('',*,*,#17271,.F.);
#24513=ORIENTED_EDGE('',*,*,#17270,.T.);
#24514=ORIENTED_EDGE('',*,*,#17272,.T.);
#24515=ORIENTED_EDGE('',*,*,#17273,.F.);
#24516=ORIENTED_EDGE('',*,*,#17272,.F.);
#24517=ORIENTED_EDGE('',*,*,#17269,.T.);
#24518=ORIENTED_EDGE('',*,*,#17274,.T.);
#24519=ORIENTED_EDGE('',*,*,#17275,.F.);
#24520=ORIENTED_EDGE('',*,*,#17274,.F.);
#24521=ORIENTED_EDGE('',*,*,#17268,.F.);
#24522=ORIENTED_EDGE('',*,*,#17276,.F.);
#24523=ORIENTED_EDGE('',*,*,#17277,.T.);
#24524=ORIENTED_EDGE('',*,*,#17278,.F.);
#24525=ORIENTED_EDGE('',*,*,#17279,.F.);
#24526=ORIENTED_EDGE('',*,*,#17280,.F.);
#24527=ORIENTED_EDGE('',*,*,#17279,.T.);
#24528=ORIENTED_EDGE('',*,*,#17281,.T.);
#24529=ORIENTED_EDGE('',*,*,#17282,.F.);
#24530=ORIENTED_EDGE('',*,*,#17281,.F.);
#24531=ORIENTED_EDGE('',*,*,#17278,.T.);
#24532=ORIENTED_EDGE('',*,*,#17283,.T.);
#24533=ORIENTED_EDGE('',*,*,#17284,.F.);
#24534=ORIENTED_EDGE('',*,*,#17283,.F.);
#24535=ORIENTED_EDGE('',*,*,#17277,.F.);
#24536=ORIENTED_EDGE('',*,*,#17285,.F.);
#24537=ORIENTED_EDGE('',*,*,#17286,.T.);
#24538=ORIENTED_EDGE('',*,*,#17287,.F.);
#24539=ORIENTED_EDGE('',*,*,#17288,.F.);
#24540=ORIENTED_EDGE('',*,*,#17289,.F.);
#24541=ORIENTED_EDGE('',*,*,#17288,.T.);
#24542=ORIENTED_EDGE('',*,*,#17290,.T.);
#24543=ORIENTED_EDGE('',*,*,#17291,.F.);
#24544=ORIENTED_EDGE('',*,*,#17290,.F.);
#24545=ORIENTED_EDGE('',*,*,#17287,.T.);
#24546=ORIENTED_EDGE('',*,*,#17292,.T.);
#24547=ORIENTED_EDGE('',*,*,#17293,.F.);
#24548=ORIENTED_EDGE('',*,*,#17292,.F.);
#24549=ORIENTED_EDGE('',*,*,#17286,.F.);
#24550=ORIENTED_EDGE('',*,*,#17294,.F.);
#24551=ORIENTED_EDGE('',*,*,#17295,.T.);
#24552=ORIENTED_EDGE('',*,*,#17296,.F.);
#24553=ORIENTED_EDGE('',*,*,#17297,.F.);
#24554=ORIENTED_EDGE('',*,*,#17298,.F.);
#24555=ORIENTED_EDGE('',*,*,#17297,.T.);
#24556=ORIENTED_EDGE('',*,*,#17299,.T.);
#24557=ORIENTED_EDGE('',*,*,#17300,.F.);
#24558=ORIENTED_EDGE('',*,*,#17299,.F.);
#24559=ORIENTED_EDGE('',*,*,#17296,.T.);
#24560=ORIENTED_EDGE('',*,*,#17301,.T.);
#24561=ORIENTED_EDGE('',*,*,#17302,.F.);
#24562=ORIENTED_EDGE('',*,*,#17301,.F.);
#24563=ORIENTED_EDGE('',*,*,#17295,.F.);
#24564=ORIENTED_EDGE('',*,*,#17303,.F.);
#24565=ORIENTED_EDGE('',*,*,#17304,.T.);
#24566=ORIENTED_EDGE('',*,*,#17305,.F.);
#24567=ORIENTED_EDGE('',*,*,#17306,.F.);
#24568=ORIENTED_EDGE('',*,*,#17307,.F.);
#24569=ORIENTED_EDGE('',*,*,#17306,.T.);
#24570=ORIENTED_EDGE('',*,*,#17308,.T.);
#24571=ORIENTED_EDGE('',*,*,#17309,.F.);
#24572=ORIENTED_EDGE('',*,*,#17308,.F.);
#24573=ORIENTED_EDGE('',*,*,#17305,.T.);
#24574=ORIENTED_EDGE('',*,*,#17310,.T.);
#24575=ORIENTED_EDGE('',*,*,#17311,.F.);
#24576=ORIENTED_EDGE('',*,*,#17310,.F.);
#24577=ORIENTED_EDGE('',*,*,#17304,.F.);
#24578=ORIENTED_EDGE('',*,*,#17312,.F.);
#24579=ORIENTED_EDGE('',*,*,#17313,.T.);
#24580=ORIENTED_EDGE('',*,*,#17314,.F.);
#24581=ORIENTED_EDGE('',*,*,#17315,.F.);
#24582=ORIENTED_EDGE('',*,*,#17316,.F.);
#24583=ORIENTED_EDGE('',*,*,#17315,.T.);
#24584=ORIENTED_EDGE('',*,*,#17317,.T.);
#24585=ORIENTED_EDGE('',*,*,#17318,.F.);
#24586=ORIENTED_EDGE('',*,*,#17317,.F.);
#24587=ORIENTED_EDGE('',*,*,#17314,.T.);
#24588=ORIENTED_EDGE('',*,*,#17319,.T.);
#24589=ORIENTED_EDGE('',*,*,#17320,.F.);
#24590=ORIENTED_EDGE('',*,*,#17319,.F.);
#24591=ORIENTED_EDGE('',*,*,#17313,.F.);
#24592=ORIENTED_EDGE('',*,*,#17321,.F.);
#24593=ORIENTED_EDGE('',*,*,#17322,.T.);
#24594=ORIENTED_EDGE('',*,*,#17323,.F.);
#24595=ORIENTED_EDGE('',*,*,#17324,.F.);
#24596=ORIENTED_EDGE('',*,*,#17325,.F.);
#24597=ORIENTED_EDGE('',*,*,#17324,.T.);
#24598=ORIENTED_EDGE('',*,*,#17326,.T.);
#24599=ORIENTED_EDGE('',*,*,#17327,.F.);
#24600=ORIENTED_EDGE('',*,*,#17326,.F.);
#24601=ORIENTED_EDGE('',*,*,#17323,.T.);
#24602=ORIENTED_EDGE('',*,*,#17328,.T.);
#24603=ORIENTED_EDGE('',*,*,#17329,.F.);
#24604=ORIENTED_EDGE('',*,*,#17328,.F.);
#24605=ORIENTED_EDGE('',*,*,#17322,.F.);
#24606=ORIENTED_EDGE('',*,*,#17330,.F.);
#24607=ORIENTED_EDGE('',*,*,#17331,.T.);
#24608=ORIENTED_EDGE('',*,*,#17332,.F.);
#24609=ORIENTED_EDGE('',*,*,#17333,.F.);
#24610=ORIENTED_EDGE('',*,*,#17334,.F.);
#24611=ORIENTED_EDGE('',*,*,#17333,.T.);
#24612=ORIENTED_EDGE('',*,*,#17335,.T.);
#24613=ORIENTED_EDGE('',*,*,#17336,.F.);
#24614=ORIENTED_EDGE('',*,*,#17335,.F.);
#24615=ORIENTED_EDGE('',*,*,#17332,.T.);
#24616=ORIENTED_EDGE('',*,*,#17337,.T.);
#24617=ORIENTED_EDGE('',*,*,#17338,.F.);
#24618=ORIENTED_EDGE('',*,*,#17337,.F.);
#24619=ORIENTED_EDGE('',*,*,#17331,.F.);
#24620=ORIENTED_EDGE('',*,*,#17339,.F.);
#24621=ORIENTED_EDGE('',*,*,#17340,.T.);
#24622=ORIENTED_EDGE('',*,*,#17341,.F.);
#24623=ORIENTED_EDGE('',*,*,#17342,.F.);
#24624=ORIENTED_EDGE('',*,*,#17343,.F.);
#24625=ORIENTED_EDGE('',*,*,#17342,.T.);
#24626=ORIENTED_EDGE('',*,*,#17344,.T.);
#24627=ORIENTED_EDGE('',*,*,#17345,.F.);
#24628=ORIENTED_EDGE('',*,*,#17344,.F.);
#24629=ORIENTED_EDGE('',*,*,#17341,.T.);
#24630=ORIENTED_EDGE('',*,*,#17346,.T.);
#24631=ORIENTED_EDGE('',*,*,#17347,.F.);
#24632=ORIENTED_EDGE('',*,*,#17346,.F.);
#24633=ORIENTED_EDGE('',*,*,#17340,.F.);
#24634=ORIENTED_EDGE('',*,*,#17348,.F.);
#24635=ORIENTED_EDGE('',*,*,#17349,.T.);
#24636=ORIENTED_EDGE('',*,*,#17350,.F.);
#24637=ORIENTED_EDGE('',*,*,#17351,.F.);
#24638=ORIENTED_EDGE('',*,*,#17352,.F.);
#24639=ORIENTED_EDGE('',*,*,#17351,.T.);
#24640=ORIENTED_EDGE('',*,*,#17353,.T.);
#24641=ORIENTED_EDGE('',*,*,#17354,.F.);
#24642=ORIENTED_EDGE('',*,*,#17353,.F.);
#24643=ORIENTED_EDGE('',*,*,#17350,.T.);
#24644=ORIENTED_EDGE('',*,*,#17355,.T.);
#24645=ORIENTED_EDGE('',*,*,#17356,.F.);
#24646=ORIENTED_EDGE('',*,*,#17355,.F.);
#24647=ORIENTED_EDGE('',*,*,#17349,.F.);
#24648=ORIENTED_EDGE('',*,*,#17357,.F.);
#24649=ORIENTED_EDGE('',*,*,#17358,.T.);
#24650=ORIENTED_EDGE('',*,*,#17359,.F.);
#24651=ORIENTED_EDGE('',*,*,#17360,.F.);
#24652=ORIENTED_EDGE('',*,*,#17361,.F.);
#24653=ORIENTED_EDGE('',*,*,#17360,.T.);
#24654=ORIENTED_EDGE('',*,*,#17362,.T.);
#24655=ORIENTED_EDGE('',*,*,#17363,.F.);
#24656=ORIENTED_EDGE('',*,*,#17362,.F.);
#24657=ORIENTED_EDGE('',*,*,#17359,.T.);
#24658=ORIENTED_EDGE('',*,*,#17364,.T.);
#24659=ORIENTED_EDGE('',*,*,#17365,.F.);
#24660=ORIENTED_EDGE('',*,*,#17364,.F.);
#24661=ORIENTED_EDGE('',*,*,#17358,.F.);
#24662=ORIENTED_EDGE('',*,*,#17366,.F.);
#24663=ORIENTED_EDGE('',*,*,#17367,.T.);
#24664=ORIENTED_EDGE('',*,*,#17368,.F.);
#24665=ORIENTED_EDGE('',*,*,#17369,.F.);
#24666=ORIENTED_EDGE('',*,*,#17370,.F.);
#24667=ORIENTED_EDGE('',*,*,#17369,.T.);
#24668=ORIENTED_EDGE('',*,*,#17371,.T.);
#24669=ORIENTED_EDGE('',*,*,#17372,.F.);
#24670=ORIENTED_EDGE('',*,*,#17371,.F.);
#24671=ORIENTED_EDGE('',*,*,#17368,.T.);
#24672=ORIENTED_EDGE('',*,*,#17373,.T.);
#24673=ORIENTED_EDGE('',*,*,#17374,.F.);
#24674=ORIENTED_EDGE('',*,*,#17373,.F.);
#24675=ORIENTED_EDGE('',*,*,#17367,.F.);
#24676=ORIENTED_EDGE('',*,*,#17375,.F.);
#24677=ORIENTED_EDGE('',*,*,#17376,.T.);
#24678=ORIENTED_EDGE('',*,*,#17377,.F.);
#24679=ORIENTED_EDGE('',*,*,#17378,.F.);
#24680=ORIENTED_EDGE('',*,*,#17379,.F.);
#24681=ORIENTED_EDGE('',*,*,#17378,.T.);
#24682=ORIENTED_EDGE('',*,*,#17380,.T.);
#24683=ORIENTED_EDGE('',*,*,#17381,.F.);
#24684=ORIENTED_EDGE('',*,*,#17380,.F.);
#24685=ORIENTED_EDGE('',*,*,#17377,.T.);
#24686=ORIENTED_EDGE('',*,*,#17382,.T.);
#24687=ORIENTED_EDGE('',*,*,#17383,.F.);
#24688=ORIENTED_EDGE('',*,*,#17382,.F.);
#24689=ORIENTED_EDGE('',*,*,#17376,.F.);
#24690=ORIENTED_EDGE('',*,*,#17384,.F.);
#24691=ORIENTED_EDGE('',*,*,#17385,.T.);
#24692=ORIENTED_EDGE('',*,*,#17386,.F.);
#24693=ORIENTED_EDGE('',*,*,#17387,.F.);
#24694=ORIENTED_EDGE('',*,*,#17388,.F.);
#24695=ORIENTED_EDGE('',*,*,#17387,.T.);
#24696=ORIENTED_EDGE('',*,*,#17389,.T.);
#24697=ORIENTED_EDGE('',*,*,#17390,.F.);
#24698=ORIENTED_EDGE('',*,*,#17389,.F.);
#24699=ORIENTED_EDGE('',*,*,#17386,.T.);
#24700=ORIENTED_EDGE('',*,*,#17391,.T.);
#24701=ORIENTED_EDGE('',*,*,#17392,.F.);
#24702=ORIENTED_EDGE('',*,*,#17391,.F.);
#24703=ORIENTED_EDGE('',*,*,#17385,.F.);
#24704=ORIENTED_EDGE('',*,*,#17393,.F.);
#24705=ORIENTED_EDGE('',*,*,#17394,.T.);
#24706=ORIENTED_EDGE('',*,*,#17395,.F.);
#24707=ORIENTED_EDGE('',*,*,#17396,.F.);
#24708=ORIENTED_EDGE('',*,*,#17397,.F.);
#24709=ORIENTED_EDGE('',*,*,#17396,.T.);
#24710=ORIENTED_EDGE('',*,*,#17398,.T.);
#24711=ORIENTED_EDGE('',*,*,#17399,.F.);
#24712=ORIENTED_EDGE('',*,*,#17398,.F.);
#24713=ORIENTED_EDGE('',*,*,#17395,.T.);
#24714=ORIENTED_EDGE('',*,*,#17400,.T.);
#24715=ORIENTED_EDGE('',*,*,#17401,.F.);
#24716=ORIENTED_EDGE('',*,*,#17400,.F.);
#24717=ORIENTED_EDGE('',*,*,#17394,.F.);
#24718=ORIENTED_EDGE('',*,*,#17402,.F.);
#24719=ORIENTED_EDGE('',*,*,#17403,.T.);
#24720=ORIENTED_EDGE('',*,*,#17404,.F.);
#24721=ORIENTED_EDGE('',*,*,#17405,.F.);
#24722=ORIENTED_EDGE('',*,*,#17406,.F.);
#24723=ORIENTED_EDGE('',*,*,#17405,.T.);
#24724=ORIENTED_EDGE('',*,*,#17407,.T.);
#24725=ORIENTED_EDGE('',*,*,#17408,.F.);
#24726=ORIENTED_EDGE('',*,*,#17409,.F.);
#24727=ORIENTED_EDGE('',*,*,#17407,.F.);
#24728=ORIENTED_EDGE('',*,*,#17404,.T.);
#24729=ORIENTED_EDGE('',*,*,#17410,.T.);
#24730=ORIENTED_EDGE('',*,*,#17411,.F.);
#24731=ORIENTED_EDGE('',*,*,#17410,.F.);
#24732=ORIENTED_EDGE('',*,*,#17403,.F.);
#24733=ORIENTED_EDGE('',*,*,#17412,.F.);
#24734=ORIENTED_EDGE('',*,*,#17413,.F.);
#24735=ORIENTED_EDGE('',*,*,#17414,.T.);
#24736=ORIENTED_EDGE('',*,*,#17415,.F.);
#24737=ORIENTED_EDGE('',*,*,#17416,.F.);
#24738=ORIENTED_EDGE('',*,*,#17417,.F.);
#24739=ORIENTED_EDGE('',*,*,#17416,.T.);
#24740=ORIENTED_EDGE('',*,*,#17418,.T.);
#24741=ORIENTED_EDGE('',*,*,#17419,.F.);
#24742=ORIENTED_EDGE('',*,*,#17418,.F.);
#24743=ORIENTED_EDGE('',*,*,#17415,.T.);
#24744=ORIENTED_EDGE('',*,*,#17420,.T.);
#24745=ORIENTED_EDGE('',*,*,#17421,.F.);
#24746=ORIENTED_EDGE('',*,*,#17420,.F.);
#24747=ORIENTED_EDGE('',*,*,#17414,.F.);
#24748=ORIENTED_EDGE('',*,*,#17422,.F.);
#24749=ORIENTED_EDGE('',*,*,#17423,.T.);
#24750=ORIENTED_EDGE('',*,*,#17424,.F.);
#24751=ORIENTED_EDGE('',*,*,#17425,.F.);
#24752=ORIENTED_EDGE('',*,*,#17426,.F.);
#24753=ORIENTED_EDGE('',*,*,#17425,.T.);
#24754=ORIENTED_EDGE('',*,*,#17427,.T.);
#24755=ORIENTED_EDGE('',*,*,#17428,.F.);
#24756=ORIENTED_EDGE('',*,*,#17427,.F.);
#24757=ORIENTED_EDGE('',*,*,#17424,.T.);
#24758=ORIENTED_EDGE('',*,*,#17429,.T.);
#24759=ORIENTED_EDGE('',*,*,#17430,.F.);
#24760=ORIENTED_EDGE('',*,*,#17429,.F.);
#24761=ORIENTED_EDGE('',*,*,#17423,.F.);
#24762=ORIENTED_EDGE('',*,*,#17431,.F.);
#24763=ORIENTED_EDGE('',*,*,#17432,.T.);
#24764=ORIENTED_EDGE('',*,*,#17433,.F.);
#24765=ORIENTED_EDGE('',*,*,#17434,.F.);
#24766=ORIENTED_EDGE('',*,*,#17435,.F.);
#24767=ORIENTED_EDGE('',*,*,#17434,.T.);
#24768=ORIENTED_EDGE('',*,*,#17436,.T.);
#24769=ORIENTED_EDGE('',*,*,#17437,.F.);
#24770=ORIENTED_EDGE('',*,*,#17436,.F.);
#24771=ORIENTED_EDGE('',*,*,#17433,.T.);
#24772=ORIENTED_EDGE('',*,*,#17438,.T.);
#24773=ORIENTED_EDGE('',*,*,#17439,.F.);
#24774=ORIENTED_EDGE('',*,*,#17438,.F.);
#24775=ORIENTED_EDGE('',*,*,#17432,.F.);
#24776=ORIENTED_EDGE('',*,*,#17440,.F.);
#24777=ORIENTED_EDGE('',*,*,#17441,.T.);
#24778=ORIENTED_EDGE('',*,*,#17442,.F.);
#24779=ORIENTED_EDGE('',*,*,#17443,.F.);
#24780=ORIENTED_EDGE('',*,*,#17444,.F.);
#24781=ORIENTED_EDGE('',*,*,#17443,.T.);
#24782=ORIENTED_EDGE('',*,*,#17445,.T.);
#24783=ORIENTED_EDGE('',*,*,#17446,.F.);
#24784=ORIENTED_EDGE('',*,*,#17445,.F.);
#24785=ORIENTED_EDGE('',*,*,#17442,.T.);
#24786=ORIENTED_EDGE('',*,*,#17447,.T.);
#24787=ORIENTED_EDGE('',*,*,#17448,.F.);
#24788=ORIENTED_EDGE('',*,*,#17447,.F.);
#24789=ORIENTED_EDGE('',*,*,#17441,.F.);
#24790=ORIENTED_EDGE('',*,*,#17449,.F.);
#24791=ORIENTED_EDGE('',*,*,#17450,.T.);
#24792=ORIENTED_EDGE('',*,*,#17451,.F.);
#24793=ORIENTED_EDGE('',*,*,#17452,.F.);
#24794=ORIENTED_EDGE('',*,*,#17453,.F.);
#24795=ORIENTED_EDGE('',*,*,#17452,.T.);
#24796=ORIENTED_EDGE('',*,*,#17454,.T.);
#24797=ORIENTED_EDGE('',*,*,#17455,.F.);
#24798=ORIENTED_EDGE('',*,*,#17454,.F.);
#24799=ORIENTED_EDGE('',*,*,#17451,.T.);
#24800=ORIENTED_EDGE('',*,*,#17456,.T.);
#24801=ORIENTED_EDGE('',*,*,#17457,.F.);
#24802=ORIENTED_EDGE('',*,*,#17456,.F.);
#24803=ORIENTED_EDGE('',*,*,#17450,.F.);
#24804=ORIENTED_EDGE('',*,*,#17458,.F.);
#24805=ORIENTED_EDGE('',*,*,#17459,.T.);
#24806=ORIENTED_EDGE('',*,*,#17460,.F.);
#24807=ORIENTED_EDGE('',*,*,#17461,.F.);
#24808=ORIENTED_EDGE('',*,*,#17462,.F.);
#24809=ORIENTED_EDGE('',*,*,#17461,.T.);
#24810=ORIENTED_EDGE('',*,*,#17463,.T.);
#24811=ORIENTED_EDGE('',*,*,#17464,.F.);
#24812=ORIENTED_EDGE('',*,*,#17463,.F.);
#24813=ORIENTED_EDGE('',*,*,#17460,.T.);
#24814=ORIENTED_EDGE('',*,*,#17465,.T.);
#24815=ORIENTED_EDGE('',*,*,#17466,.F.);
#24816=ORIENTED_EDGE('',*,*,#17465,.F.);
#24817=ORIENTED_EDGE('',*,*,#17459,.F.);
#24818=ORIENTED_EDGE('',*,*,#17467,.F.);
#24819=ORIENTED_EDGE('',*,*,#17468,.T.);
#24820=ORIENTED_EDGE('',*,*,#17469,.F.);
#24821=ORIENTED_EDGE('',*,*,#17470,.F.);
#24822=ORIENTED_EDGE('',*,*,#17471,.F.);
#24823=ORIENTED_EDGE('',*,*,#17470,.T.);
#24824=ORIENTED_EDGE('',*,*,#17472,.T.);
#24825=ORIENTED_EDGE('',*,*,#17473,.F.);
#24826=ORIENTED_EDGE('',*,*,#17472,.F.);
#24827=ORIENTED_EDGE('',*,*,#17469,.T.);
#24828=ORIENTED_EDGE('',*,*,#17474,.T.);
#24829=ORIENTED_EDGE('',*,*,#17475,.F.);
#24830=ORIENTED_EDGE('',*,*,#17474,.F.);
#24831=ORIENTED_EDGE('',*,*,#17468,.F.);
#24832=ORIENTED_EDGE('',*,*,#17476,.F.);
#24833=ORIENTED_EDGE('',*,*,#17477,.T.);
#24834=ORIENTED_EDGE('',*,*,#17478,.F.);
#24835=ORIENTED_EDGE('',*,*,#17479,.F.);
#24836=ORIENTED_EDGE('',*,*,#17480,.F.);
#24837=ORIENTED_EDGE('',*,*,#17479,.T.);
#24838=ORIENTED_EDGE('',*,*,#17481,.T.);
#24839=ORIENTED_EDGE('',*,*,#17482,.F.);
#24840=ORIENTED_EDGE('',*,*,#17481,.F.);
#24841=ORIENTED_EDGE('',*,*,#17478,.T.);
#24842=ORIENTED_EDGE('',*,*,#17483,.T.);
#24843=ORIENTED_EDGE('',*,*,#17484,.F.);
#24844=ORIENTED_EDGE('',*,*,#17483,.F.);
#24845=ORIENTED_EDGE('',*,*,#17477,.F.);
#24846=ORIENTED_EDGE('',*,*,#17485,.F.);
#24847=ORIENTED_EDGE('',*,*,#17486,.T.);
#24848=ORIENTED_EDGE('',*,*,#17487,.F.);
#24849=ORIENTED_EDGE('',*,*,#17488,.F.);
#24850=ORIENTED_EDGE('',*,*,#17489,.F.);
#24851=ORIENTED_EDGE('',*,*,#17488,.T.);
#24852=ORIENTED_EDGE('',*,*,#17490,.T.);
#24853=ORIENTED_EDGE('',*,*,#17491,.F.);
#24854=ORIENTED_EDGE('',*,*,#17490,.F.);
#24855=ORIENTED_EDGE('',*,*,#17487,.T.);
#24856=ORIENTED_EDGE('',*,*,#17492,.T.);
#24857=ORIENTED_EDGE('',*,*,#17493,.F.);
#24858=ORIENTED_EDGE('',*,*,#17492,.F.);
#24859=ORIENTED_EDGE('',*,*,#17486,.F.);
#24860=ORIENTED_EDGE('',*,*,#17494,.F.);
#24861=ORIENTED_EDGE('',*,*,#17495,.T.);
#24862=ORIENTED_EDGE('',*,*,#17496,.F.);
#24863=ORIENTED_EDGE('',*,*,#17497,.F.);
#24864=ORIENTED_EDGE('',*,*,#17498,.F.);
#24865=ORIENTED_EDGE('',*,*,#17497,.T.);
#24866=ORIENTED_EDGE('',*,*,#17499,.T.);
#24867=ORIENTED_EDGE('',*,*,#17500,.F.);
#24868=ORIENTED_EDGE('',*,*,#17499,.F.);
#24869=ORIENTED_EDGE('',*,*,#17496,.T.);
#24870=ORIENTED_EDGE('',*,*,#17501,.T.);
#24871=ORIENTED_EDGE('',*,*,#17502,.F.);
#24872=ORIENTED_EDGE('',*,*,#17501,.F.);
#24873=ORIENTED_EDGE('',*,*,#17495,.F.);
#24874=ORIENTED_EDGE('',*,*,#17503,.F.);
#24875=ORIENTED_EDGE('',*,*,#17504,.T.);
#24876=ORIENTED_EDGE('',*,*,#17505,.F.);
#24877=ORIENTED_EDGE('',*,*,#17506,.F.);
#24878=ORIENTED_EDGE('',*,*,#17507,.F.);
#24879=ORIENTED_EDGE('',*,*,#17506,.T.);
#24880=ORIENTED_EDGE('',*,*,#17508,.T.);
#24881=ORIENTED_EDGE('',*,*,#17509,.F.);
#24882=ORIENTED_EDGE('',*,*,#17508,.F.);
#24883=ORIENTED_EDGE('',*,*,#17505,.T.);
#24884=ORIENTED_EDGE('',*,*,#17510,.T.);
#24885=ORIENTED_EDGE('',*,*,#17511,.F.);
#24886=ORIENTED_EDGE('',*,*,#17510,.F.);
#24887=ORIENTED_EDGE('',*,*,#17504,.F.);
#24888=ORIENTED_EDGE('',*,*,#17512,.F.);
#24889=ORIENTED_EDGE('',*,*,#17513,.T.);
#24890=ORIENTED_EDGE('',*,*,#17514,.F.);
#24891=ORIENTED_EDGE('',*,*,#17515,.F.);
#24892=ORIENTED_EDGE('',*,*,#17516,.F.);
#24893=ORIENTED_EDGE('',*,*,#17515,.T.);
#24894=ORIENTED_EDGE('',*,*,#17517,.T.);
#24895=ORIENTED_EDGE('',*,*,#17518,.F.);
#24896=ORIENTED_EDGE('',*,*,#17517,.F.);
#24897=ORIENTED_EDGE('',*,*,#17514,.T.);
#24898=ORIENTED_EDGE('',*,*,#17519,.T.);
#24899=ORIENTED_EDGE('',*,*,#17520,.F.);
#24900=ORIENTED_EDGE('',*,*,#17519,.F.);
#24901=ORIENTED_EDGE('',*,*,#17513,.F.);
#24902=ORIENTED_EDGE('',*,*,#17521,.F.);
#24903=ORIENTED_EDGE('',*,*,#17522,.T.);
#24904=ORIENTED_EDGE('',*,*,#17523,.F.);
#24905=ORIENTED_EDGE('',*,*,#17524,.F.);
#24906=ORIENTED_EDGE('',*,*,#17525,.F.);
#24907=ORIENTED_EDGE('',*,*,#17524,.T.);
#24908=ORIENTED_EDGE('',*,*,#17526,.T.);
#24909=ORIENTED_EDGE('',*,*,#17527,.F.);
#24910=ORIENTED_EDGE('',*,*,#17526,.F.);
#24911=ORIENTED_EDGE('',*,*,#17523,.T.);
#24912=ORIENTED_EDGE('',*,*,#17528,.T.);
#24913=ORIENTED_EDGE('',*,*,#17529,.F.);
#24914=ORIENTED_EDGE('',*,*,#17528,.F.);
#24915=ORIENTED_EDGE('',*,*,#17522,.F.);
#24916=ORIENTED_EDGE('',*,*,#17530,.F.);
#24917=ORIENTED_EDGE('',*,*,#17531,.T.);
#24918=ORIENTED_EDGE('',*,*,#17532,.F.);
#24919=ORIENTED_EDGE('',*,*,#17533,.F.);
#24920=ORIENTED_EDGE('',*,*,#17534,.F.);
#24921=ORIENTED_EDGE('',*,*,#17533,.T.);
#24922=ORIENTED_EDGE('',*,*,#17535,.T.);
#24923=ORIENTED_EDGE('',*,*,#17536,.F.);
#24924=ORIENTED_EDGE('',*,*,#17535,.F.);
#24925=ORIENTED_EDGE('',*,*,#17532,.T.);
#24926=ORIENTED_EDGE('',*,*,#17537,.T.);
#24927=ORIENTED_EDGE('',*,*,#17538,.F.);
#24928=ORIENTED_EDGE('',*,*,#17537,.F.);
#24929=ORIENTED_EDGE('',*,*,#17531,.F.);
#24930=ORIENTED_EDGE('',*,*,#17539,.F.);
#24931=ORIENTED_EDGE('',*,*,#17540,.T.);
#24932=ORIENTED_EDGE('',*,*,#17541,.F.);
#24933=ORIENTED_EDGE('',*,*,#17542,.F.);
#24934=ORIENTED_EDGE('',*,*,#17543,.F.);
#24935=ORIENTED_EDGE('',*,*,#17542,.T.);
#24936=ORIENTED_EDGE('',*,*,#17544,.T.);
#24937=ORIENTED_EDGE('',*,*,#17545,.F.);
#24938=ORIENTED_EDGE('',*,*,#17544,.F.);
#24939=ORIENTED_EDGE('',*,*,#17541,.T.);
#24940=ORIENTED_EDGE('',*,*,#17546,.T.);
#24941=ORIENTED_EDGE('',*,*,#17547,.F.);
#24942=ORIENTED_EDGE('',*,*,#17546,.F.);
#24943=ORIENTED_EDGE('',*,*,#17540,.F.);
#24944=ORIENTED_EDGE('',*,*,#17548,.F.);
#24945=ORIENTED_EDGE('',*,*,#17549,.T.);
#24946=ORIENTED_EDGE('',*,*,#17550,.F.);
#24947=ORIENTED_EDGE('',*,*,#17551,.F.);
#24948=ORIENTED_EDGE('',*,*,#17552,.F.);
#24949=ORIENTED_EDGE('',*,*,#17551,.T.);
#24950=ORIENTED_EDGE('',*,*,#17553,.T.);
#24951=ORIENTED_EDGE('',*,*,#17554,.F.);
#24952=ORIENTED_EDGE('',*,*,#17553,.F.);
#24953=ORIENTED_EDGE('',*,*,#17550,.T.);
#24954=ORIENTED_EDGE('',*,*,#17555,.T.);
#24955=ORIENTED_EDGE('',*,*,#17556,.F.);
#24956=ORIENTED_EDGE('',*,*,#17555,.F.);
#24957=ORIENTED_EDGE('',*,*,#17549,.F.);
#24958=ORIENTED_EDGE('',*,*,#17557,.F.);
#24959=ORIENTED_EDGE('',*,*,#17558,.T.);
#24960=ORIENTED_EDGE('',*,*,#17559,.F.);
#24961=ORIENTED_EDGE('',*,*,#17560,.F.);
#24962=ORIENTED_EDGE('',*,*,#17561,.F.);
#24963=ORIENTED_EDGE('',*,*,#17560,.T.);
#24964=ORIENTED_EDGE('',*,*,#17562,.T.);
#24965=ORIENTED_EDGE('',*,*,#17563,.F.);
#24966=ORIENTED_EDGE('',*,*,#17562,.F.);
#24967=ORIENTED_EDGE('',*,*,#17559,.T.);
#24968=ORIENTED_EDGE('',*,*,#17564,.T.);
#24969=ORIENTED_EDGE('',*,*,#17565,.F.);
#24970=ORIENTED_EDGE('',*,*,#17564,.F.);
#24971=ORIENTED_EDGE('',*,*,#17558,.F.);
#24972=ORIENTED_EDGE('',*,*,#17566,.F.);
#24973=ORIENTED_EDGE('',*,*,#17567,.T.);
#24974=ORIENTED_EDGE('',*,*,#17568,.F.);
#24975=ORIENTED_EDGE('',*,*,#17569,.F.);
#24976=ORIENTED_EDGE('',*,*,#17570,.F.);
#24977=ORIENTED_EDGE('',*,*,#17569,.T.);
#24978=ORIENTED_EDGE('',*,*,#17571,.T.);
#24979=ORIENTED_EDGE('',*,*,#17572,.F.);
#24980=ORIENTED_EDGE('',*,*,#17571,.F.);
#24981=ORIENTED_EDGE('',*,*,#17568,.T.);
#24982=ORIENTED_EDGE('',*,*,#17573,.T.);
#24983=ORIENTED_EDGE('',*,*,#17574,.F.);
#24984=ORIENTED_EDGE('',*,*,#17573,.F.);
#24985=ORIENTED_EDGE('',*,*,#17567,.F.);
#24986=ORIENTED_EDGE('',*,*,#17575,.F.);
#24987=ORIENTED_EDGE('',*,*,#17576,.T.);
#24988=ORIENTED_EDGE('',*,*,#17577,.T.);
#24989=ORIENTED_EDGE('',*,*,#17578,.F.);
#24990=ORIENTED_EDGE('',*,*,#17579,.F.);
#24991=ORIENTED_EDGE('',*,*,#17580,.T.);
#24992=ORIENTED_EDGE('',*,*,#17581,.T.);
#24993=ORIENTED_EDGE('',*,*,#17576,.F.);
#24994=ORIENTED_EDGE('',*,*,#17582,.F.);
#24995=ORIENTED_EDGE('',*,*,#17583,.T.);
#24996=ORIENTED_EDGE('',*,*,#17584,.T.);
#24997=ORIENTED_EDGE('',*,*,#17580,.F.);
#24998=ORIENTED_EDGE('',*,*,#17585,.F.);
#24999=ORIENTED_EDGE('',*,*,#17586,.T.);
#25000=ORIENTED_EDGE('',*,*,#17587,.T.);
#25001=ORIENTED_EDGE('',*,*,#17583,.F.);
#25002=ORIENTED_EDGE('',*,*,#17588,.F.);
#25003=ORIENTED_EDGE('',*,*,#17589,.T.);
#25004=ORIENTED_EDGE('',*,*,#17590,.T.);
#25005=ORIENTED_EDGE('',*,*,#17586,.F.);
#25006=ORIENTED_EDGE('',*,*,#17591,.F.);
#25007=ORIENTED_EDGE('',*,*,#17578,.T.);
#25008=ORIENTED_EDGE('',*,*,#17592,.T.);
#25009=ORIENTED_EDGE('',*,*,#17589,.F.);
#25010=ORIENTED_EDGE('',*,*,#17592,.F.);
#25011=ORIENTED_EDGE('',*,*,#17577,.F.);
#25012=ORIENTED_EDGE('',*,*,#17581,.F.);
#25013=ORIENTED_EDGE('',*,*,#17584,.F.);
#25014=ORIENTED_EDGE('',*,*,#17587,.F.);
#25015=ORIENTED_EDGE('',*,*,#17590,.F.);
#25016=ORIENTED_EDGE('',*,*,#17593,.F.);
#25017=ORIENTED_EDGE('',*,*,#17242,.F.);
#25018=ORIENTED_EDGE('',*,*,#17118,.F.);
#25019=ORIENTED_EDGE('',*,*,#17243,.F.);
#25020=ORIENTED_EDGE('',*,*,#17594,.T.);
#25021=ORIENTED_EDGE('',*,*,#17593,.T.);
#25022=ORIENTED_EDGE('',*,*,#17594,.F.);
#25023=ORIENTED_EDGE('',*,*,#17174,.T.);
#25024=ORIENTED_EDGE('',*,*,#17239,.T.);
#25025=ORIENTED_EDGE('',*,*,#17595,.F.);
#25026=ORIENTED_EDGE('',*,*,#17248,.T.);
#25027=ORIENTED_EDGE('',*,*,#17596,.F.);
#25028=ORIENTED_EDGE('',*,*,#17595,.T.);
#25029=ORIENTED_EDGE('',*,*,#17238,.T.);
#25030=ORIENTED_EDGE('',*,*,#17182,.T.);
#25031=ORIENTED_EDGE('',*,*,#17179,.T.);
#25032=ORIENTED_EDGE('',*,*,#17247,.T.);
#25033=ORIENTED_EDGE('',*,*,#17597,.F.);
#25034=ORIENTED_EDGE('',*,*,#17598,.T.);
#25035=ORIENTED_EDGE('',*,*,#17412,.T.);
#25036=ORIENTED_EDGE('',*,*,#17402,.T.);
#25037=ORIENTED_EDGE('',*,*,#17406,.T.);
#25038=ORIENTED_EDGE('',*,*,#17599,.T.);
#25039=ORIENTED_EDGE('',*,*,#17596,.T.);
#25040=ORIENTED_EDGE('',*,*,#17599,.F.);
#25041=ORIENTED_EDGE('',*,*,#17408,.T.);
#25042=ORIENTED_EDGE('',*,*,#17409,.T.);
#25043=ORIENTED_EDGE('',*,*,#17411,.T.);
#25044=ORIENTED_EDGE('',*,*,#17598,.F.);
#25045=ORIENTED_EDGE('',*,*,#17255,.T.);
#25046=ORIENTED_EDGE('',*,*,#17257,.T.);
#25047=ORIENTED_EDGE('',*,*,#17249,.T.);
#25048=ORIENTED_EDGE('',*,*,#17253,.T.);
#25049=ORIENTED_EDGE('',*,*,#17264,.T.);
#25050=ORIENTED_EDGE('',*,*,#17266,.T.);
#25051=ORIENTED_EDGE('',*,*,#17258,.T.);
#25052=ORIENTED_EDGE('',*,*,#17262,.T.);
#25053=ORIENTED_EDGE('',*,*,#17273,.T.);
#25054=ORIENTED_EDGE('',*,*,#17275,.T.);
#25055=ORIENTED_EDGE('',*,*,#17267,.T.);
#25056=ORIENTED_EDGE('',*,*,#17271,.T.);
#25057=ORIENTED_EDGE('',*,*,#17282,.T.);
#25058=ORIENTED_EDGE('',*,*,#17284,.T.);
#25059=ORIENTED_EDGE('',*,*,#17276,.T.);
#25060=ORIENTED_EDGE('',*,*,#17280,.T.);
#25061=ORIENTED_EDGE('',*,*,#17291,.T.);
#25062=ORIENTED_EDGE('',*,*,#17293,.T.);
#25063=ORIENTED_EDGE('',*,*,#17285,.T.);
#25064=ORIENTED_EDGE('',*,*,#17289,.T.);
#25065=ORIENTED_EDGE('',*,*,#17300,.T.);
#25066=ORIENTED_EDGE('',*,*,#17302,.T.);
#25067=ORIENTED_EDGE('',*,*,#17294,.T.);
#25068=ORIENTED_EDGE('',*,*,#17298,.T.);
#25069=ORIENTED_EDGE('',*,*,#17309,.T.);
#25070=ORIENTED_EDGE('',*,*,#17311,.T.);
#25071=ORIENTED_EDGE('',*,*,#17303,.T.);
#25072=ORIENTED_EDGE('',*,*,#17307,.T.);
#25073=ORIENTED_EDGE('',*,*,#17318,.T.);
#25074=ORIENTED_EDGE('',*,*,#17320,.T.);
#25075=ORIENTED_EDGE('',*,*,#17312,.T.);
#25076=ORIENTED_EDGE('',*,*,#17316,.T.);
#25077=ORIENTED_EDGE('',*,*,#17327,.T.);
#25078=ORIENTED_EDGE('',*,*,#17329,.T.);
#25079=ORIENTED_EDGE('',*,*,#17321,.T.);
#25080=ORIENTED_EDGE('',*,*,#17325,.T.);
#25081=ORIENTED_EDGE('',*,*,#17336,.T.);
#25082=ORIENTED_EDGE('',*,*,#17338,.T.);
#25083=ORIENTED_EDGE('',*,*,#17330,.T.);
#25084=ORIENTED_EDGE('',*,*,#17334,.T.);
#25085=ORIENTED_EDGE('',*,*,#17345,.T.);
#25086=ORIENTED_EDGE('',*,*,#17347,.T.);
#25087=ORIENTED_EDGE('',*,*,#17339,.T.);
#25088=ORIENTED_EDGE('',*,*,#17343,.T.);
#25089=ORIENTED_EDGE('',*,*,#17354,.T.);
#25090=ORIENTED_EDGE('',*,*,#17356,.T.);
#25091=ORIENTED_EDGE('',*,*,#17348,.T.);
#25092=ORIENTED_EDGE('',*,*,#17352,.T.);
#25093=ORIENTED_EDGE('',*,*,#17363,.T.);
#25094=ORIENTED_EDGE('',*,*,#17365,.T.);
#25095=ORIENTED_EDGE('',*,*,#17357,.T.);
#25096=ORIENTED_EDGE('',*,*,#17361,.T.);
#25097=ORIENTED_EDGE('',*,*,#17372,.T.);
#25098=ORIENTED_EDGE('',*,*,#17374,.T.);
#25099=ORIENTED_EDGE('',*,*,#17366,.T.);
#25100=ORIENTED_EDGE('',*,*,#17370,.T.);
#25101=ORIENTED_EDGE('',*,*,#17381,.T.);
#25102=ORIENTED_EDGE('',*,*,#17383,.T.);
#25103=ORIENTED_EDGE('',*,*,#17375,.T.);
#25104=ORIENTED_EDGE('',*,*,#17379,.T.);
#25105=ORIENTED_EDGE('',*,*,#17390,.T.);
#25106=ORIENTED_EDGE('',*,*,#17392,.T.);
#25107=ORIENTED_EDGE('',*,*,#17384,.T.);
#25108=ORIENTED_EDGE('',*,*,#17388,.T.);
#25109=ORIENTED_EDGE('',*,*,#17399,.T.);
#25110=ORIENTED_EDGE('',*,*,#17401,.T.);
#25111=ORIENTED_EDGE('',*,*,#17393,.T.);
#25112=ORIENTED_EDGE('',*,*,#17397,.T.);
#25113=ORIENTED_EDGE('',*,*,#17419,.T.);
#25114=ORIENTED_EDGE('',*,*,#17421,.T.);
#25115=ORIENTED_EDGE('',*,*,#17413,.T.);
#25116=ORIENTED_EDGE('',*,*,#17417,.T.);
#25117=ORIENTED_EDGE('',*,*,#17428,.T.);
#25118=ORIENTED_EDGE('',*,*,#17430,.T.);
#25119=ORIENTED_EDGE('',*,*,#17422,.T.);
#25120=ORIENTED_EDGE('',*,*,#17426,.T.);
#25121=ORIENTED_EDGE('',*,*,#17437,.T.);
#25122=ORIENTED_EDGE('',*,*,#17439,.T.);
#25123=ORIENTED_EDGE('',*,*,#17431,.T.);
#25124=ORIENTED_EDGE('',*,*,#17435,.T.);
#25125=ORIENTED_EDGE('',*,*,#17446,.T.);
#25126=ORIENTED_EDGE('',*,*,#17448,.T.);
#25127=ORIENTED_EDGE('',*,*,#17440,.T.);
#25128=ORIENTED_EDGE('',*,*,#17444,.T.);
#25129=ORIENTED_EDGE('',*,*,#17455,.T.);
#25130=ORIENTED_EDGE('',*,*,#17457,.T.);
#25131=ORIENTED_EDGE('',*,*,#17449,.T.);
#25132=ORIENTED_EDGE('',*,*,#17453,.T.);
#25133=ORIENTED_EDGE('',*,*,#17464,.T.);
#25134=ORIENTED_EDGE('',*,*,#17466,.T.);
#25135=ORIENTED_EDGE('',*,*,#17458,.T.);
#25136=ORIENTED_EDGE('',*,*,#17462,.T.);
#25137=ORIENTED_EDGE('',*,*,#17473,.T.);
#25138=ORIENTED_EDGE('',*,*,#17475,.T.);
#25139=ORIENTED_EDGE('',*,*,#17467,.T.);
#25140=ORIENTED_EDGE('',*,*,#17471,.T.);
#25141=ORIENTED_EDGE('',*,*,#17482,.T.);
#25142=ORIENTED_EDGE('',*,*,#17484,.T.);
#25143=ORIENTED_EDGE('',*,*,#17476,.T.);
#25144=ORIENTED_EDGE('',*,*,#17480,.T.);
#25145=ORIENTED_EDGE('',*,*,#17491,.T.);
#25146=ORIENTED_EDGE('',*,*,#17493,.T.);
#25147=ORIENTED_EDGE('',*,*,#17485,.T.);
#25148=ORIENTED_EDGE('',*,*,#17489,.T.);
#25149=ORIENTED_EDGE('',*,*,#17500,.T.);
#25150=ORIENTED_EDGE('',*,*,#17502,.T.);
#25151=ORIENTED_EDGE('',*,*,#17494,.T.);
#25152=ORIENTED_EDGE('',*,*,#17498,.T.);
#25153=ORIENTED_EDGE('',*,*,#17509,.T.);
#25154=ORIENTED_EDGE('',*,*,#17511,.T.);
#25155=ORIENTED_EDGE('',*,*,#17503,.T.);
#25156=ORIENTED_EDGE('',*,*,#17507,.T.);
#25157=ORIENTED_EDGE('',*,*,#17518,.T.);
#25158=ORIENTED_EDGE('',*,*,#17520,.T.);
#25159=ORIENTED_EDGE('',*,*,#17512,.T.);
#25160=ORIENTED_EDGE('',*,*,#17516,.T.);
#25161=ORIENTED_EDGE('',*,*,#17527,.T.);
#25162=ORIENTED_EDGE('',*,*,#17529,.T.);
#25163=ORIENTED_EDGE('',*,*,#17521,.T.);
#25164=ORIENTED_EDGE('',*,*,#17525,.T.);
#25165=ORIENTED_EDGE('',*,*,#17536,.T.);
#25166=ORIENTED_EDGE('',*,*,#17538,.T.);
#25167=ORIENTED_EDGE('',*,*,#17530,.T.);
#25168=ORIENTED_EDGE('',*,*,#17534,.T.);
#25169=ORIENTED_EDGE('',*,*,#17545,.T.);
#25170=ORIENTED_EDGE('',*,*,#17547,.T.);
#25171=ORIENTED_EDGE('',*,*,#17539,.T.);
#25172=ORIENTED_EDGE('',*,*,#17543,.T.);
#25173=ORIENTED_EDGE('',*,*,#17554,.T.);
#25174=ORIENTED_EDGE('',*,*,#17556,.T.);
#25175=ORIENTED_EDGE('',*,*,#17548,.T.);
#25176=ORIENTED_EDGE('',*,*,#17552,.T.);
#25177=ORIENTED_EDGE('',*,*,#17563,.T.);
#25178=ORIENTED_EDGE('',*,*,#17565,.T.);
#25179=ORIENTED_EDGE('',*,*,#17557,.T.);
#25180=ORIENTED_EDGE('',*,*,#17561,.T.);
#25181=ORIENTED_EDGE('',*,*,#17572,.T.);
#25182=ORIENTED_EDGE('',*,*,#17574,.T.);
#25183=ORIENTED_EDGE('',*,*,#17566,.T.);
#25184=ORIENTED_EDGE('',*,*,#17570,.T.);
#25185=ORIENTED_EDGE('',*,*,#17600,.F.);
#25186=ORIENTED_EDGE('',*,*,#17601,.T.);
#25187=ORIENTED_EDGE('',*,*,#17597,.T.);
#25188=ORIENTED_EDGE('',*,*,#17601,.F.);
#25189=ORIENTED_EDGE('',*,*,#17600,.T.);
#25190=ORIENTED_EDGE('',*,*,#17575,.T.);
#25191=ORIENTED_EDGE('',*,*,#17591,.T.);
#25192=ORIENTED_EDGE('',*,*,#17588,.T.);
#25193=ORIENTED_EDGE('',*,*,#17585,.T.);
#25194=ORIENTED_EDGE('',*,*,#17582,.T.);
#25195=ORIENTED_EDGE('',*,*,#17579,.T.);
#26936=ADVANCED_FACE('',(#8112),#6756,.T.);
#26937=ADVANCED_FACE('',(#8113),#6757,.T.);
#26938=ADVANCED_FACE('',(#8114),#6758,.T.);
#26939=ADVANCED_FACE('',(#8115),#6759,.T.);
#26940=ADVANCED_FACE('',(#8116),#6760,.T.);
#26941=ADVANCED_FACE('',(#8117),#6761,.T.);
#26942=ADVANCED_FACE('',(#8118),#6762,.T.);
#26943=ADVANCED_FACE('',(#8119),#6763,.T.);
#26944=ADVANCED_FACE('',(#8120),#6764,.T.);
#26945=ADVANCED_FACE('',(#8121),#6765,.T.);
#26946=ADVANCED_FACE('',(#8122),#6766,.T.);
#26947=ADVANCED_FACE('',(#8123),#6767,.T.);
#26948=ADVANCED_FACE('',(#8124),#6768,.T.);
#26949=ADVANCED_FACE('',(#8125),#6769,.T.);
#26950=ADVANCED_FACE('',(#8126),#6770,.T.);
#26951=ADVANCED_FACE('',(#8127),#6771,.T.);
#26952=ADVANCED_FACE('',(#8128),#6772,.T.);
#26953=ADVANCED_FACE('',(#8129),#6773,.T.);
#26954=ADVANCED_FACE('',(#8130),#6774,.T.);
#26955=ADVANCED_FACE('',(#8131),#6775,.T.);
#26956=ADVANCED_FACE('',(#8132),#6776,.T.);
#26957=ADVANCED_FACE('',(#8133),#6777,.T.);
#26958=ADVANCED_FACE('',(#8134),#6778,.T.);
#26959=ADVANCED_FACE('',(#8135),#6779,.T.);
#26960=ADVANCED_FACE('',(#8136),#6780,.T.);
#26961=ADVANCED_FACE('',(#8137),#6781,.T.);
#26962=ADVANCED_FACE('',(#8138),#6782,.T.);
#26963=ADVANCED_FACE('',(#8139),#6783,.T.);
#26964=ADVANCED_FACE('',(#8140),#6784,.T.);
#26965=ADVANCED_FACE('',(#8141),#6785,.T.);
#26966=ADVANCED_FACE('',(#8142),#6786,.T.);
#26967=ADVANCED_FACE('',(#8143),#6787,.T.);
#26968=ADVANCED_FACE('',(#8144),#6788,.T.);
#26969=ADVANCED_FACE('',(#8145),#6789,.T.);
#26970=ADVANCED_FACE('',(#8146),#6790,.T.);
#26971=ADVANCED_FACE('',(#8147),#6791,.T.);
#26972=ADVANCED_FACE('',(#8148),#6792,.T.);
#26973=ADVANCED_FACE('',(#8149),#6793,.T.);
#26974=ADVANCED_FACE('',(#8150),#6794,.T.);
#26975=ADVANCED_FACE('',(#8151),#6795,.T.);
#26976=ADVANCED_FACE('',(#8152),#580,.F.);
#26977=ADVANCED_FACE('',(#8153),#1553,.T.);
#26978=ADVANCED_FACE('',(#8154),#6796,.T.);
#26979=ADVANCED_FACE('',(#8155),#581,.F.);
#26980=ADVANCED_FACE('',(#8156),#1554,.F.);
#26981=ADVANCED_FACE('',(#8157),#1555,.T.);
#26982=ADVANCED_FACE('',(#8158),#1556,.F.);
#26983=ADVANCED_FACE('',(#8159),#1557,.F.);
#26984=ADVANCED_FACE('',(#8160),#1558,.F.);
#26985=ADVANCED_FACE('',(#8161),#1559,.T.);
#26986=ADVANCED_FACE('',(#8162),#1560,.F.);
#26987=ADVANCED_FACE('',(#8163),#1561,.F.);
#26988=ADVANCED_FACE('',(#8164),#1562,.F.);
#26989=ADVANCED_FACE('',(#8165),#1563,.T.);
#26990=ADVANCED_FACE('',(#8166),#1564,.F.);
#26991=ADVANCED_FACE('',(#8167),#1565,.F.);
#26992=ADVANCED_FACE('',(#8168),#1566,.F.);
#26993=ADVANCED_FACE('',(#8169),#1567,.T.);
#26994=ADVANCED_FACE('',(#8170),#1568,.F.);
#26995=ADVANCED_FACE('',(#8171),#1569,.F.);
#26996=ADVANCED_FACE('',(#8172),#1570,.F.);
#26997=ADVANCED_FACE('',(#8173),#1571,.T.);
#26998=ADVANCED_FACE('',(#8174),#1572,.F.);
#26999=ADVANCED_FACE('',(#8175),#1573,.F.);
#27000=ADVANCED_FACE('',(#8176),#1574,.F.);
#27001=ADVANCED_FACE('',(#8177),#1575,.T.);
#27002=ADVANCED_FACE('',(#8178),#1576,.F.);
#27003=ADVANCED_FACE('',(#8179),#1577,.F.);
#27004=ADVANCED_FACE('',(#8180),#1578,.F.);
#27005=ADVANCED_FACE('',(#8181),#1579,.T.);
#27006=ADVANCED_FACE('',(#8182),#1580,.F.);
#27007=ADVANCED_FACE('',(#8183),#1581,.F.);
#27008=ADVANCED_FACE('',(#8184),#1582,.F.);
#27009=ADVANCED_FACE('',(#8185),#1583,.T.);
#27010=ADVANCED_FACE('',(#8186),#1584,.F.);
#27011=ADVANCED_FACE('',(#8187),#1585,.F.);
#27012=ADVANCED_FACE('',(#8188),#1586,.F.);
#27013=ADVANCED_FACE('',(#8189),#1587,.T.);
#27014=ADVANCED_FACE('',(#8190),#1588,.F.);
#27015=ADVANCED_FACE('',(#8191),#1589,.F.);
#27016=ADVANCED_FACE('',(#8192),#1590,.F.);
#27017=ADVANCED_FACE('',(#8193),#1591,.T.);
#27018=ADVANCED_FACE('',(#8194),#1592,.F.);
#27019=ADVANCED_FACE('',(#8195),#1593,.F.);
#27020=ADVANCED_FACE('',(#8196),#1594,.F.);
#27021=ADVANCED_FACE('',(#8197),#1595,.T.);
#27022=ADVANCED_FACE('',(#8198),#1596,.F.);
#27023=ADVANCED_FACE('',(#8199),#1597,.F.);
#27024=ADVANCED_FACE('',(#8200),#1598,.F.);
#27025=ADVANCED_FACE('',(#8201),#1599,.T.);
#27026=ADVANCED_FACE('',(#8202),#1600,.F.);
#27027=ADVANCED_FACE('',(#8203),#1601,.F.);
#27028=ADVANCED_FACE('',(#8204),#1602,.F.);
#27029=ADVANCED_FACE('',(#8205),#1603,.T.);
#27030=ADVANCED_FACE('',(#8206),#1604,.F.);
#27031=ADVANCED_FACE('',(#8207),#1605,.F.);
#27032=ADVANCED_FACE('',(#8208),#1606,.F.);
#27033=ADVANCED_FACE('',(#8209),#1607,.T.);
#27034=ADVANCED_FACE('',(#8210),#1608,.F.);
#27035=ADVANCED_FACE('',(#8211),#1609,.F.);
#27036=ADVANCED_FACE('',(#8212),#1610,.F.);
#27037=ADVANCED_FACE('',(#8213),#1611,.T.);
#27038=ADVANCED_FACE('',(#8214),#1612,.F.);
#27039=ADVANCED_FACE('',(#8215),#1613,.F.);
#27040=ADVANCED_FACE('',(#8216),#1614,.F.);
#27041=ADVANCED_FACE('',(#8217),#1615,.T.);
#27042=ADVANCED_FACE('',(#8218),#1616,.F.);
#27043=ADVANCED_FACE('',(#8219),#1617,.F.);
#27044=ADVANCED_FACE('',(#8220),#1618,.F.);
#27045=ADVANCED_FACE('',(#8221),#1619,.T.);
#27046=ADVANCED_FACE('',(#8222),#1620,.F.);
#27047=ADVANCED_FACE('',(#8223),#1621,.F.);
#27048=ADVANCED_FACE('',(#8224),#1622,.F.);
#27049=ADVANCED_FACE('',(#8225),#1623,.T.);
#27050=ADVANCED_FACE('',(#8226),#1624,.F.);
#27051=ADVANCED_FACE('',(#8227),#1625,.F.);
#27052=ADVANCED_FACE('',(#8228),#1626,.F.);
#27053=ADVANCED_FACE('',(#8229),#1627,.T.);
#27054=ADVANCED_FACE('',(#8230),#1628,.F.);
#27055=ADVANCED_FACE('',(#8231),#1629,.F.);
#27056=ADVANCED_FACE('',(#8232),#1630,.F.);
#27057=ADVANCED_FACE('',(#8233),#1631,.T.);
#27058=ADVANCED_FACE('',(#8234),#1632,.F.);
#27059=ADVANCED_FACE('',(#8235),#1633,.F.);
#27060=ADVANCED_FACE('',(#8236),#1634,.F.);
#27061=ADVANCED_FACE('',(#8237),#1635,.T.);
#27062=ADVANCED_FACE('',(#8238),#1636,.F.);
#27063=ADVANCED_FACE('',(#8239),#1637,.F.);
#27064=ADVANCED_FACE('',(#8240),#1638,.F.);
#27065=ADVANCED_FACE('',(#8241),#1639,.T.);
#27066=ADVANCED_FACE('',(#8242),#1640,.F.);
#27067=ADVANCED_FACE('',(#8243),#1641,.F.);
#27068=ADVANCED_FACE('',(#8244),#1642,.F.);
#27069=ADVANCED_FACE('',(#8245),#1643,.T.);
#27070=ADVANCED_FACE('',(#8246),#1644,.F.);
#27071=ADVANCED_FACE('',(#8247),#1645,.F.);
#27072=ADVANCED_FACE('',(#8248),#1646,.F.);
#27073=ADVANCED_FACE('',(#8249),#1647,.T.);
#27074=ADVANCED_FACE('',(#8250),#1648,.F.);
#27075=ADVANCED_FACE('',(#8251),#1649,.F.);
#27076=ADVANCED_FACE('',(#8252),#1650,.F.);
#27077=ADVANCED_FACE('',(#8253),#1651,.T.);
#27078=ADVANCED_FACE('',(#8254),#1652,.F.);
#27079=ADVANCED_FACE('',(#8255),#1653,.F.);
#27080=ADVANCED_FACE('',(#8256),#1654,.F.);
#27081=ADVANCED_FACE('',(#8257),#1655,.T.);
#27082=ADVANCED_FACE('',(#8258),#1656,.F.);
#27083=ADVANCED_FACE('',(#8259),#1657,.F.);
#27084=ADVANCED_FACE('',(#8260),#1658,.F.);
#27085=ADVANCED_FACE('',(#8261),#1659,.T.);
#27086=ADVANCED_FACE('',(#8262),#1660,.F.);
#27087=ADVANCED_FACE('',(#8263),#1661,.F.);
#27088=ADVANCED_FACE('',(#8264),#1662,.F.);
#27089=ADVANCED_FACE('',(#8265),#1663,.T.);
#27090=ADVANCED_FACE('',(#8266),#1664,.F.);
#27091=ADVANCED_FACE('',(#8267),#1665,.F.);
#27092=ADVANCED_FACE('',(#8268),#1666,.F.);
#27093=ADVANCED_FACE('',(#8269),#1667,.T.);
#27094=ADVANCED_FACE('',(#8270),#1668,.F.);
#27095=ADVANCED_FACE('',(#8271),#1669,.F.);
#27096=ADVANCED_FACE('',(#8272),#1670,.F.);
#27097=ADVANCED_FACE('',(#8273),#1671,.T.);
#27098=ADVANCED_FACE('',(#8274),#1672,.F.);
#27099=ADVANCED_FACE('',(#8275),#1673,.F.);
#27100=ADVANCED_FACE('',(#8276),#1674,.F.);
#27101=ADVANCED_FACE('',(#8277),#1675,.T.);
#27102=ADVANCED_FACE('',(#8278),#1676,.F.);
#27103=ADVANCED_FACE('',(#8279),#1677,.F.);
#27104=ADVANCED_FACE('',(#8280),#1678,.F.);
#27105=ADVANCED_FACE('',(#8281),#1679,.T.);
#27106=ADVANCED_FACE('',(#8282),#1680,.F.);
#27107=ADVANCED_FACE('',(#8283),#1681,.F.);
#27108=ADVANCED_FACE('',(#8284),#1682,.F.);
#27109=ADVANCED_FACE('',(#8285),#1683,.T.);
#27110=ADVANCED_FACE('',(#8286),#1684,.F.);
#27111=ADVANCED_FACE('',(#8287),#1685,.F.);
#27112=ADVANCED_FACE('',(#8288),#1686,.F.);
#27113=ADVANCED_FACE('',(#8289),#1687,.T.);
#27114=ADVANCED_FACE('',(#8290),#1688,.F.);
#27115=ADVANCED_FACE('',(#8291),#1689,.F.);
#27116=ADVANCED_FACE('',(#8292),#1690,.F.);
#27117=ADVANCED_FACE('',(#8293),#1691,.T.);
#27118=ADVANCED_FACE('',(#8294),#1692,.F.);
#27119=ADVANCED_FACE('',(#8295),#1693,.F.);
#27120=ADVANCED_FACE('',(#8296),#1694,.F.);
#27121=ADVANCED_FACE('',(#8297),#1695,.T.);
#27122=ADVANCED_FACE('',(#8298),#1696,.F.);
#27123=ADVANCED_FACE('',(#8299),#1697,.F.);
#27124=ADVANCED_FACE('',(#8300),#1698,.F.);
#27125=ADVANCED_FACE('',(#8301),#1699,.F.);
#27126=ADVANCED_FACE('',(#8302),#1700,.F.);
#27127=ADVANCED_FACE('',(#8303),#1701,.F.);
#27128=ADVANCED_FACE('',(#8304),#1702,.F.);
#27129=ADVANCED_FACE('',(#8305),#1703,.F.);
#27130=ADVANCED_FACE('',(#8306),#1704,.F.);
#27131=ADVANCED_FACE('',(#8307),#1705,.T.);
#27132=ADVANCED_FACE('',(#8308),#408,.T.);
#27133=ADVANCED_FACE('',(#8309),#6797,.T.);
#27134=ADVANCED_FACE('',(#8310,#717),#1706,.T.);
#27135=ADVANCED_FACE('',(#8311,#718,#719,#720,#721,#722,#723,#724,#725,
#726,#727,#728,#729,#730,#731,#732,#733,#734,#735,#736,#737,#738,#739,#740,
#741,#742,#743,#744,#745,#746,#747,#748,#749,#750,#751,#752),#6798,.T.);
#27136=ADVANCED_FACE('',(#8312),#409,.T.);
#27137=ADVANCED_FACE('',(#8313,#753),#1707,.T.);
#27238=CLOSED_SHELL('',(#26936,#26937,#26938,#26939,#26940,#26941,#26942,
#26943,#26944,#26945,#26946,#26947,#26948,#26949,#26950,#26951,#26952,#26953,
#26954,#26955,#26956,#26957,#26958,#26959,#26960,#26961,#26962,#26963,#26964,
#26965,#26966,#26967,#26968,#26969,#26970,#26971,#26972,#26973,#26974,#26975,
#26976,#26977,#26978,#26979,#26980,#26981,#26982,#26983,#26984,#26985,#26986,
#26987,#26988,#26989,#26990,#26991,#26992,#26993,#26994,#26995,#26996,#26997,
#26998,#26999,#27000,#27001,#27002,#27003,#27004,#27005,#27006,#27007,#27008,
#27009,#27010,#27011,#27012,#27013,#27014,#27015,#27016,#27017,#27018,#27019,
#27020,#27021,#27022,#27023,#27024,#27025,#27026,#27027,#27028,#27029,#27030,
#27031,#27032,#27033,#27034,#27035,#27036,#27037,#27038,#27039,#27040,#27041,
#27042,#27043,#27044,#27045,#27046,#27047,#27048,#27049,#27050,#27051,#27052,
#27053,#27054,#27055,#27056,#27057,#27058,#27059,#27060,#27061,#27062,#27063,
#27064,#27065,#27066,#27067,#27068,#27069,#27070,#27071,#27072,#27073,#27074,
#27075,#27076,#27077,#27078,#27079,#27080,#27081,#27082,#27083,#27084,#27085,
#27086,#27087,#27088,#27089,#27090,#27091,#27092,#27093,#27094,#27095,#27096,
#27097,#27098,#27099,#27100,#27101,#27102,#27103,#27104,#27105,#27106,#27107,
#27108,#27109,#27110,#27111,#27112,#27113,#27114,#27115,#27116,#27117,#27118,
#27119,#27120,#27121,#27122,#27123,#27124,#27125,#27126,#27127,#27128,#27129,
#27130,#27131,#27132,#27133,#27134,#27135,#27136,#27137));
#29560=AXIS2_PLACEMENT_3D('',#49727,#36105,#36106);
#29561=AXIS2_PLACEMENT_3D('',#49728,#36107,#36108);
#29562=AXIS2_PLACEMENT_3D('',#49744,#36110,#36111);
#29563=AXIS2_PLACEMENT_3D('',#49755,#36112,#36113);
#29564=AXIS2_PLACEMENT_3D('',#49803,#36115,#36116);
#29565=AXIS2_PLACEMENT_3D('',#49851,#36118,#36119);
#29566=AXIS2_PLACEMENT_3D('',#49899,#36121,#36122);
#29567=AXIS2_PLACEMENT_3D('',#49953,#36124,#36125);
#29568=AXIS2_PLACEMENT_3D('',#50001,#36127,#36128);
#29569=AXIS2_PLACEMENT_3D('',#50049,#36130,#36131);
#29570=AXIS2_PLACEMENT_3D('',#50103,#36133,#36134);
#29571=AXIS2_PLACEMENT_3D('',#50151,#36136,#36137);
#29572=AXIS2_PLACEMENT_3D('',#50199,#36139,#36140);
#29573=AXIS2_PLACEMENT_3D('',#50247,#36142,#36143);
#29574=AXIS2_PLACEMENT_3D('',#50301,#36145,#36146);
#29575=AXIS2_PLACEMENT_3D('',#50349,#36148,#36149);
#29576=AXIS2_PLACEMENT_3D('',#50397,#36151,#36152);
#29577=AXIS2_PLACEMENT_3D('',#50451,#36154,#36155);
#29578=AXIS2_PLACEMENT_3D('',#50499,#36157,#36158);
#29579=AXIS2_PLACEMENT_3D('',#50547,#36160,#36161);
#29580=AXIS2_PLACEMENT_3D('',#50595,#36163,#36164);
#29581=AXIS2_PLACEMENT_3D('',#50649,#36166,#36167);
#29582=AXIS2_PLACEMENT_3D('',#50697,#36169,#36170);
#29583=AXIS2_PLACEMENT_3D('',#50706,#36172,#36173);
#29584=AXIS2_PLACEMENT_3D('',#50707,#36174,#36175);
#29585=AXIS2_PLACEMENT_3D('',#50722,#36177,#36178);
#29586=AXIS2_PLACEMENT_3D('',#50733,#36179,#36180);
#29587=AXIS2_PLACEMENT_3D('',#50758,#36182,#36183);
#29588=AXIS2_PLACEMENT_3D('',#50783,#36185,#36186);
#29589=AXIS2_PLACEMENT_3D('',#50807,#36188,#36189);
#29590=AXIS2_PLACEMENT_3D('',#50831,#36191,#36192);
#29591=AXIS2_PLACEMENT_3D('',#50856,#36194,#36195);
#29592=AXIS2_PLACEMENT_3D('',#50881,#36197,#36198);
#29593=AXIS2_PLACEMENT_3D('',#50905,#36200,#36201);
#29594=AXIS2_PLACEMENT_3D('',#50930,#36203,#36204);
#29595=AXIS2_PLACEMENT_3D('',#50955,#36206,#36207);
#29596=AXIS2_PLACEMENT_3D('',#50979,#36209,#36210);
#29597=AXIS2_PLACEMENT_3D('',#51003,#36212,#36213);
#29598=AXIS2_PLACEMENT_3D('',#51028,#36215,#36216);
#29599=AXIS2_PLACEMENT_3D('',#51053,#36218,#36219);
#29600=AXIS2_PLACEMENT_3D('',#51077,#36221,#36222);
#29601=AXIS2_PLACEMENT_3D('',#51102,#36224,#36225);
#29602=AXIS2_PLACEMENT_3D('',#51127,#36227,#36228);
#29603=AXIS2_PLACEMENT_3D('',#51151,#36230,#36231);
#29604=AXIS2_PLACEMENT_3D('',#51929,#36233,#36234);
#29605=AXIS2_PLACEMENT_3D('',#51931,#36235,#36236);
#29606=AXIS2_PLACEMENT_3D('',#51932,#36237,#36238);
#29607=AXIS2_PLACEMENT_3D('',#52037,#36239,#36240);
#29608=AXIS2_PLACEMENT_3D('',#52038,#36241,#36242);
#29609=AXIS2_PLACEMENT_3D('',#52689,#36243,#36244);
#29610=AXIS2_PLACEMENT_3D('',#52698,#36249,#36250);
#29611=AXIS2_PLACEMENT_3D('',#52700,#36251,#36252);
#29612=AXIS2_PLACEMENT_3D('',#52702,#36254,#36255);
#29613=AXIS2_PLACEMENT_3D('',#52706,#36258,#36259);
#29614=AXIS2_PLACEMENT_3D('',#52707,#36260,#36261);
#29615=AXIS2_PLACEMENT_3D('',#52708,#36262,#36263);
#29616=AXIS2_PLACEMENT_3D('',#52717,#36268,#36269);
#29617=AXIS2_PLACEMENT_3D('',#52719,#36270,#36271);
#29618=AXIS2_PLACEMENT_3D('',#52721,#36273,#36274);
#29619=AXIS2_PLACEMENT_3D('',#52725,#36277,#36278);
#29620=AXIS2_PLACEMENT_3D('',#52726,#36279,#36280);
#29621=AXIS2_PLACEMENT_3D('',#52727,#36281,#36282);
#29622=AXIS2_PLACEMENT_3D('',#52736,#36287,#36288);
#29623=AXIS2_PLACEMENT_3D('',#52738,#36289,#36290);
#29624=AXIS2_PLACEMENT_3D('',#52740,#36292,#36293);
#29625=AXIS2_PLACEMENT_3D('',#52744,#36296,#36297);
#29626=AXIS2_PLACEMENT_3D('',#52745,#36298,#36299);
#29627=AXIS2_PLACEMENT_3D('',#52746,#36300,#36301);
#29628=AXIS2_PLACEMENT_3D('',#52755,#36306,#36307);
#29629=AXIS2_PLACEMENT_3D('',#52757,#36308,#36309);
#29630=AXIS2_PLACEMENT_3D('',#52759,#36311,#36312);
#29631=AXIS2_PLACEMENT_3D('',#52763,#36315,#36316);
#29632=AXIS2_PLACEMENT_3D('',#52764,#36317,#36318);
#29633=AXIS2_PLACEMENT_3D('',#52765,#36319,#36320);
#29634=AXIS2_PLACEMENT_3D('',#52774,#36325,#36326);
#29635=AXIS2_PLACEMENT_3D('',#52776,#36327,#36328);
#29636=AXIS2_PLACEMENT_3D('',#52778,#36330,#36331);
#29637=AXIS2_PLACEMENT_3D('',#52782,#36334,#36335);
#29638=AXIS2_PLACEMENT_3D('',#52783,#36336,#36337);
#29639=AXIS2_PLACEMENT_3D('',#52784,#36338,#36339);
#29640=AXIS2_PLACEMENT_3D('',#52793,#36344,#36345);
#29641=AXIS2_PLACEMENT_3D('',#52795,#36346,#36347);
#29642=AXIS2_PLACEMENT_3D('',#52797,#36349,#36350);
#29643=AXIS2_PLACEMENT_3D('',#52801,#36353,#36354);
#29644=AXIS2_PLACEMENT_3D('',#52802,#36355,#36356);
#29645=AXIS2_PLACEMENT_3D('',#52803,#36357,#36358);
#29646=AXIS2_PLACEMENT_3D('',#52812,#36363,#36364);
#29647=AXIS2_PLACEMENT_3D('',#52814,#36365,#36366);
#29648=AXIS2_PLACEMENT_3D('',#52816,#36368,#36369);
#29649=AXIS2_PLACEMENT_3D('',#52820,#36372,#36373);
#29650=AXIS2_PLACEMENT_3D('',#52821,#36374,#36375);
#29651=AXIS2_PLACEMENT_3D('',#52822,#36376,#36377);
#29652=AXIS2_PLACEMENT_3D('',#52831,#36382,#36383);
#29653=AXIS2_PLACEMENT_3D('',#52833,#36384,#36385);
#29654=AXIS2_PLACEMENT_3D('',#52835,#36387,#36388);
#29655=AXIS2_PLACEMENT_3D('',#52839,#36391,#36392);
#29656=AXIS2_PLACEMENT_3D('',#52840,#36393,#36394);
#29657=AXIS2_PLACEMENT_3D('',#52841,#36395,#36396);
#29658=AXIS2_PLACEMENT_3D('',#52850,#36401,#36402);
#29659=AXIS2_PLACEMENT_3D('',#52852,#36403,#36404);
#29660=AXIS2_PLACEMENT_3D('',#52854,#36406,#36407);
#29661=AXIS2_PLACEMENT_3D('',#52858,#36410,#36411);
#29662=AXIS2_PLACEMENT_3D('',#52859,#36412,#36413);
#29663=AXIS2_PLACEMENT_3D('',#52860,#36414,#36415);
#29664=AXIS2_PLACEMENT_3D('',#52869,#36420,#36421);
#29665=AXIS2_PLACEMENT_3D('',#52871,#36422,#36423);
#29666=AXIS2_PLACEMENT_3D('',#52873,#36425,#36426);
#29667=AXIS2_PLACEMENT_3D('',#52877,#36429,#36430);
#29668=AXIS2_PLACEMENT_3D('',#52878,#36431,#36432);
#29669=AXIS2_PLACEMENT_3D('',#52879,#36433,#36434);
#29670=AXIS2_PLACEMENT_3D('',#52888,#36439,#36440);
#29671=AXIS2_PLACEMENT_3D('',#52890,#36441,#36442);
#29672=AXIS2_PLACEMENT_3D('',#52892,#36444,#36445);
#29673=AXIS2_PLACEMENT_3D('',#52896,#36448,#36449);
#29674=AXIS2_PLACEMENT_3D('',#52897,#36450,#36451);
#29675=AXIS2_PLACEMENT_3D('',#52898,#36452,#36453);
#29676=AXIS2_PLACEMENT_3D('',#52907,#36458,#36459);
#29677=AXIS2_PLACEMENT_3D('',#52909,#36460,#36461);
#29678=AXIS2_PLACEMENT_3D('',#52911,#36463,#36464);
#29679=AXIS2_PLACEMENT_3D('',#52915,#36467,#36468);
#29680=AXIS2_PLACEMENT_3D('',#52916,#36469,#36470);
#29681=AXIS2_PLACEMENT_3D('',#52917,#36471,#36472);
#29682=AXIS2_PLACEMENT_3D('',#52926,#36477,#36478);
#29683=AXIS2_PLACEMENT_3D('',#52928,#36479,#36480);
#29684=AXIS2_PLACEMENT_3D('',#52930,#36482,#36483);
#29685=AXIS2_PLACEMENT_3D('',#52934,#36486,#36487);
#29686=AXIS2_PLACEMENT_3D('',#52935,#36488,#36489);
#29687=AXIS2_PLACEMENT_3D('',#52936,#36490,#36491);
#29688=AXIS2_PLACEMENT_3D('',#52945,#36496,#36497);
#29689=AXIS2_PLACEMENT_3D('',#52947,#36498,#36499);
#29690=AXIS2_PLACEMENT_3D('',#52949,#36501,#36502);
#29691=AXIS2_PLACEMENT_3D('',#52953,#36505,#36506);
#29692=AXIS2_PLACEMENT_3D('',#52954,#36507,#36508);
#29693=AXIS2_PLACEMENT_3D('',#52955,#36509,#36510);
#29694=AXIS2_PLACEMENT_3D('',#52964,#36515,#36516);
#29695=AXIS2_PLACEMENT_3D('',#52966,#36517,#36518);
#29696=AXIS2_PLACEMENT_3D('',#52968,#36520,#36521);
#29697=AXIS2_PLACEMENT_3D('',#52972,#36524,#36525);
#29698=AXIS2_PLACEMENT_3D('',#52973,#36526,#36527);
#29699=AXIS2_PLACEMENT_3D('',#52974,#36528,#36529);
#29700=AXIS2_PLACEMENT_3D('',#52983,#36534,#36535);
#29701=AXIS2_PLACEMENT_3D('',#52985,#36536,#36537);
#29702=AXIS2_PLACEMENT_3D('',#52987,#36539,#36540);
#29703=AXIS2_PLACEMENT_3D('',#52991,#36543,#36544);
#29704=AXIS2_PLACEMENT_3D('',#52992,#36545,#36546);
#29705=AXIS2_PLACEMENT_3D('',#52993,#36547,#36548);
#29706=AXIS2_PLACEMENT_3D('',#53002,#36553,#36554);
#29707=AXIS2_PLACEMENT_3D('',#53004,#36555,#36556);
#29708=AXIS2_PLACEMENT_3D('',#53006,#36558,#36559);
#29709=AXIS2_PLACEMENT_3D('',#53010,#36562,#36563);
#29710=AXIS2_PLACEMENT_3D('',#53011,#36564,#36565);
#29711=AXIS2_PLACEMENT_3D('',#53012,#36566,#36567);
#29712=AXIS2_PLACEMENT_3D('',#53021,#36572,#36573);
#29713=AXIS2_PLACEMENT_3D('',#53023,#36574,#36575);
#29714=AXIS2_PLACEMENT_3D('',#53026,#36577,#36578);
#29715=AXIS2_PLACEMENT_3D('',#53027,#36579,#36580);
#29716=AXIS2_PLACEMENT_3D('',#53031,#36583,#36584);
#29717=AXIS2_PLACEMENT_3D('',#53033,#36585,#36586);
#29718=AXIS2_PLACEMENT_3D('',#53034,#36587,#36588);
#29719=AXIS2_PLACEMENT_3D('',#53035,#36589,#36590);
#29720=AXIS2_PLACEMENT_3D('',#53044,#36595,#36596);
#29721=AXIS2_PLACEMENT_3D('',#53046,#36597,#36598);
#29722=AXIS2_PLACEMENT_3D('',#53048,#36600,#36601);
#29723=AXIS2_PLACEMENT_3D('',#53052,#36604,#36605);
#29724=AXIS2_PLACEMENT_3D('',#53053,#36606,#36607);
#29725=AXIS2_PLACEMENT_3D('',#53054,#36608,#36609);
#29726=AXIS2_PLACEMENT_3D('',#53063,#36614,#36615);
#29727=AXIS2_PLACEMENT_3D('',#53065,#36616,#36617);
#29728=AXIS2_PLACEMENT_3D('',#53067,#36619,#36620);
#29729=AXIS2_PLACEMENT_3D('',#53071,#36623,#36624);
#29730=AXIS2_PLACEMENT_3D('',#53072,#36625,#36626);
#29731=AXIS2_PLACEMENT_3D('',#53073,#36627,#36628);
#29732=AXIS2_PLACEMENT_3D('',#53082,#36633,#36634);
#29733=AXIS2_PLACEMENT_3D('',#53084,#36635,#36636);
#29734=AXIS2_PLACEMENT_3D('',#53086,#36638,#36639);
#29735=AXIS2_PLACEMENT_3D('',#53090,#36642,#36643);
#29736=AXIS2_PLACEMENT_3D('',#53091,#36644,#36645);
#29737=AXIS2_PLACEMENT_3D('',#53092,#36646,#36647);
#29738=AXIS2_PLACEMENT_3D('',#53101,#36652,#36653);
#29739=AXIS2_PLACEMENT_3D('',#53103,#36654,#36655);
#29740=AXIS2_PLACEMENT_3D('',#53105,#36657,#36658);
#29741=AXIS2_PLACEMENT_3D('',#53109,#36661,#36662);
#29742=AXIS2_PLACEMENT_3D('',#53110,#36663,#36664);
#29743=AXIS2_PLACEMENT_3D('',#53111,#36665,#36666);
#29744=AXIS2_PLACEMENT_3D('',#53120,#36671,#36672);
#29745=AXIS2_PLACEMENT_3D('',#53122,#36673,#36674);
#29746=AXIS2_PLACEMENT_3D('',#53124,#36676,#36677);
#29747=AXIS2_PLACEMENT_3D('',#53128,#36680,#36681);
#29748=AXIS2_PLACEMENT_3D('',#53129,#36682,#36683);
#29749=AXIS2_PLACEMENT_3D('',#53130,#36684,#36685);
#29750=AXIS2_PLACEMENT_3D('',#53139,#36690,#36691);
#29751=AXIS2_PLACEMENT_3D('',#53141,#36692,#36693);
#29752=AXIS2_PLACEMENT_3D('',#53143,#36695,#36696);
#29753=AXIS2_PLACEMENT_3D('',#53147,#36699,#36700);
#29754=AXIS2_PLACEMENT_3D('',#53148,#36701,#36702);
#29755=AXIS2_PLACEMENT_3D('',#53149,#36703,#36704);
#29756=AXIS2_PLACEMENT_3D('',#53158,#36709,#36710);
#29757=AXIS2_PLACEMENT_3D('',#53160,#36711,#36712);
#29758=AXIS2_PLACEMENT_3D('',#53162,#36714,#36715);
#29759=AXIS2_PLACEMENT_3D('',#53166,#36718,#36719);
#29760=AXIS2_PLACEMENT_3D('',#53167,#36720,#36721);
#29761=AXIS2_PLACEMENT_3D('',#53168,#36722,#36723);
#29762=AXIS2_PLACEMENT_3D('',#53177,#36728,#36729);
#29763=AXIS2_PLACEMENT_3D('',#53179,#36730,#36731);
#29764=AXIS2_PLACEMENT_3D('',#53181,#36733,#36734);
#29765=AXIS2_PLACEMENT_3D('',#53185,#36737,#36738);
#29766=AXIS2_PLACEMENT_3D('',#53186,#36739,#36740);
#29767=AXIS2_PLACEMENT_3D('',#53187,#36741,#36742);
#29768=AXIS2_PLACEMENT_3D('',#53196,#36747,#36748);
#29769=AXIS2_PLACEMENT_3D('',#53198,#36749,#36750);
#29770=AXIS2_PLACEMENT_3D('',#53200,#36752,#36753);
#29771=AXIS2_PLACEMENT_3D('',#53204,#36756,#36757);
#29772=AXIS2_PLACEMENT_3D('',#53205,#36758,#36759);
#29773=AXIS2_PLACEMENT_3D('',#53206,#36760,#36761);
#29774=AXIS2_PLACEMENT_3D('',#53215,#36766,#36767);
#29775=AXIS2_PLACEMENT_3D('',#53217,#36768,#36769);
#29776=AXIS2_PLACEMENT_3D('',#53219,#36771,#36772);
#29777=AXIS2_PLACEMENT_3D('',#53223,#36775,#36776);
#29778=AXIS2_PLACEMENT_3D('',#53224,#36777,#36778);
#29779=AXIS2_PLACEMENT_3D('',#53225,#36779,#36780);
#29780=AXIS2_PLACEMENT_3D('',#53234,#36785,#36786);
#29781=AXIS2_PLACEMENT_3D('',#53236,#36787,#36788);
#29782=AXIS2_PLACEMENT_3D('',#53238,#36790,#36791);
#29783=AXIS2_PLACEMENT_3D('',#53242,#36794,#36795);
#29784=AXIS2_PLACEMENT_3D('',#53243,#36796,#36797);
#29785=AXIS2_PLACEMENT_3D('',#53244,#36798,#36799);
#29786=AXIS2_PLACEMENT_3D('',#53253,#36804,#36805);
#29787=AXIS2_PLACEMENT_3D('',#53255,#36806,#36807);
#29788=AXIS2_PLACEMENT_3D('',#53257,#36809,#36810);
#29789=AXIS2_PLACEMENT_3D('',#53261,#36813,#36814);
#29790=AXIS2_PLACEMENT_3D('',#53262,#36815,#36816);
#29791=AXIS2_PLACEMENT_3D('',#53263,#36817,#36818);
#29792=AXIS2_PLACEMENT_3D('',#53272,#36823,#36824);
#29793=AXIS2_PLACEMENT_3D('',#53274,#36825,#36826);
#29794=AXIS2_PLACEMENT_3D('',#53276,#36828,#36829);
#29795=AXIS2_PLACEMENT_3D('',#53280,#36832,#36833);
#29796=AXIS2_PLACEMENT_3D('',#53281,#36834,#36835);
#29797=AXIS2_PLACEMENT_3D('',#53282,#36836,#36837);
#29798=AXIS2_PLACEMENT_3D('',#53291,#36842,#36843);
#29799=AXIS2_PLACEMENT_3D('',#53293,#36844,#36845);
#29800=AXIS2_PLACEMENT_3D('',#53295,#36847,#36848);
#29801=AXIS2_PLACEMENT_3D('',#53299,#36851,#36852);
#29802=AXIS2_PLACEMENT_3D('',#53300,#36853,#36854);
#29803=AXIS2_PLACEMENT_3D('',#53301,#36855,#36856);
#29804=AXIS2_PLACEMENT_3D('',#53310,#36861,#36862);
#29805=AXIS2_PLACEMENT_3D('',#53312,#36863,#36864);
#29806=AXIS2_PLACEMENT_3D('',#53314,#36866,#36867);
#29807=AXIS2_PLACEMENT_3D('',#53318,#36870,#36871);
#29808=AXIS2_PLACEMENT_3D('',#53319,#36872,#36873);
#29809=AXIS2_PLACEMENT_3D('',#53320,#36874,#36875);
#29810=AXIS2_PLACEMENT_3D('',#53329,#36880,#36881);
#29811=AXIS2_PLACEMENT_3D('',#53331,#36882,#36883);
#29812=AXIS2_PLACEMENT_3D('',#53333,#36885,#36886);
#29813=AXIS2_PLACEMENT_3D('',#53337,#36889,#36890);
#29814=AXIS2_PLACEMENT_3D('',#53338,#36891,#36892);
#29815=AXIS2_PLACEMENT_3D('',#53339,#36893,#36894);
#29816=AXIS2_PLACEMENT_3D('',#53348,#36899,#36900);
#29817=AXIS2_PLACEMENT_3D('',#53350,#36901,#36902);
#29818=AXIS2_PLACEMENT_3D('',#53352,#36904,#36905);
#29819=AXIS2_PLACEMENT_3D('',#53356,#36908,#36909);
#29820=AXIS2_PLACEMENT_3D('',#53357,#36910,#36911);
#29821=AXIS2_PLACEMENT_3D('',#53358,#36912,#36913);
#29822=AXIS2_PLACEMENT_3D('',#53367,#36918,#36919);
#29823=AXIS2_PLACEMENT_3D('',#53369,#36920,#36921);
#29824=AXIS2_PLACEMENT_3D('',#53371,#36923,#36924);
#29825=AXIS2_PLACEMENT_3D('',#53375,#36927,#36928);
#29826=AXIS2_PLACEMENT_3D('',#53376,#36929,#36930);
#29827=AXIS2_PLACEMENT_3D('',#53377,#36931,#36932);
#29828=AXIS2_PLACEMENT_3D('',#53386,#36937,#36938);
#29829=AXIS2_PLACEMENT_3D('',#53392,#36942,#36943);
#29830=AXIS2_PLACEMENT_3D('',#53398,#36947,#36948);
#29831=AXIS2_PLACEMENT_3D('',#53404,#36952,#36953);
#29832=AXIS2_PLACEMENT_3D('',#53410,#36957,#36958);
#29833=AXIS2_PLACEMENT_3D('',#53413,#36961,#36962);
#29834=AXIS2_PLACEMENT_3D('',#53414,#36963,#36964);
#29835=AXIS2_PLACEMENT_3D('',#53416,#36965,#36966);
#29836=AXIS2_PLACEMENT_3D('',#53417,#36967,#36968);
#29837=AXIS2_PLACEMENT_3D('',#53419,#36970,#36971);
#29838=AXIS2_PLACEMENT_3D('',#53420,#36972,#36973);
#29839=AXIS2_PLACEMENT_3D('',#53421,#36974,#36975);
#29840=AXIS2_PLACEMENT_3D('',#53423,#36976,#36977);
#29841=AXIS2_PLACEMENT_3D('',#53424,#36978,#36979);
#29842=AXIS2_PLACEMENT_3D('',#53426,#36980,#36981);
#29843=AXIS2_PLACEMENT_3D('',#53429,#36984,#36985);
#29844=AXIS2_PLACEMENT_3D('',#53431,#36986,#36987);
#29845=AXIS2_PLACEMENT_3D('',#53433,#36989,#36990);
#36105=DIRECTION('axis',(0.,0.,1.));
#36106=DIRECTION('refdir',(1.,0.,0.));
#36107=DIRECTION('center_axis',(1.,0.,0.));
#36108=DIRECTION('ref_axis',(0.,1.,0.));
#36109=DIRECTION('',(-1.,0.,0.));
#36110=DIRECTION('center_axis',(1.,0.,0.));
#36111=DIRECTION('ref_axis',(0.,1.,0.));
#36112=DIRECTION('center_axis',(1.,0.,0.));
#36113=DIRECTION('ref_axis',(0.,1.,0.));
#36114=DIRECTION('',(-1.,0.,0.));
#36115=DIRECTION('center_axis',(1.,0.,0.));
#36116=DIRECTION('ref_axis',(0.,1.,0.));
#36117=DIRECTION('',(-1.,0.,0.));
#36118=DIRECTION('center_axis',(1.,0.,0.));
#36119=DIRECTION('ref_axis',(0.,1.,0.));
#36120=DIRECTION('',(-1.,0.,0.));
#36121=DIRECTION('center_axis',(1.,0.,0.));
#36122=DIRECTION('ref_axis',(0.,1.,0.));
#36123=DIRECTION('',(-1.,0.,0.));
#36124=DIRECTION('center_axis',(1.,0.,0.));
#36125=DIRECTION('ref_axis',(0.,1.,0.));
#36126=DIRECTION('',(-1.,0.,0.));
#36127=DIRECTION('center_axis',(1.,0.,0.));
#36128=DIRECTION('ref_axis',(0.,1.,0.));
#36129=DIRECTION('',(-1.,0.,0.));
#36130=DIRECTION('center_axis',(1.,0.,0.));
#36131=DIRECTION('ref_axis',(0.,1.,0.));
#36132=DIRECTION('',(-1.,0.,0.));
#36133=DIRECTION('center_axis',(1.,0.,0.));
#36134=DIRECTION('ref_axis',(0.,1.,0.));
#36135=DIRECTION('',(-1.,0.,0.));
#36136=DIRECTION('center_axis',(1.,0.,0.));
#36137=DIRECTION('ref_axis',(0.,1.,0.));
#36138=DIRECTION('',(-1.,0.,0.));
#36139=DIRECTION('center_axis',(1.,0.,0.));
#36140=DIRECTION('ref_axis',(0.,1.,0.));
#36141=DIRECTION('',(-1.,0.,0.));
#36142=DIRECTION('center_axis',(1.,0.,0.));
#36143=DIRECTION('ref_axis',(0.,1.,0.));
#36144=DIRECTION('',(-1.,0.,0.));
#36145=DIRECTION('center_axis',(1.,0.,0.));
#36146=DIRECTION('ref_axis',(0.,1.,0.));
#36147=DIRECTION('',(-1.,0.,0.));
#36148=DIRECTION('center_axis',(1.,0.,0.));
#36149=DIRECTION('ref_axis',(0.,1.,0.));
#36150=DIRECTION('',(-1.,0.,0.));
#36151=DIRECTION('center_axis',(1.,0.,0.));
#36152=DIRECTION('ref_axis',(0.,1.,0.));
#36153=DIRECTION('',(-1.,0.,0.));
#36154=DIRECTION('center_axis',(1.,0.,0.));
#36155=DIRECTION('ref_axis',(0.,1.,0.));
#36156=DIRECTION('',(-1.,0.,0.));
#36157=DIRECTION('center_axis',(1.,0.,0.));
#36158=DIRECTION('ref_axis',(0.,1.,0.));
#36159=DIRECTION('',(-1.,0.,0.));
#36160=DIRECTION('center_axis',(1.,0.,0.));
#36161=DIRECTION('ref_axis',(0.,1.,0.));
#36162=DIRECTION('',(-1.,0.,0.));
#36163=DIRECTION('center_axis',(1.,0.,0.));
#36164=DIRECTION('ref_axis',(0.,1.,0.));
#36165=DIRECTION('',(-1.,0.,0.));
#36166=DIRECTION('center_axis',(1.,0.,0.));
#36167=DIRECTION('ref_axis',(0.,1.,0.));
#36168=DIRECTION('',(-1.,0.,0.));
#36169=DIRECTION('center_axis',(1.,0.,0.));
#36170=DIRECTION('ref_axis',(0.,1.,1.18505573263654E-13));
#36171=DIRECTION('',(1.,0.,0.));
#36172=DIRECTION('center_axis',(1.,0.,0.));
#36173=DIRECTION('ref_axis',(0.,1.,1.18505573263654E-13));
#36174=DIRECTION('center_axis',(1.,0.,0.));
#36175=DIRECTION('ref_axis',(0.,1.,1.18505573263654E-13));
#36176=DIRECTION('',(1.,0.,0.));
#36177=DIRECTION('center_axis',(1.,0.,0.));
#36178=DIRECTION('ref_axis',(0.,1.,1.18505573263654E-13));
#36179=DIRECTION('center_axis',(1.,0.,0.));
#36180=DIRECTION('ref_axis',(0.,1.,1.18505573263654E-13));
#36181=DIRECTION('',(1.,0.,0.));
#36182=DIRECTION('center_axis',(1.,0.,0.));
#36183=DIRECTION('ref_axis',(0.,1.,1.18505573263654E-13));
#36184=DIRECTION('',(1.,0.,0.));
#36185=DIRECTION('center_axis',(1.,0.,0.));
#36186=DIRECTION('ref_axis',(0.,1.,1.18505573263654E-13));
#36187=DIRECTION('',(1.,0.,0.));
#36188=DIRECTION('center_axis',(1.,0.,0.));
#36189=DIRECTION('ref_axis',(0.,1.,1.18505573263654E-13));
#36190=DIRECTION('',(1.,0.,0.));
#36191=DIRECTION('center_axis',(1.,0.,0.));
#36192=DIRECTION('ref_axis',(0.,1.,1.18505573263654E-13));
#36193=DIRECTION('',(1.,0.,0.));
#36194=DIRECTION('center_axis',(1.,0.,0.));
#36195=DIRECTION('ref_axis',(0.,1.,1.18505573263654E-13));
#36196=DIRECTION('',(1.,0.,0.));
#36197=DIRECTION('center_axis',(1.,0.,0.));
#36198=DIRECTION('ref_axis',(0.,1.,1.18505573263654E-13));
#36199=DIRECTION('',(1.,0.,0.));
#36200=DIRECTION('center_axis',(1.,0.,0.));
#36201=DIRECTION('ref_axis',(0.,1.,1.18505573263654E-13));
#36202=DIRECTION('',(1.,0.,0.));
#36203=DIRECTION('center_axis',(1.,0.,0.));
#36204=DIRECTION('ref_axis',(0.,1.,1.18505573263654E-13));
#36205=DIRECTION('',(1.,0.,0.));
#36206=DIRECTION('center_axis',(1.,0.,0.));
#36207=DIRECTION('ref_axis',(0.,1.,1.18505573263654E-13));
#36208=DIRECTION('',(1.,0.,0.));
#36209=DIRECTION('center_axis',(1.,0.,0.));
#36210=DIRECTION('ref_axis',(0.,1.,1.18505573263654E-13));
#36211=DIRECTION('',(1.,0.,0.));
#36212=DIRECTION('center_axis',(1.,0.,0.));
#36213=DIRECTION('ref_axis',(0.,1.,1.18505573263654E-13));
#36214=DIRECTION('',(1.,0.,0.));
#36215=DIRECTION('center_axis',(1.,0.,0.));
#36216=DIRECTION('ref_axis',(0.,1.,1.18505573263654E-13));
#36217=DIRECTION('',(1.,0.,0.));
#36218=DIRECTION('center_axis',(1.,0.,0.));
#36219=DIRECTION('ref_axis',(0.,1.,1.18505573263654E-13));
#36220=DIRECTION('',(1.,0.,0.));
#36221=DIRECTION('center_axis',(1.,0.,0.));
#36222=DIRECTION('ref_axis',(0.,1.,1.18505573263654E-13));
#36223=DIRECTION('',(1.,0.,0.));
#36224=DIRECTION('center_axis',(1.,0.,0.));
#36225=DIRECTION('ref_axis',(0.,1.,1.18505573263654E-13));
#36226=DIRECTION('',(1.,0.,0.));
#36227=DIRECTION('center_axis',(1.,0.,0.));
#36228=DIRECTION('ref_axis',(0.,1.,1.18505573263654E-13));
#36229=DIRECTION('',(1.,0.,0.));
#36230=DIRECTION('center_axis',(1.,0.,0.));
#36231=DIRECTION('ref_axis',(0.,1.,1.18505573263654E-13));
#36232=DIRECTION('',(1.,0.,0.));
#36233=DIRECTION('center_axis',(1.,0.,0.));
#36234=DIRECTION('ref_axis',(0.,0.,-1.));
#36235=DIRECTION('center_axis',(1.,0.,0.));
#36236=DIRECTION('ref_axis',(0.,1.,0.));
#36237=DIRECTION('center_axis',(1.,0.,0.));
#36238=DIRECTION('ref_axis',(0.,1.,0.));
#36239=DIRECTION('center_axis',(-1.,0.,0.));
#36240=DIRECTION('ref_axis',(0.,1.,1.18505573263654E-13));
#36241=DIRECTION('center_axis',(1.,0.,0.));
#36242=DIRECTION('ref_axis',(0.,1.,1.18505573263654E-13));
#36243=DIRECTION('center_axis',(0.,-0.451966109673778,0.892035109009926));
#36244=DIRECTION('ref_axis',(0.,-0.892035109009926,-0.451966109673778));
#36245=DIRECTION('',(-1.,0.,0.));
#36246=DIRECTION('',(0.,-0.892035109009926,-0.451966109673778));
#36247=DIRECTION('',(1.,0.,0.));
#36248=DIRECTION('',(0.,-0.892035109009926,-0.451966109673778));
#36249=DIRECTION('center_axis',(1.,0.,0.));
#36250=DIRECTION('ref_axis',(0.,-0.17364817766693,-0.984807753012208));
#36251=DIRECTION('center_axis',(-1.,0.,0.));
#36252=DIRECTION('ref_axis',(0.,1.,0.));
#36253=DIRECTION('',(0.,0.68365729580961,-0.729803193940867));
#36254=DIRECTION('center_axis',(0.,-0.729803193940867,-0.683657295809611));
#36255=DIRECTION('ref_axis',(0.,0.68365729580961,-0.729803193940867));
#36256=DIRECTION('',(1.,0.,0.));
#36257=DIRECTION('',(0.,0.68365729580961,-0.729803193940867));
#36258=DIRECTION('center_axis',(1.,0.,0.));
#36259=DIRECTION('ref_axis',(0.,-0.17364817766693,-0.984807753012208));
#36260=DIRECTION('center_axis',(1.,0.,0.));
#36261=DIRECTION('ref_axis',(0.,1.,0.));
#36262=DIRECTION('center_axis',(0.,-0.290199457811006,0.956966182624129));
#36263=DIRECTION('ref_axis',(0.,-0.956966182624129,-0.290199457811006));
#36264=DIRECTION('',(-1.,0.,0.));
#36265=DIRECTION('',(0.,-0.956966182624129,-0.290199457811006));
#36266=DIRECTION('',(1.,0.,0.));
#36267=DIRECTION('',(0.,-0.956966182624129,-0.290199457811006));
#36268=DIRECTION('center_axis',(1.,0.,0.));
#36269=DIRECTION('ref_axis',(0.,-0.342020143325669,-0.939692620785908));
#36270=DIRECTION('center_axis',(-1.,0.,0.));
#36271=DIRECTION('ref_axis',(0.,1.,0.));
#36272=DIRECTION('',(0.,0.546542010633327,-0.837431687132079));
#36273=DIRECTION('center_axis',(0.,-0.837431687132079,-0.546542010633327));
#36274=DIRECTION('ref_axis',(0.,0.546542010633327,-0.837431687132079));
#36275=DIRECTION('',(1.,0.,0.));
#36276=DIRECTION('',(0.,0.546542010633327,-0.837431687132079));
#36277=DIRECTION('center_axis',(1.,0.,0.));
#36278=DIRECTION('ref_axis',(0.,-0.342020143325669,-0.939692620785908));
#36279=DIRECTION('center_axis',(1.,0.,0.));
#36280=DIRECTION('ref_axis',(0.,1.,0.));
#36281=DIRECTION('center_axis',(0.,-0.11961524227066,0.992820323027551));
#36282=DIRECTION('ref_axis',(0.,-0.992820323027551,-0.11961524227066));
#36283=DIRECTION('',(-1.,0.,0.));
#36284=DIRECTION('',(0.,-0.992820323027551,-0.11961524227066));
#36285=DIRECTION('',(1.,0.,0.));
#36286=DIRECTION('',(0.,-0.992820323027551,-0.11961524227066));
#36287=DIRECTION('center_axis',(1.,0.,0.));
#36288=DIRECTION('ref_axis',(0.,-0.5,-0.866025403784438));
#36289=DIRECTION('center_axis',(-1.,0.,0.));
#36290=DIRECTION('ref_axis',(0.,1.,0.));
#36291=DIRECTION('',(0.,0.392820323027553,-0.919615242270662));
#36292=DIRECTION('center_axis',(0.,-0.919615242270662,-0.392820323027553));
#36293=DIRECTION('ref_axis',(0.,0.392820323027553,-0.919615242270662));
#36294=DIRECTION('',(1.,0.,0.));
#36295=DIRECTION('',(0.,0.392820323027553,-0.919615242270662));
#36296=DIRECTION('center_axis',(1.,0.,0.));
#36297=DIRECTION('ref_axis',(0.,-0.5,-0.866025403784438));
#36298=DIRECTION('center_axis',(1.,0.,0.));
#36299=DIRECTION('ref_axis',(0.,1.,0.));
#36300=DIRECTION('center_axis',(0.,0.0546034218778482,0.998508120307106));
#36301=DIRECTION('ref_axis',(0.,-0.998508120307106,0.0546034218778482));
#36302=DIRECTION('',(-1.,0.,0.));
#36303=DIRECTION('',(0.,-0.998508120307106,0.0546034218778482));
#36304=DIRECTION('',(1.,0.,0.));
#36305=DIRECTION('',(0.,-0.998508120307106,0.0546034218778482));
#36306=DIRECTION('center_axis',(1.,0.,0.));
#36307=DIRECTION('ref_axis',(0.,-0.64278760968654,-0.766044443118978));
#36308=DIRECTION('center_axis',(-1.,0.,0.));
#36309=DIRECTION('ref_axis',(0.,1.,0.));
#36310=DIRECTION('',(0.,0.227162988683261,-0.973856753620618));
#36311=DIRECTION('center_axis',(0.,-0.973856753620618,-0.227162988683262));
#36312=DIRECTION('ref_axis',(0.,0.227162988683261,-0.973856753620618));
#36313=DIRECTION('',(1.,0.,0.));
#36314=DIRECTION('',(0.,0.227162988683261,-0.973856753620618));
#36315=DIRECTION('center_axis',(1.,0.,0.));
#36316=DIRECTION('ref_axis',(0.,-0.64278760968654,-0.766044443118978));
#36317=DIRECTION('center_axis',(1.,0.,0.));
#36318=DIRECTION('ref_axis',(0.,1.,0.));
#36319=DIRECTION('center_axis',(0.,0.227162988683262,0.973856753620618));
#36320=DIRECTION('ref_axis',(0.,-0.973856753620618,0.227162988683262));
#36321=DIRECTION('',(-1.,0.,0.));
#36322=DIRECTION('',(0.,-0.973856753620618,0.227162988683262));
#36323=DIRECTION('',(1.,0.,0.));
#36324=DIRECTION('',(0.,-0.973856753620618,0.227162988683262));
#36325=DIRECTION('center_axis',(1.,0.,0.));
#36326=DIRECTION('ref_axis',(0.,-0.766044443118978,-0.642787609686539));
#36327=DIRECTION('center_axis',(-1.,0.,0.));
#36328=DIRECTION('ref_axis',(0.,1.,0.));
#36329=DIRECTION('',(0.,0.0546034218778476,-0.998508120307106));
#36330=DIRECTION('center_axis',(0.,-0.998508120307106,-0.0546034218778476));
#36331=DIRECTION('ref_axis',(0.,0.0546034218778476,-0.998508120307106));
#36332=DIRECTION('',(1.,0.,0.));
#36333=DIRECTION('',(0.,0.0546034218778476,-0.998508120307106));
#36334=DIRECTION('center_axis',(1.,0.,0.));
#36335=DIRECTION('ref_axis',(0.,-0.766044443118978,-0.642787609686539));
#36336=DIRECTION('center_axis',(1.,0.,0.));
#36337=DIRECTION('ref_axis',(0.,1.,0.));
#36338=DIRECTION('center_axis',(0.,0.392820323027554,0.919615242270662));
#36339=DIRECTION('ref_axis',(0.,-0.919615242270662,0.392820323027554));
#36340=DIRECTION('',(-1.,0.,0.));
#36341=DIRECTION('',(0.,-0.919615242270662,0.392820323027554));
#36342=DIRECTION('',(1.,0.,0.));
#36343=DIRECTION('',(0.,-0.919615242270662,0.392820323027554));
#36344=DIRECTION('center_axis',(1.,0.,0.));
#36345=DIRECTION('ref_axis',(0.,-0.866025403784439,-0.5));
#36346=DIRECTION('center_axis',(-1.,0.,0.));
#36347=DIRECTION('ref_axis',(0.,1.,0.));
#36348=DIRECTION('',(0.,-0.11961524227066,-0.992820323027551));
#36349=DIRECTION('center_axis',(0.,-0.992820323027551,0.11961524227066));
#36350=DIRECTION('ref_axis',(0.,-0.11961524227066,-0.992820323027551));
#36351=DIRECTION('',(1.,0.,0.));
#36352=DIRECTION('',(0.,-0.11961524227066,-0.992820323027551));
#36353=DIRECTION('center_axis',(1.,0.,0.));
#36354=DIRECTION('ref_axis',(0.,-0.866025403784439,-0.5));
#36355=DIRECTION('center_axis',(1.,0.,0.));
#36356=DIRECTION('ref_axis',(0.,1.,0.));
#36357=DIRECTION('center_axis',(0.,0.546542010633329,0.837431687132078));
#36358=DIRECTION('ref_axis',(0.,-0.837431687132078,0.546542010633329));
#36359=DIRECTION('',(-1.,0.,0.));
#36360=DIRECTION('',(0.,-0.837431687132078,0.546542010633329));
#36361=DIRECTION('',(1.,0.,0.));
#36362=DIRECTION('',(0.,-0.837431687132078,0.546542010633329));
#36363=DIRECTION('center_axis',(1.,0.,0.));
#36364=DIRECTION('ref_axis',(0.,-0.939692620785909,-0.342020143325668));
#36365=DIRECTION('center_axis',(-1.,0.,0.));
#36366=DIRECTION('ref_axis',(0.,1.,0.));
#36367=DIRECTION('',(0.,-0.290199457811008,-0.956966182624129));
#36368=DIRECTION('center_axis',(0.,-0.956966182624129,0.290199457811008));
#36369=DIRECTION('ref_axis',(0.,-0.290199457811008,-0.956966182624129));
#36370=DIRECTION('',(1.,0.,0.));
#36371=DIRECTION('',(0.,-0.290199457811008,-0.956966182624129));
#36372=DIRECTION('center_axis',(1.,0.,0.));
#36373=DIRECTION('ref_axis',(0.,-0.939692620785909,-0.342020143325668));
#36374=DIRECTION('center_axis',(1.,0.,0.));
#36375=DIRECTION('ref_axis',(0.,1.,0.));
#36376=DIRECTION('center_axis',(0.,0.683657295809611,0.729803193940867));
#36377=DIRECTION('ref_axis',(0.,-0.729803193940867,0.683657295809611));
#36378=DIRECTION('',(-1.,0.,0.));
#36379=DIRECTION('',(0.,-0.729803193940867,0.683657295809611));
#36380=DIRECTION('',(1.,0.,0.));
#36381=DIRECTION('',(0.,-0.729803193940867,0.683657295809611));
#36382=DIRECTION('center_axis',(1.,0.,0.));
#36383=DIRECTION('ref_axis',(0.,-0.984807753012208,-0.17364817766693));
#36384=DIRECTION('center_axis',(-1.,0.,0.));
#36385=DIRECTION('ref_axis',(0.,1.,0.));
#36386=DIRECTION('',(0.,-0.451966109673778,-0.892035109009926));
#36387=DIRECTION('center_axis',(0.,-0.892035109009926,0.451966109673778));
#36388=DIRECTION('ref_axis',(0.,-0.451966109673778,-0.892035109009926));
#36389=DIRECTION('',(1.,0.,0.));
#36390=DIRECTION('',(0.,-0.451966109673778,-0.892035109009926));
#36391=DIRECTION('center_axis',(1.,0.,0.));
#36392=DIRECTION('ref_axis',(0.,-0.984807753012208,-0.17364817766693));
#36393=DIRECTION('center_axis',(1.,0.,0.));
#36394=DIRECTION('ref_axis',(0.,1.,0.));
#36395=DIRECTION('center_axis',(0.,0.800000000000002,0.599999999999997));
#36396=DIRECTION('ref_axis',(0.,-0.599999999999997,0.800000000000002));
#36397=DIRECTION('',(-1.,0.,0.));
#36398=DIRECTION('',(0.,-0.599999999999997,0.800000000000002));
#36399=DIRECTION('',(1.,0.,0.));
#36400=DIRECTION('',(0.,-0.599999999999997,0.800000000000002));
#36401=DIRECTION('center_axis',(1.,0.,0.));
#36402=DIRECTION('ref_axis',(0.,-1.,1.83697019872103E-16));
#36403=DIRECTION('center_axis',(-1.,0.,0.));
#36404=DIRECTION('ref_axis',(0.,1.,0.));
#36405=DIRECTION('',(0.,-0.599999999999998,-0.800000000000002));
#36406=DIRECTION('center_axis',(0.,-0.800000000000002,0.599999999999998));
#36407=DIRECTION('ref_axis',(0.,-0.599999999999998,-0.800000000000002));
#36408=DIRECTION('',(1.,0.,0.));
#36409=DIRECTION('',(0.,-0.599999999999998,-0.800000000000002));
#36410=DIRECTION('center_axis',(1.,0.,0.));
#36411=DIRECTION('ref_axis',(0.,-1.,1.83697019872103E-16));
#36412=DIRECTION('center_axis',(1.,0.,0.));
#36413=DIRECTION('ref_axis',(0.,1.,0.));
#36414=DIRECTION('center_axis',(0.,0.892035109009926,0.451966109673778));
#36415=DIRECTION('ref_axis',(0.,-0.451966109673778,0.892035109009926));
#36416=DIRECTION('',(-1.,0.,0.));
#36417=DIRECTION('',(0.,-0.451966109673778,0.892035109009926));
#36418=DIRECTION('',(1.,0.,0.));
#36419=DIRECTION('',(0.,-0.451966109673778,0.892035109009926));
#36420=DIRECTION('center_axis',(1.,0.,0.));
#36421=DIRECTION('ref_axis',(0.,-0.984807753012208,0.17364817766693));
#36422=DIRECTION('center_axis',(-1.,0.,0.));
#36423=DIRECTION('ref_axis',(0.,1.,0.));
#36424=DIRECTION('',(0.,-0.729803193940867,-0.683657295809611));
#36425=DIRECTION('center_axis',(0.,-0.683657295809611,0.729803193940867));
#36426=DIRECTION('ref_axis',(0.,-0.729803193940867,-0.683657295809611));
#36427=DIRECTION('',(1.,0.,0.));
#36428=DIRECTION('',(0.,-0.729803193940867,-0.683657295809611));
#36429=DIRECTION('center_axis',(1.,0.,0.));
#36430=DIRECTION('ref_axis',(0.,-0.984807753012208,0.17364817766693));
#36431=DIRECTION('center_axis',(1.,0.,0.));
#36432=DIRECTION('ref_axis',(0.,1.,0.));
#36433=DIRECTION('center_axis',(0.,0.956966182624129,0.290199457811006));
#36434=DIRECTION('ref_axis',(0.,-0.290199457811006,0.956966182624129));
#36435=DIRECTION('',(-1.,0.,0.));
#36436=DIRECTION('',(0.,-0.290199457811006,0.956966182624129));
#36437=DIRECTION('',(1.,0.,0.));
#36438=DIRECTION('',(0.,-0.290199457811006,0.956966182624129));
#36439=DIRECTION('center_axis',(1.,0.,0.));
#36440=DIRECTION('ref_axis',(0.,-0.939692620785908,0.342020143325669));
#36441=DIRECTION('center_axis',(-1.,0.,0.));
#36442=DIRECTION('ref_axis',(0.,1.,0.));
#36443=DIRECTION('',(0.,-0.837431687132079,-0.546542010633328));
#36444=DIRECTION('center_axis',(0.,-0.546542010633328,0.837431687132079));
#36445=DIRECTION('ref_axis',(0.,-0.837431687132079,-0.546542010633328));
#36446=DIRECTION('',(1.,0.,0.));
#36447=DIRECTION('',(0.,-0.837431687132079,-0.546542010633328));
#36448=DIRECTION('center_axis',(1.,0.,0.));
#36449=DIRECTION('ref_axis',(0.,-0.939692620785908,0.342020143325669));
#36450=DIRECTION('center_axis',(1.,0.,0.));
#36451=DIRECTION('ref_axis',(0.,1.,0.));
#36452=DIRECTION('center_axis',(0.,0.992820323027551,0.11961524227066));
#36453=DIRECTION('ref_axis',(0.,-0.11961524227066,0.992820323027551));
#36454=DIRECTION('',(-1.,0.,0.));
#36455=DIRECTION('',(0.,-0.11961524227066,0.992820323027551));
#36456=DIRECTION('',(1.,0.,0.));
#36457=DIRECTION('',(0.,-0.11961524227066,0.992820323027551));
#36458=DIRECTION('center_axis',(1.,0.,0.));
#36459=DIRECTION('ref_axis',(0.,-0.866025403784438,0.5));
#36460=DIRECTION('center_axis',(-1.,0.,0.));
#36461=DIRECTION('ref_axis',(0.,1.,0.));
#36462=DIRECTION('',(0.,-0.919615242270662,-0.392820323027553));
#36463=DIRECTION('center_axis',(0.,-0.392820323027553,0.919615242270662));
#36464=DIRECTION('ref_axis',(0.,-0.919615242270662,-0.392820323027553));
#36465=DIRECTION('',(1.,0.,0.));
#36466=DIRECTION('',(0.,-0.919615242270662,-0.392820323027553));
#36467=DIRECTION('center_axis',(1.,0.,0.));
#36468=DIRECTION('ref_axis',(0.,-0.866025403784438,0.5));
#36469=DIRECTION('center_axis',(1.,0.,0.));
#36470=DIRECTION('ref_axis',(0.,1.,0.));
#36471=DIRECTION('center_axis',(0.,0.998508120307106,-0.054603421877848));
#36472=DIRECTION('ref_axis',(0.,0.054603421877848,0.998508120307106));
#36473=DIRECTION('',(-1.,0.,0.));
#36474=DIRECTION('',(0.,0.054603421877848,0.998508120307106));
#36475=DIRECTION('',(1.,0.,0.));
#36476=DIRECTION('',(0.,0.054603421877848,0.998508120307106));
#36477=DIRECTION('center_axis',(1.,0.,0.));
#36478=DIRECTION('ref_axis',(0.,-0.766044443118978,0.642787609686539));
#36479=DIRECTION('center_axis',(-1.,0.,0.));
#36480=DIRECTION('ref_axis',(0.,1.,0.));
#36481=DIRECTION('',(0.,-0.973856753620618,-0.227162988683262));
#36482=DIRECTION('center_axis',(0.,-0.227162988683262,0.973856753620618));
#36483=DIRECTION('ref_axis',(0.,-0.973856753620618,-0.227162988683262));
#36484=DIRECTION('',(1.,0.,0.));
#36485=DIRECTION('',(0.,-0.973856753620618,-0.227162988683262));
#36486=DIRECTION('center_axis',(1.,0.,0.));
#36487=DIRECTION('ref_axis',(0.,-0.766044443118978,0.642787609686539));
#36488=DIRECTION('center_axis',(1.,0.,0.));
#36489=DIRECTION('ref_axis',(0.,1.,0.));
#36490=DIRECTION('center_axis',(0.,0.973856753620618,-0.227162988683262));
#36491=DIRECTION('ref_axis',(0.,0.227162988683262,0.973856753620618));
#36492=DIRECTION('',(-1.,0.,0.));
#36493=DIRECTION('',(0.,0.227162988683262,0.973856753620618));
#36494=DIRECTION('',(1.,0.,0.));
#36495=DIRECTION('',(0.,0.227162988683262,0.973856753620618));
#36496=DIRECTION('center_axis',(1.,0.,0.));
#36497=DIRECTION('ref_axis',(0.,-0.642787609686539,0.766044443118978));
#36498=DIRECTION('center_axis',(-1.,0.,0.));
#36499=DIRECTION('ref_axis',(0.,1.,0.));
#36500=DIRECTION('',(0.,-0.998508120307106,-0.0546034218778477));
#36501=DIRECTION('center_axis',(0.,-0.0546034218778477,0.998508120307106));
#36502=DIRECTION('ref_axis',(0.,-0.998508120307106,-0.0546034218778477));
#36503=DIRECTION('',(1.,0.,0.));
#36504=DIRECTION('',(0.,-0.998508120307106,-0.0546034218778477));
#36505=DIRECTION('center_axis',(1.,0.,0.));
#36506=DIRECTION('ref_axis',(0.,-0.642787609686539,0.766044443118978));
#36507=DIRECTION('center_axis',(1.,0.,0.));
#36508=DIRECTION('ref_axis',(0.,1.,0.));
#36509=DIRECTION('center_axis',(0.,0.919615242270662,-0.392820323027554));
#36510=DIRECTION('ref_axis',(0.,0.392820323027554,0.919615242270662));
#36511=DIRECTION('',(-1.,0.,0.));
#36512=DIRECTION('',(0.,0.392820323027554,0.919615242270662));
#36513=DIRECTION('',(1.,0.,0.));
#36514=DIRECTION('',(0.,0.392820323027554,0.919615242270662));
#36515=DIRECTION('center_axis',(1.,0.,0.));
#36516=DIRECTION('ref_axis',(0.,-0.5,0.866025403784439));
#36517=DIRECTION('center_axis',(-1.,0.,0.));
#36518=DIRECTION('ref_axis',(0.,1.,0.));
#36519=DIRECTION('',(0.,-0.992820323027551,0.11961524227066));
#36520=DIRECTION('center_axis',(0.,0.11961524227066,0.992820323027551));
#36521=DIRECTION('ref_axis',(0.,-0.992820323027551,0.11961524227066));
#36522=DIRECTION('',(1.,0.,0.));
#36523=DIRECTION('',(0.,-0.992820323027551,0.11961524227066));
#36524=DIRECTION('center_axis',(1.,0.,0.));
#36525=DIRECTION('ref_axis',(0.,-0.5,0.866025403784439));
#36526=DIRECTION('center_axis',(1.,0.,0.));
#36527=DIRECTION('ref_axis',(0.,1.,0.));
#36528=DIRECTION('center_axis',(0.,0.837431687132078,-0.546542010633328));
#36529=DIRECTION('ref_axis',(0.,0.546542010633328,0.837431687132078));
#36530=DIRECTION('',(-1.,0.,0.));
#36531=DIRECTION('',(0.,0.546542010633328,0.837431687132078));
#36532=DIRECTION('',(1.,0.,0.));
#36533=DIRECTION('',(0.,0.546542010633328,0.837431687132078));
#36534=DIRECTION('center_axis',(1.,0.,0.));
#36535=DIRECTION('ref_axis',(0.,-0.342020143325669,0.939692620785909));
#36536=DIRECTION('center_axis',(-1.,0.,0.));
#36537=DIRECTION('ref_axis',(0.,1.,0.));
#36538=DIRECTION('',(0.,-0.956966182624129,0.290199457811007));
#36539=DIRECTION('center_axis',(0.,0.290199457811007,0.956966182624129));
#36540=DIRECTION('ref_axis',(0.,-0.956966182624129,0.290199457811007));
#36541=DIRECTION('',(1.,0.,0.));
#36542=DIRECTION('',(0.,-0.956966182624129,0.290199457811007));
#36543=DIRECTION('center_axis',(1.,0.,0.));
#36544=DIRECTION('ref_axis',(0.,-0.342020143325669,0.939692620785909));
#36545=DIRECTION('center_axis',(1.,0.,0.));
#36546=DIRECTION('ref_axis',(0.,1.,0.));
#36547=DIRECTION('center_axis',(0.,0.729803193940867,-0.683657295809611));
#36548=DIRECTION('ref_axis',(0.,0.683657295809611,0.729803193940867));
#36549=DIRECTION('',(-1.,0.,0.));
#36550=DIRECTION('',(0.,0.683657295809611,0.729803193940867));
#36551=DIRECTION('',(1.,0.,0.));
#36552=DIRECTION('',(0.,0.683657295809611,0.729803193940867));
#36553=DIRECTION('center_axis',(1.,0.,0.));
#36554=DIRECTION('ref_axis',(0.,-0.17364817766693,0.984807753012208));
#36555=DIRECTION('center_axis',(-1.,0.,0.));
#36556=DIRECTION('ref_axis',(0.,1.,0.));
#36557=DIRECTION('',(0.,-0.892035109009926,0.451966109673778));
#36558=DIRECTION('center_axis',(0.,0.451966109673778,0.892035109009926));
#36559=DIRECTION('ref_axis',(0.,-0.892035109009926,0.451966109673778));
#36560=DIRECTION('',(1.,0.,0.));
#36561=DIRECTION('',(0.,-0.892035109009926,0.451966109673778));
#36562=DIRECTION('center_axis',(1.,0.,0.));
#36563=DIRECTION('ref_axis',(0.,-0.17364817766693,0.984807753012208));
#36564=DIRECTION('center_axis',(1.,0.,0.));
#36565=DIRECTION('ref_axis',(0.,1.,0.));
#36566=DIRECTION('center_axis',(0.,0.599999999999997,-0.800000000000002));
#36567=DIRECTION('ref_axis',(0.,0.800000000000002,0.599999999999997));
#36568=DIRECTION('',(-1.,0.,0.));
#36569=DIRECTION('',(0.,0.800000000000002,0.599999999999997));
#36570=DIRECTION('',(1.,0.,0.));
#36571=DIRECTION('',(0.,0.800000000000002,0.599999999999997));
#36572=DIRECTION('center_axis',(1.,0.,0.));
#36573=DIRECTION('ref_axis',(0.,1.22464679914735E-16,1.));
#36574=DIRECTION('center_axis',(-1.,0.,0.));
#36575=DIRECTION('ref_axis',(0.,1.,0.));
#36576=DIRECTION('',(0.,-0.800000000000002,0.599999999999998));
#36577=DIRECTION('center_axis',(-1.,0.,0.));
#36578=DIRECTION('ref_axis',(0.,1.,0.));
#36579=DIRECTION('center_axis',(0.,0.599999999999998,0.800000000000002));
#36580=DIRECTION('ref_axis',(0.,-0.800000000000002,0.599999999999998));
#36581=DIRECTION('',(1.,0.,0.));
#36582=DIRECTION('',(0.,-0.800000000000002,0.599999999999998));
#36583=DIRECTION('center_axis',(1.,0.,0.));
#36584=DIRECTION('ref_axis',(0.,1.22464679914735E-16,1.));
#36585=DIRECTION('center_axis',(1.,0.,0.));
#36586=DIRECTION('ref_axis',(0.,1.,0.));
#36587=DIRECTION('center_axis',(1.,0.,0.));
#36588=DIRECTION('ref_axis',(0.,1.,0.));
#36589=DIRECTION('center_axis',(0.,0.451966109673778,-0.892035109009926));
#36590=DIRECTION('ref_axis',(0.,0.892035109009926,0.451966109673777));
#36591=DIRECTION('',(-1.,0.,0.));
#36592=DIRECTION('',(0.,0.892035109009926,0.451966109673777));
#36593=DIRECTION('',(1.,0.,0.));
#36594=DIRECTION('',(0.,0.892035109009926,0.451966109673777));
#36595=DIRECTION('center_axis',(1.,0.,0.));
#36596=DIRECTION('ref_axis',(0.,0.173648177666931,0.984807753012208));
#36597=DIRECTION('center_axis',(-1.,0.,0.));
#36598=DIRECTION('ref_axis',(0.,1.,0.));
#36599=DIRECTION('',(0.,-0.68365729580961,0.729803193940867));
#36600=DIRECTION('center_axis',(0.,0.729803193940867,0.68365729580961));
#36601=DIRECTION('ref_axis',(0.,-0.68365729580961,0.729803193940867));
#36602=DIRECTION('',(1.,0.,0.));
#36603=DIRECTION('',(0.,-0.68365729580961,0.729803193940867));
#36604=DIRECTION('center_axis',(1.,0.,0.));
#36605=DIRECTION('ref_axis',(0.,0.173648177666931,0.984807753012208));
#36606=DIRECTION('center_axis',(1.,0.,0.));
#36607=DIRECTION('ref_axis',(0.,1.,0.));
#36608=DIRECTION('center_axis',(0.,0.290199457811007,-0.956966182624129));
#36609=DIRECTION('ref_axis',(0.,0.956966182624129,0.290199457811007));
#36610=DIRECTION('',(-1.,0.,0.));
#36611=DIRECTION('',(0.,0.956966182624129,0.290199457811007));
#36612=DIRECTION('',(1.,0.,0.));
#36613=DIRECTION('',(0.,0.956966182624129,0.290199457811007));
#36614=DIRECTION('center_axis',(1.,0.,0.));
#36615=DIRECTION('ref_axis',(0.,0.342020143325669,0.939692620785908));
#36616=DIRECTION('center_axis',(-1.,0.,0.));
#36617=DIRECTION('ref_axis',(0.,1.,0.));
#36618=DIRECTION('',(0.,-0.546542010633328,0.837431687132078));
#36619=DIRECTION('center_axis',(0.,0.837431687132078,0.546542010633328));
#36620=DIRECTION('ref_axis',(0.,-0.546542010633328,0.837431687132078));
#36621=DIRECTION('',(1.,0.,0.));
#36622=DIRECTION('',(0.,-0.546542010633328,0.837431687132078));
#36623=DIRECTION('center_axis',(1.,0.,0.));
#36624=DIRECTION('ref_axis',(0.,0.342020143325669,0.939692620785908));
#36625=DIRECTION('center_axis',(1.,0.,0.));
#36626=DIRECTION('ref_axis',(0.,1.,0.));
#36627=DIRECTION('center_axis',(0.,0.11961524227066,-0.992820323027551));
#36628=DIRECTION('ref_axis',(0.,0.992820323027551,0.11961524227066));
#36629=DIRECTION('',(-1.,0.,0.));
#36630=DIRECTION('',(0.,0.992820323027551,0.11961524227066));
#36631=DIRECTION('',(1.,0.,0.));
#36632=DIRECTION('',(0.,0.992820323027551,0.11961524227066));
#36633=DIRECTION('center_axis',(1.,0.,0.));
#36634=DIRECTION('ref_axis',(0.,0.5,0.866025403784439));
#36635=DIRECTION('center_axis',(-1.,0.,0.));
#36636=DIRECTION('ref_axis',(0.,1.,0.));
#36637=DIRECTION('',(0.,-0.392820323027554,0.919615242270662));
#36638=DIRECTION('center_axis',(0.,0.919615242270662,0.392820323027554));
#36639=DIRECTION('ref_axis',(0.,-0.392820323027554,0.919615242270662));
#36640=DIRECTION('',(1.,0.,0.));
#36641=DIRECTION('',(0.,-0.392820323027554,0.919615242270662));
#36642=DIRECTION('center_axis',(1.,0.,0.));
#36643=DIRECTION('ref_axis',(0.,0.5,0.866025403784439));
#36644=DIRECTION('center_axis',(1.,0.,0.));
#36645=DIRECTION('ref_axis',(0.,1.,0.));
#36646=DIRECTION('center_axis',(0.,-0.054603421877848,-0.998508120307106));
#36647=DIRECTION('ref_axis',(0.,0.998508120307106,-0.054603421877848));
#36648=DIRECTION('',(-1.,0.,0.));
#36649=DIRECTION('',(0.,0.998508120307106,-0.054603421877848));
#36650=DIRECTION('',(1.,0.,0.));
#36651=DIRECTION('',(0.,0.998508120307106,-0.054603421877848));
#36652=DIRECTION('center_axis',(1.,0.,0.));
#36653=DIRECTION('ref_axis',(0.,0.642787609686539,0.766044443118978));
#36654=DIRECTION('center_axis',(-1.,0.,0.));
#36655=DIRECTION('ref_axis',(0.,1.,0.));
#36656=DIRECTION('',(0.,-0.227162988683262,0.973856753620618));
#36657=DIRECTION('center_axis',(0.,0.973856753620618,0.227162988683262));
#36658=DIRECTION('ref_axis',(0.,-0.227162988683262,0.973856753620618));
#36659=DIRECTION('',(1.,0.,0.));
#36660=DIRECTION('',(0.,-0.227162988683262,0.973856753620618));
#36661=DIRECTION('center_axis',(1.,0.,0.));
#36662=DIRECTION('ref_axis',(0.,0.642787609686539,0.766044443118978));
#36663=DIRECTION('center_axis',(1.,0.,0.));
#36664=DIRECTION('ref_axis',(0.,1.,0.));
#36665=DIRECTION('center_axis',(0.,-0.227162988683262,-0.973856753620618));
#36666=DIRECTION('ref_axis',(0.,0.973856753620618,-0.227162988683262));
#36667=DIRECTION('',(-1.,0.,0.));
#36668=DIRECTION('',(0.,0.973856753620618,-0.227162988683262));
#36669=DIRECTION('',(1.,0.,0.));
#36670=DIRECTION('',(0.,0.973856753620618,-0.227162988683262));
#36671=DIRECTION('center_axis',(1.,0.,0.));
#36672=DIRECTION('ref_axis',(0.,0.766044443118978,0.642787609686539));
#36673=DIRECTION('center_axis',(-1.,0.,0.));
#36674=DIRECTION('ref_axis',(0.,1.,0.));
#36675=DIRECTION('',(0.,-0.0546034218778478,0.998508120307106));
#36676=DIRECTION('center_axis',(0.,0.998508120307106,0.0546034218778478));
#36677=DIRECTION('ref_axis',(0.,-0.0546034218778478,0.998508120307106));
#36678=DIRECTION('',(1.,0.,0.));
#36679=DIRECTION('',(0.,-0.0546034218778478,0.998508120307106));
#36680=DIRECTION('center_axis',(1.,0.,0.));
#36681=DIRECTION('ref_axis',(0.,0.766044443118978,0.642787609686539));
#36682=DIRECTION('center_axis',(1.,0.,0.));
#36683=DIRECTION('ref_axis',(0.,1.,0.));
#36684=DIRECTION('center_axis',(0.,-0.392820323027554,-0.919615242270662));
#36685=DIRECTION('ref_axis',(0.,0.919615242270662,-0.392820323027554));
#36686=DIRECTION('',(-1.,0.,0.));
#36687=DIRECTION('',(0.,0.919615242270662,-0.392820323027554));
#36688=DIRECTION('',(1.,0.,0.));
#36689=DIRECTION('',(0.,0.919615242270662,-0.392820323027554));
#36690=DIRECTION('center_axis',(1.,0.,0.));
#36691=DIRECTION('ref_axis',(0.,0.866025403784439,0.5));
#36692=DIRECTION('center_axis',(-1.,0.,0.));
#36693=DIRECTION('ref_axis',(0.,1.,0.));
#36694=DIRECTION('',(0.,0.11961524227066,0.992820323027551));
#36695=DIRECTION('center_axis',(0.,0.992820323027551,-0.11961524227066));
#36696=DIRECTION('ref_axis',(0.,0.11961524227066,0.992820323027551));
#36697=DIRECTION('',(1.,0.,0.));
#36698=DIRECTION('',(0.,0.11961524227066,0.992820323027551));
#36699=DIRECTION('center_axis',(1.,0.,0.));
#36700=DIRECTION('ref_axis',(0.,0.866025403784439,0.5));
#36701=DIRECTION('center_axis',(1.,0.,0.));
#36702=DIRECTION('ref_axis',(0.,1.,0.));
#36703=DIRECTION('center_axis',(0.,-0.546542010633328,-0.837431687132078));
#36704=DIRECTION('ref_axis',(0.,0.837431687132078,-0.546542010633328));
#36705=DIRECTION('',(-1.,0.,0.));
#36706=DIRECTION('',(0.,0.837431687132078,-0.546542010633328));
#36707=DIRECTION('',(1.,0.,0.));
#36708=DIRECTION('',(0.,0.837431687132078,-0.546542010633328));
#36709=DIRECTION('center_axis',(1.,0.,0.));
#36710=DIRECTION('ref_axis',(0.,0.939692620785908,0.342020143325669));
#36711=DIRECTION('center_axis',(-1.,0.,0.));
#36712=DIRECTION('ref_axis',(0.,1.,0.));
#36713=DIRECTION('',(0.,0.290199457811007,0.956966182624129));
#36714=DIRECTION('center_axis',(0.,0.956966182624129,-0.290199457811007));
#36715=DIRECTION('ref_axis',(0.,0.290199457811007,0.956966182624129));
#36716=DIRECTION('',(1.,0.,0.));
#36717=DIRECTION('',(0.,0.290199457811007,0.956966182624129));
#36718=DIRECTION('center_axis',(1.,0.,0.));
#36719=DIRECTION('ref_axis',(0.,0.939692620785908,0.342020143325669));
#36720=DIRECTION('center_axis',(1.,0.,0.));
#36721=DIRECTION('ref_axis',(0.,1.,0.));
#36722=DIRECTION('center_axis',(0.,-0.683657295809611,-0.729803193940867));
#36723=DIRECTION('ref_axis',(0.,0.729803193940867,-0.683657295809611));
#36724=DIRECTION('',(-1.,0.,0.));
#36725=DIRECTION('',(0.,0.729803193940867,-0.683657295809611));
#36726=DIRECTION('',(1.,0.,0.));
#36727=DIRECTION('',(0.,0.729803193940867,-0.683657295809611));
#36728=DIRECTION('center_axis',(1.,0.,0.));
#36729=DIRECTION('ref_axis',(0.,0.984807753012208,0.17364817766693));
#36730=DIRECTION('center_axis',(-1.,0.,0.));
#36731=DIRECTION('ref_axis',(0.,1.,0.));
#36732=DIRECTION('',(0.,0.451966109673778,0.892035109009926));
#36733=DIRECTION('center_axis',(0.,0.892035109009926,-0.451966109673778));
#36734=DIRECTION('ref_axis',(0.,0.451966109673778,0.892035109009926));
#36735=DIRECTION('',(1.,0.,0.));
#36736=DIRECTION('',(0.,0.451966109673778,0.892035109009926));
#36737=DIRECTION('center_axis',(1.,0.,0.));
#36738=DIRECTION('ref_axis',(0.,0.984807753012208,0.17364817766693));
#36739=DIRECTION('center_axis',(1.,0.,0.));
#36740=DIRECTION('ref_axis',(0.,1.,0.));
#36741=DIRECTION('center_axis',(0.,-0.800000000000002,-0.599999999999998));
#36742=DIRECTION('ref_axis',(0.,0.599999999999998,-0.800000000000002));
#36743=DIRECTION('',(-1.,0.,0.));
#36744=DIRECTION('',(0.,0.599999999999998,-0.800000000000002));
#36745=DIRECTION('',(1.,0.,0.));
#36746=DIRECTION('',(0.,0.599999999999998,-0.800000000000002));
#36747=DIRECTION('center_axis',(1.,0.,0.));
#36748=DIRECTION('ref_axis',(0.,1.,-6.12323399573677E-17));
#36749=DIRECTION('center_axis',(-1.,0.,0.));
#36750=DIRECTION('ref_axis',(0.,1.,0.));
#36751=DIRECTION('',(0.,0.599999999999998,0.800000000000002));
#36752=DIRECTION('center_axis',(0.,0.800000000000002,-0.599999999999998));
#36753=DIRECTION('ref_axis',(0.,0.599999999999998,0.800000000000002));
#36754=DIRECTION('',(1.,0.,0.));
#36755=DIRECTION('',(0.,0.599999999999998,0.800000000000002));
#36756=DIRECTION('center_axis',(1.,0.,0.));
#36757=DIRECTION('ref_axis',(0.,1.,-6.12323399573677E-17));
#36758=DIRECTION('center_axis',(1.,0.,0.));
#36759=DIRECTION('ref_axis',(0.,1.,0.));
#36760=DIRECTION('center_axis',(0.,-0.892035109009926,-0.451966109673778));
#36761=DIRECTION('ref_axis',(0.,0.451966109673778,-0.892035109009926));
#36762=DIRECTION('',(-1.,0.,0.));
#36763=DIRECTION('',(0.,0.451966109673778,-0.892035109009926));
#36764=DIRECTION('',(1.,0.,0.));
#36765=DIRECTION('',(0.,0.451966109673778,-0.892035109009926));
#36766=DIRECTION('center_axis',(1.,0.,0.));
#36767=DIRECTION('ref_axis',(0.,0.984807753012208,-0.17364817766693));
#36768=DIRECTION('center_axis',(-1.,0.,0.));
#36769=DIRECTION('ref_axis',(0.,1.,0.));
#36770=DIRECTION('',(0.,0.729803193940867,0.68365729580961));
#36771=DIRECTION('center_axis',(0.,0.683657295809611,-0.729803193940867));
#36772=DIRECTION('ref_axis',(0.,0.729803193940867,0.68365729580961));
#36773=DIRECTION('',(1.,0.,0.));
#36774=DIRECTION('',(0.,0.729803193940867,0.68365729580961));
#36775=DIRECTION('center_axis',(1.,0.,0.));
#36776=DIRECTION('ref_axis',(0.,0.984807753012208,-0.17364817766693));
#36777=DIRECTION('center_axis',(1.,0.,0.));
#36778=DIRECTION('ref_axis',(0.,1.,0.));
#36779=DIRECTION('center_axis',(0.,-0.956966182624129,-0.290199457811007));
#36780=DIRECTION('ref_axis',(0.,0.290199457811007,-0.956966182624129));
#36781=DIRECTION('',(-1.,0.,0.));
#36782=DIRECTION('',(0.,0.290199457811007,-0.956966182624129));
#36783=DIRECTION('',(1.,0.,0.));
#36784=DIRECTION('',(0.,0.290199457811007,-0.956966182624129));
#36785=DIRECTION('center_axis',(1.,0.,0.));
#36786=DIRECTION('ref_axis',(0.,0.939692620785908,-0.342020143325669));
#36787=DIRECTION('center_axis',(-1.,0.,0.));
#36788=DIRECTION('ref_axis',(0.,1.,0.));
#36789=DIRECTION('',(0.,0.837431687132078,0.546542010633328));
#36790=DIRECTION('center_axis',(0.,0.546542010633328,-0.837431687132078));
#36791=DIRECTION('ref_axis',(0.,0.837431687132078,0.546542010633328));
#36792=DIRECTION('',(1.,0.,0.));
#36793=DIRECTION('',(0.,0.837431687132078,0.546542010633328));
#36794=DIRECTION('center_axis',(1.,0.,0.));
#36795=DIRECTION('ref_axis',(0.,0.939692620785908,-0.342020143325669));
#36796=DIRECTION('center_axis',(1.,0.,0.));
#36797=DIRECTION('ref_axis',(0.,1.,0.));
#36798=DIRECTION('center_axis',(0.,-0.992820323027551,-0.11961524227066));
#36799=DIRECTION('ref_axis',(0.,0.11961524227066,-0.992820323027551));
#36800=DIRECTION('',(-1.,0.,0.));
#36801=DIRECTION('',(0.,0.11961524227066,-0.992820323027551));
#36802=DIRECTION('',(1.,0.,0.));
#36803=DIRECTION('',(0.,0.11961524227066,-0.992820323027551));
#36804=DIRECTION('center_axis',(1.,0.,0.));
#36805=DIRECTION('ref_axis',(0.,0.866025403784439,-0.5));
#36806=DIRECTION('center_axis',(-1.,0.,0.));
#36807=DIRECTION('ref_axis',(0.,1.,0.));
#36808=DIRECTION('',(0.,0.919615242270662,0.392820323027554));
#36809=DIRECTION('center_axis',(0.,0.392820323027554,-0.919615242270662));
#36810=DIRECTION('ref_axis',(0.,0.919615242270662,0.392820323027554));
#36811=DIRECTION('',(1.,0.,0.));
#36812=DIRECTION('',(0.,0.919615242270662,0.392820323027554));
#36813=DIRECTION('center_axis',(1.,0.,0.));
#36814=DIRECTION('ref_axis',(0.,0.866025403784439,-0.5));
#36815=DIRECTION('center_axis',(1.,0.,0.));
#36816=DIRECTION('ref_axis',(0.,1.,0.));
#36817=DIRECTION('center_axis',(0.,-0.998508120307106,0.0546034218778478));
#36818=DIRECTION('ref_axis',(0.,-0.0546034218778478,-0.998508120307106));
#36819=DIRECTION('',(-1.,0.,0.));
#36820=DIRECTION('',(0.,-0.0546034218778478,-0.998508120307106));
#36821=DIRECTION('',(1.,0.,0.));
#36822=DIRECTION('',(0.,-0.0546034218778478,-0.998508120307106));
#36823=DIRECTION('center_axis',(1.,0.,0.));
#36824=DIRECTION('ref_axis',(0.,0.766044443118978,-0.642787609686539));
#36825=DIRECTION('center_axis',(-1.,0.,0.));
#36826=DIRECTION('ref_axis',(0.,1.,0.));
#36827=DIRECTION('',(0.,0.973856753620618,0.227162988683262));
#36828=DIRECTION('center_axis',(0.,0.227162988683262,-0.973856753620618));
#36829=DIRECTION('ref_axis',(0.,0.973856753620618,0.227162988683262));
#36830=DIRECTION('',(1.,0.,0.));
#36831=DIRECTION('',(0.,0.973856753620618,0.227162988683262));
#36832=DIRECTION('center_axis',(1.,0.,0.));
#36833=DIRECTION('ref_axis',(0.,0.766044443118978,-0.642787609686539));
#36834=DIRECTION('center_axis',(1.,0.,0.));
#36835=DIRECTION('ref_axis',(0.,1.,0.));
#36836=DIRECTION('center_axis',(0.,-0.973856753620618,0.227162988683262));
#36837=DIRECTION('ref_axis',(0.,-0.227162988683262,-0.973856753620618));
#36838=DIRECTION('',(-1.,0.,0.));
#36839=DIRECTION('',(0.,-0.227162988683262,-0.973856753620618));
#36840=DIRECTION('',(1.,0.,0.));
#36841=DIRECTION('',(0.,-0.227162988683262,-0.973856753620618));
#36842=DIRECTION('center_axis',(1.,0.,0.));
#36843=DIRECTION('ref_axis',(0.,0.642787609686539,-0.766044443118978));
#36844=DIRECTION('center_axis',(-1.,0.,0.));
#36845=DIRECTION('ref_axis',(0.,1.,0.));
#36846=DIRECTION('',(0.,0.998508120307106,0.0546034218778477));
#36847=DIRECTION('center_axis',(0.,0.0546034218778477,-0.998508120307106));
#36848=DIRECTION('ref_axis',(0.,0.998508120307106,0.0546034218778477));
#36849=DIRECTION('',(1.,0.,0.));
#36850=DIRECTION('',(0.,0.998508120307106,0.0546034218778477));
#36851=DIRECTION('center_axis',(1.,0.,0.));
#36852=DIRECTION('ref_axis',(0.,0.642787609686539,-0.766044443118978));
#36853=DIRECTION('center_axis',(1.,0.,0.));
#36854=DIRECTION('ref_axis',(0.,1.,0.));
#36855=DIRECTION('center_axis',(0.,-0.919615242270662,0.392820323027554));
#36856=DIRECTION('ref_axis',(0.,-0.392820323027554,-0.919615242270662));
#36857=DIRECTION('',(-1.,0.,0.));
#36858=DIRECTION('',(0.,-0.392820323027554,-0.919615242270662));
#36859=DIRECTION('',(1.,0.,0.));
#36860=DIRECTION('',(0.,-0.392820323027554,-0.919615242270662));
#36861=DIRECTION('center_axis',(1.,0.,0.));
#36862=DIRECTION('ref_axis',(0.,0.5,-0.866025403784439));
#36863=DIRECTION('center_axis',(-1.,0.,0.));
#36864=DIRECTION('ref_axis',(0.,1.,0.));
#36865=DIRECTION('',(0.,0.992820323027551,-0.11961524227066));
#36866=DIRECTION('center_axis',(0.,-0.11961524227066,-0.992820323027551));
#36867=DIRECTION('ref_axis',(0.,0.992820323027551,-0.11961524227066));
#36868=DIRECTION('',(1.,0.,0.));
#36869=DIRECTION('',(0.,0.992820323027551,-0.11961524227066));
#36870=DIRECTION('center_axis',(1.,0.,0.));
#36871=DIRECTION('ref_axis',(0.,0.5,-0.866025403784439));
#36872=DIRECTION('center_axis',(1.,0.,0.));
#36873=DIRECTION('ref_axis',(0.,1.,0.));
#36874=DIRECTION('center_axis',(0.,-0.837431687132078,0.546542010633328));
#36875=DIRECTION('ref_axis',(0.,-0.546542010633328,-0.837431687132078));
#36876=DIRECTION('',(-1.,0.,0.));
#36877=DIRECTION('',(0.,-0.546542010633328,-0.837431687132078));
#36878=DIRECTION('',(1.,0.,0.));
#36879=DIRECTION('',(0.,-0.546542010633328,-0.837431687132078));
#36880=DIRECTION('center_axis',(1.,0.,0.));
#36881=DIRECTION('ref_axis',(0.,0.342020143325669,-0.939692620785908));
#36882=DIRECTION('center_axis',(-1.,0.,0.));
#36883=DIRECTION('ref_axis',(0.,1.,0.));
#36884=DIRECTION('',(0.,0.956966182624129,-0.290199457811007));
#36885=DIRECTION('center_axis',(0.,-0.290199457811007,-0.956966182624129));
#36886=DIRECTION('ref_axis',(0.,0.956966182624129,-0.290199457811007));
#36887=DIRECTION('',(1.,0.,0.));
#36888=DIRECTION('',(0.,0.956966182624129,-0.290199457811007));
#36889=DIRECTION('center_axis',(1.,0.,0.));
#36890=DIRECTION('ref_axis',(0.,0.342020143325669,-0.939692620785908));
#36891=DIRECTION('center_axis',(1.,0.,0.));
#36892=DIRECTION('ref_axis',(0.,1.,0.));
#36893=DIRECTION('center_axis',(0.,-0.729803193940867,0.683657295809611));
#36894=DIRECTION('ref_axis',(0.,-0.683657295809611,-0.729803193940867));
#36895=DIRECTION('',(-1.,0.,0.));
#36896=DIRECTION('',(0.,-0.683657295809611,-0.729803193940867));
#36897=DIRECTION('',(1.,0.,0.));
#36898=DIRECTION('',(0.,-0.683657295809611,-0.729803193940867));
#36899=DIRECTION('center_axis',(1.,0.,0.));
#36900=DIRECTION('ref_axis',(0.,0.17364817766693,-0.984807753012208));
#36901=DIRECTION('center_axis',(-1.,0.,0.));
#36902=DIRECTION('ref_axis',(0.,1.,0.));
#36903=DIRECTION('',(0.,0.892035109009926,-0.451966109673778));
#36904=DIRECTION('center_axis',(0.,-0.451966109673778,-0.892035109009926));
#36905=DIRECTION('ref_axis',(0.,0.892035109009926,-0.451966109673778));
#36906=DIRECTION('',(1.,0.,0.));
#36907=DIRECTION('',(0.,0.892035109009926,-0.451966109673778));
#36908=DIRECTION('center_axis',(1.,0.,0.));
#36909=DIRECTION('ref_axis',(0.,0.17364817766693,-0.984807753012208));
#36910=DIRECTION('center_axis',(1.,0.,0.));
#36911=DIRECTION('ref_axis',(0.,1.,0.));
#36912=DIRECTION('center_axis',(0.,-0.599999999999998,0.800000000000002));
#36913=DIRECTION('ref_axis',(0.,-0.800000000000002,-0.599999999999998));
#36914=DIRECTION('',(-1.,0.,0.));
#36915=DIRECTION('',(0.,-0.800000000000002,-0.599999999999998));
#36916=DIRECTION('',(1.,0.,0.));
#36917=DIRECTION('',(0.,-0.800000000000002,-0.599999999999998));
#36918=DIRECTION('center_axis',(1.,0.,0.));
#36919=DIRECTION('ref_axis',(0.,0.,-1.));
#36920=DIRECTION('center_axis',(-1.,0.,0.));
#36921=DIRECTION('ref_axis',(0.,1.,0.));
#36922=DIRECTION('',(0.,0.800000000000002,-0.599999999999998));
#36923=DIRECTION('center_axis',(0.,-0.599999999999998,-0.800000000000002));
#36924=DIRECTION('ref_axis',(0.,0.800000000000002,-0.599999999999998));
#36925=DIRECTION('',(1.,0.,0.));
#36926=DIRECTION('',(0.,0.800000000000002,-0.599999999999998));
#36927=DIRECTION('center_axis',(1.,0.,0.));
#36928=DIRECTION('ref_axis',(0.,0.,-1.));
#36929=DIRECTION('center_axis',(1.,0.,0.));
#36930=DIRECTION('ref_axis',(0.,1.,0.));
#36931=DIRECTION('center_axis',(0.,0.5,0.866025403784439));
#36932=DIRECTION('ref_axis',(0.,0.866025403784439,-0.5));
#36933=DIRECTION('',(0.,0.866025403784439,-0.5));
#36934=DIRECTION('',(-1.,0.,0.));
#36935=DIRECTION('',(0.,0.866025403784439,-0.5));
#36936=DIRECTION('',(-1.,0.,0.));
#36937=DIRECTION('center_axis',(0.,-0.5,0.866025403784439));
#36938=DIRECTION('ref_axis',(0.,0.866025403784439,0.5));
#36939=DIRECTION('',(0.,0.866025403784439,0.5));
#36940=DIRECTION('',(-1.,0.,0.));
#36941=DIRECTION('',(0.,0.866025403784439,0.5));
#36942=DIRECTION('center_axis',(0.,-1.,-1.20185167898973E-16));
#36943=DIRECTION('ref_axis',(0.,-1.20185167898973E-16,1.));
#36944=DIRECTION('',(0.,-1.20185167898973E-16,1.));
#36945=DIRECTION('',(-1.,0.,0.));
#36946=DIRECTION('',(0.,-1.20185167898973E-16,1.));
#36947=DIRECTION('center_axis',(0.,-0.5,-0.866025403784439));
#36948=DIRECTION('ref_axis',(0.,-0.866025403784439,0.5));
#36949=DIRECTION('',(0.,-0.866025403784439,0.5));
#36950=DIRECTION('',(-1.,0.,0.));
#36951=DIRECTION('',(0.,-0.866025403784439,0.5));
#36952=DIRECTION('center_axis',(0.,0.5,-0.866025403784439));
#36953=DIRECTION('ref_axis',(0.,-0.866025403784439,-0.5));
#36954=DIRECTION('',(0.,-0.866025403784439,-0.5));
#36955=DIRECTION('',(-1.,0.,0.));
#36956=DIRECTION('',(0.,-0.866025403784439,-0.5));
#36957=DIRECTION('center_axis',(0.,1.,-3.60555503696918E-16));
#36958=DIRECTION('ref_axis',(0.,-3.60555503696918E-16,-1.));
#36959=DIRECTION('',(0.,-3.60555503696918E-16,-1.));
#36960=DIRECTION('',(0.,-3.60555503696918E-16,-1.));
#36961=DIRECTION('center_axis',(-1.,0.,0.));
#36962=DIRECTION('ref_axis',(0.,0.,1.));
#36963=DIRECTION('center_axis',(-1.,0.,0.));
#36964=DIRECTION('ref_axis',(0.,0.,1.));
#36965=DIRECTION('center_axis',(1.,0.,0.));
#36966=DIRECTION('ref_axis',(0.,0.,-1.));
#36967=DIRECTION('center_axis',(1.,0.,0.));
#36968=DIRECTION('ref_axis',(0.,1.,0.));
#36969=DIRECTION('',(-0.707106781186546,0.707106781186549,8.65956056235495E-17));
#36970=DIRECTION('center_axis',(1.,0.,0.));
#36971=DIRECTION('ref_axis',(0.,1.,0.));
#36972=DIRECTION('center_axis',(1.,0.,0.));
#36973=DIRECTION('ref_axis',(0.,1.,0.));
#36974=DIRECTION('center_axis',(-1.,0.,0.));
#36975=DIRECTION('ref_axis',(0.,0.,1.));
#36976=DIRECTION('center_axis',(1.,0.,0.));
#36977=DIRECTION('ref_axis',(0.,0.,-1.));
#36978=DIRECTION('center_axis',(1.,0.,0.));
#36979=DIRECTION('ref_axis',(0.,1.,0.));
#36980=DIRECTION('center_axis',(1.,0.,0.));
#36981=DIRECTION('ref_axis',(0.,0.,-1.));
#36982=DIRECTION('',(-1.,0.,0.));
#36983=DIRECTION('',(-1.,0.,0.));
#36984=DIRECTION('center_axis',(-1.,0.,0.));
#36985=DIRECTION('ref_axis',(0.,1.,0.));
#36986=DIRECTION('center_axis',(1.,0.,0.));
#36987=DIRECTION('ref_axis',(0.,0.,-1.));
#36988=DIRECTION('',(-0.707106781186547,-0.707106781186548,-8.65956056235494E-17));
#36989=DIRECTION('center_axis',(1.,0.,0.));
#36990=DIRECTION('ref_axis',(0.,0.,-1.));
#49727=CARTESIAN_POINT('',(0.,0.,0.));
#49728=CARTESIAN_POINT('Origin',(-14.75,0.,0.));
#49729=CARTESIAN_POINT('',(-29.0911584740964,-4.93085069296601,0.00239406595250471));
#49730=CARTESIAN_POINT('',(-29.3088415259036,-4.92746336814012,0.00144215323830204));
#49731=CARTESIAN_POINT('',(-14.75,-4.925,-6.03138548580071E-16));
#49732=CARTESIAN_POINT('',(-29.575,2.17167188636589,4.42425492889053));
#49733=CARTESIAN_POINT('Ctrl Pts',(-29.0911584740964,-4.93085069296601,
0.00239406595250471));
#49734=CARTESIAN_POINT('Ctrl Pts',(-29.0987040309128,-4.93188800524103,
0.15750466532186));
#49735=CARTESIAN_POINT('Ctrl Pts',(-29.1062495877292,-4.92523207312776,
0.312531807375031));
#49736=CARTESIAN_POINT('Ctrl Pts',(-29.1137951445456,-4.91059689710246,
0.466805765893802));
#49737=CARTESIAN_POINT('Ctrl Pts',(-29.1933410329187,-4.75631165258633,
2.09317468495417));
#49738=CARTESIAN_POINT('Ctrl Pts',(-29.2728869212918,-3.71524898717827,
3.63583816030893));
#49739=CARTESIAN_POINT('Ctrl Pts',(-29.3524328096649,-2.26290809811278,
4.38440317990658));
#49740=CARTESIAN_POINT('Ctrl Pts',(-29.4266218731099,-0.908371583825934,
5.08255790377123));
#49741=CARTESIAN_POINT('Ctrl Pts',(-29.5008109365549,0.803915241080997,
5.08996618673832));
#49742=CARTESIAN_POINT('Ctrl Pts',(-29.575,2.17494790042119,4.42655504786424));
#49743=CARTESIAN_POINT('',(-29.575,-2.1683958723106,4.4219548099168));
#49744=CARTESIAN_POINT('Origin',(-29.575,0.,0.));
#49745=CARTESIAN_POINT('Ctrl Pts',(-29.575,-2.16839587231058,4.42195480991681));
#49746=CARTESIAN_POINT('Ctrl Pts',(-29.5352270558135,-2.90509583874374,
4.0606989321402));
#49747=CARTESIAN_POINT('Ctrl Pts',(-29.4954541116269,-3.54417075123437,
3.51185369356184));
#49748=CARTESIAN_POINT('Ctrl Pts',(-29.4556811674404,-4.01940836209596,
2.8419582808667));
#49749=CARTESIAN_POINT('Ctrl Pts',(-29.4159082232539,-4.49464597295758,
2.17206286817154));
#49750=CARTESIAN_POINT('Ctrl Pts',(-29.3761352790673,-4.80604628219013,
1.38111728135961));
#49751=CARTESIAN_POINT('Ctrl Pts',(-29.3363623348808,-4.89820932110733,
0.567147712221922));
#49752=CARTESIAN_POINT('Ctrl Pts',(-29.3271887318884,-4.91946666443181,
0.379406175157601));
#49753=CARTESIAN_POINT('Ctrl Pts',(-29.318015128896,-4.929060779183,0.190439782628943));
#49754=CARTESIAN_POINT('Ctrl Pts',(-29.3088415259036,-4.92746336814012,
0.00144215323830204));
#49755=CARTESIAN_POINT('Origin',(-14.75,0.,0.));
#49756=CARTESIAN_POINT('',(-27.5911584740964,-4.91871916148224,0.00298870709768639));
#49757=CARTESIAN_POINT('',(-27.8088415259036,-4.91810465358294,0.00250400581179228));
#49758=CARTESIAN_POINT('',(-14.75,-4.925,-6.03138548580071E-16));
#49759=CARTESIAN_POINT('Ctrl Pts',(-27.5911584740964,-4.91871916148224,
0.00298870709768639));
#49760=CARTESIAN_POINT('Ctrl Pts',(-27.6214287006744,-4.92217786568793,
0.629288456904983));
#49761=CARTESIAN_POINT('Ctrl Pts',(-27.6516989272523,-4.81132058056506,
1.2544097760338));
#49762=CARTESIAN_POINT('Ctrl Pts',(-27.6819691538303,-4.58053680634953,
1.83157791678433));
#49763=CARTESIAN_POINT('Ctrl Pts',(-27.7615150422034,-3.97406958038444,
3.34829442957306));
#49764=CARTESIAN_POINT('Ctrl Pts',(-27.8410609305764,-2.53943282222183,
4.53386340685575));
#49765=CARTESIAN_POINT('Ctrl Pts',(-27.9206068189495,-0.935593024822473,
4.84364324705812));
#49766=CARTESIAN_POINT('Ctrl Pts',(-28.0001527073226,0.668246772576907,
5.1534230872605));
#49767=CARTESIAN_POINT('Ctrl Pts',(-28.0796985956957,2.44128960921305,4.58741379038254));
#49768=CARTESIAN_POINT('Ctrl Pts',(-28.1592444840688,3.56896084480546,3.40568511210877));
#49769=CARTESIAN_POINT('Ctrl Pts',(-28.2387903724418,4.69663208039786,2.22395643383501));
#49770=CARTESIAN_POINT('Ctrl Pts',(-28.3183362608148,5.17893171494654,0.426508374165463));
#49771=CARTESIAN_POINT('Ctrl Pts',(-28.3978821491879,4.79450650284291,-1.16110247139908));
#49772=CARTESIAN_POINT('Ctrl Pts',(-28.477428037561,4.41008129073928,-2.74871331696362));
#49773=CARTESIAN_POINT('Ctrl Pts',(-28.5569739259341,3.15893123198334,-4.12648694842314));
#49774=CARTESIAN_POINT('Ctrl Pts',(-28.6365198143072,1.61540970892298,-4.66128231395555));
#49775=CARTESIAN_POINT('Ctrl Pts',(-28.7160657026803,0.0718881858626222,
-5.19607767948796));
#49776=CARTESIAN_POINT('Ctrl Pts',(-28.7956115910533,-1.76400480150215,
-4.88789477909325));
#49777=CARTESIAN_POINT('Ctrl Pts',(-28.8751574794264,-3.04819738337245,
-3.87876614751291));
#49778=CARTESIAN_POINT('Ctrl Pts',(-28.9471578109831,-4.21057413933529,
-2.96536135006638));
#49779=CARTESIAN_POINT('Ctrl Pts',(-29.0191581425397,-4.92095257284757,
-1.4776841912631));
#49780=CARTESIAN_POINT('Ctrl Pts',(-29.0911584740964,-4.93085069296601,
0.00239406595250471));
#49781=CARTESIAN_POINT('Ctrl Pts',(-29.3088415259036,-4.92746336814012,
0.00144215323830204));
#49782=CARTESIAN_POINT('Ctrl Pts',(-29.2384692405229,-4.91520935345547,
-1.44839114811431));
#49783=CARTESIAN_POINT('Ctrl Pts',(-29.1680969551423,-4.24436898433528,
-2.90006264127696));
#49784=CARTESIAN_POINT('Ctrl Pts',(-29.0977246697616,-3.12788046011008,
-3.81474362504512));
#49785=CARTESIAN_POINT('Ctrl Pts',(-29.0181787813885,-1.86584852470544,
-4.8486607564584));
#49786=CARTESIAN_POINT('Ctrl Pts',(-28.9386328930154,-0.0344076573231608,
-5.19645995170656));
#49787=CARTESIAN_POINT('Ctrl Pts',(-28.8590870046423,1.52027960945058,-4.69387792027941));
#49788=CARTESIAN_POINT('Ctrl Pts',(-28.7795411162692,3.07496687622432,-4.19129588885225));
#49789=CARTESIAN_POINT('Ctrl Pts',(-28.6999952278962,4.35290054238952,-2.83833263074978));
#49790=CARTESIAN_POINT('Ctrl Pts',(-28.6204493395231,4.76944898889192,-1.25865959225591));
#49791=CARTESIAN_POINT('Ctrl Pts',(-28.54090345115,5.18599743539432,0.321013446237961));
#49792=CARTESIAN_POINT('Ctrl Pts',(-28.4613575627769,4.74116066223391,2.12739626512323));
#49793=CARTESIAN_POINT('Ctrl Pts',(-28.3818116744039,3.63804206657526,3.33181334358779));
#49794=CARTESIAN_POINT('Ctrl Pts',(-28.3022657860308,2.53492347091661,4.53623042205235));
#49795=CARTESIAN_POINT('Ctrl Pts',(-28.2227198976577,0.773523052759708,
5.13868176009622));
#49796=CARTESIAN_POINT('Ctrl Pts',(-28.1431740092847,-0.836391940911384,
4.8618460820682));
#49797=CARTESIAN_POINT('Ctrl Pts',(-28.0636281209116,-2.44630693458247,
4.58501040404019));
#49798=CARTESIAN_POINT('Ctrl Pts',(-27.9840822325385,-3.90473650376776,
3.42888770994031));
#49799=CARTESIAN_POINT('Ctrl Pts',(-27.9045363441654,-4.54206616433802,
1.92485926408358));
#49800=CARTESIAN_POINT('Ctrl Pts',(-27.8726380714115,-4.79763833485293,
1.32173683278195));
#49801=CARTESIAN_POINT('Ctrl Pts',(-27.8407397986575,-4.92117374333981,
0.662669505529257));
#49802=CARTESIAN_POINT('Ctrl Pts',(-27.8088415259036,-4.91810465358294,
0.00250400581179228));
#49803=CARTESIAN_POINT('Origin',(-14.75,0.,0.));
#49804=CARTESIAN_POINT('',(-26.0911584740964,-4.92036739665688,-0.00383377046079936));
#49805=CARTESIAN_POINT('',(-26.3088415259036,-4.92121007081632,-0.00410983607026229));
#49806=CARTESIAN_POINT('',(-14.75,-4.925,-6.03138548580071E-16));
#49807=CARTESIAN_POINT('Ctrl Pts',(-26.0911584740964,-4.92036739665688,
-0.00383377046079936));
#49808=CARTESIAN_POINT('Ctrl Pts',(-26.1441533704359,-4.91244432033151,
1.09173065983813));
#49809=CARTESIAN_POINT('Ctrl Pts',(-26.1971482667754,-4.55141276587038,
2.19203324705585));
#49810=CARTESIAN_POINT('Ctrl Pts',(-26.2501431631149,-3.87908362999679,
3.04775276608836));
#49811=CARTESIAN_POINT('Ctrl Pts',(-26.329689051488,-2.86991063247732,4.33219662844735));
#49812=CARTESIAN_POINT('Ctrl Pts',(-26.4092349398611,-1.15937419217738,
5.06558698769252));
#49813=CARTESIAN_POINT('Ctrl Pts',(-26.4887808282342,0.466768297211532,
4.91103020168458));
#49814=CARTESIAN_POINT('Ctrl Pts',(-26.5683267166072,2.09291078660044,4.75647341567663));
#49815=CARTESIAN_POINT('Ctrl Pts',(-26.6478726049803,3.63465932507832,3.71396948441558));
#49816=CARTESIAN_POINT('Ctrl Pts',(-26.7274184933534,4.38378843538607,2.26240825335668));
#49817=CARTESIAN_POINT('Ctrl Pts',(-26.8069643817264,5.13291754569381,0.810847022297775));
#49818=CARTESIAN_POINT('Ctrl Pts',(-26.8865102700995,5.08942722783144,-1.04977150855898));
#49819=CARTESIAN_POINT('Ctrl Pts',(-26.9660561584726,4.27329930907013,-2.46474911465105));
#49820=CARTESIAN_POINT('Ctrl Pts',(-27.0456020468457,3.45717139030882,-3.87972672074312));
#49821=CARTESIAN_POINT('Ctrl Pts',(-27.1251479352187,1.86840587064857,-4.84906340207051));
#49822=CARTESIAN_POINT('Ctrl Pts',(-27.2046938235918,0.236816482345431,
-4.92747617760022));
#49823=CARTESIAN_POINT('Ctrl Pts',(-27.2842397119649,-1.39477290595772,
-5.00588895312993));
#49824=CARTESIAN_POINT('Ctrl Pts',(-27.363785600338,-3.06918616290375,-4.19337782286196));
#49825=CARTESIAN_POINT('Ctrl Pts',(-27.4433314887111,-4.01724394449298,
-2.86319023358059));
#49826=CARTESIAN_POINT('Ctrl Pts',(-27.4926071505062,-4.60452979374673,
-2.03918945724775));
#49827=CARTESIAN_POINT('Ctrl Pts',(-27.5418828123013,-4.91308887859519,
-1.01653899859688));
#49828=CARTESIAN_POINT('Ctrl Pts',(-27.5911584740964,-4.91871916148224,
0.00298870709768639));
#49829=CARTESIAN_POINT('Ctrl Pts',(-27.8088415259036,-4.91810465358294,
0.00250400581179228));
#49830=CARTESIAN_POINT('Ctrl Pts',(-27.7611939102845,-4.91352024206437,
-0.983609324467926));
#49831=CARTESIAN_POINT('Ctrl Pts',(-27.7135462946653,-4.62644968879859,
-1.97217295080227));
#49832=CARTESIAN_POINT('Ctrl Pts',(-27.6658986790462,-4.07499817460332,
-2.78038834104901));
#49833=CARTESIAN_POINT('Ctrl Pts',(-27.5863527906731,-3.15437077234312,
-4.12967330271128));
#49834=CARTESIAN_POINT('Ctrl Pts',(-27.5068069023,-1.49688621586748,-4.97630902842222));
#49835=CARTESIAN_POINT('Ctrl Pts',(-27.427261013927,0.135976152639213,-4.93130021039854));
#49836=CARTESIAN_POINT('Ctrl Pts',(-27.3477151255539,1.7688385211459,-4.88629139237487));
#49837=CARTESIAN_POINT('Ctrl Pts',(-27.2681692371808,3.37707870168364,-3.9496380306166));
#49838=CARTESIAN_POINT('Ctrl Pts',(-27.1886233488077,4.22197683163389,-2.55164722242325));
#49839=CARTESIAN_POINT('Ctrl Pts',(-27.1090774604347,5.06687496158415,-1.1536564142299));
#49840=CARTESIAN_POINT('Ctrl Pts',(-27.0295315720616,5.14843104094691,0.705671840398515));
#49841=CARTESIAN_POINT('Ctrl Pts',(-26.9499856836885,4.42915646105591,2.17225163970649));
#49842=CARTESIAN_POINT('Ctrl Pts',(-26.8704397953154,3.7098818811649,3.63883143901446));
#49843=CARTESIAN_POINT('Ctrl Pts',(-26.7908939069423,2.18977664202013,4.71266278300198));
#49844=CARTESIAN_POINT('Ctrl Pts',(-26.7113480185693,0.567134884896936,
4.90045492678425));
#49845=CARTESIAN_POINT('Ctrl Pts',(-26.6318021301962,-1.05550687222627,
5.08824707056651));
#49846=CARTESIAN_POINT('Ctrl Pts',(-26.5522562418232,-2.7806851473279,4.39000001414349));
#49847=CARTESIAN_POINT('Ctrl Pts',(-26.4727103534501,-3.81592225162572,
3.12646916519825));
#49848=CARTESIAN_POINT('Ctrl Pts',(-26.4180874109346,-4.52680370627415,
2.25882189467213));
#49849=CARTESIAN_POINT('Ctrl Pts',(-26.3634644684191,-4.91235316928586,
1.12462305447093));
#49850=CARTESIAN_POINT('Ctrl Pts',(-26.3088415259036,-4.92121007081632,
-0.00410983607026228));
#49851=CARTESIAN_POINT('Origin',(-14.75,0.,0.));
#49852=CARTESIAN_POINT('',(-24.5911584740964,-4.93264761214373,-0.00145024765580815));
#49853=CARTESIAN_POINT('',(-24.8088415259036,-4.93298564037245,-0.000844910194652536));
#49854=CARTESIAN_POINT('',(-14.75,-4.925,-6.03138548580071E-16));
#49855=CARTESIAN_POINT('Ctrl Pts',(-24.5911584740964,-4.93264761214373,
-0.00145024765580815));
#49856=CARTESIAN_POINT('Ctrl Pts',(-24.6668780401975,-4.9266177416151,1.55388178409041));
#49857=CARTESIAN_POINT('Ctrl Pts',(-24.7425976062985,-4.12958481778531,
3.11453421006534));
#49858=CARTESIAN_POINT('Ctrl Pts',(-24.8183171723996,-2.86343383037207,
4.01706799645064));
#49859=CARTESIAN_POINT('Ctrl Pts',(-24.8978630607726,-1.53330067860747,
4.96520934909558));
#49860=CARTESIAN_POINT('Ctrl Pts',(-24.9774089491457,0.314560165826125,
5.18703834835445));
#49861=CARTESIAN_POINT('Ctrl Pts',(-25.0569548375188,1.83130840270388,4.58065477546433));
#49862=CARTESIAN_POINT('Ctrl Pts',(-25.1365007258919,3.34805663958163,3.9742712025742));
#49863=CARTESIAN_POINT('Ctrl Pts',(-25.2160466142649,4.53369226890353,2.5396750575351));
#49864=CARTESIAN_POINT('Ctrl Pts',(-25.295592502638,4.84357719847932,0.935867858373788));
#49865=CARTESIAN_POINT('Ctrl Pts',(-25.3751383910111,5.15346212805511,-0.667939340787529));
#49866=CARTESIAN_POINT('Ctrl Pts',(-25.4546842793842,4.58759635788477,-2.44095759407106));
#49867=CARTESIAN_POINT('Ctrl Pts',(-25.5342301677572,3.40591819971526,-3.56872660483793));
#49868=CARTESIAN_POINT('Ctrl Pts',(-25.6137760561303,2.22424004154574,-4.69649561560481));
#49869=CARTESIAN_POINT('Ctrl Pts',(-25.6933219445034,0.426749495377071,
-5.17901538385504));
#49870=CARTESIAN_POINT('Ctrl Pts',(-25.7728678328765,-1.16085155874105,
-4.79463371383198));
#49871=CARTESIAN_POINT('Ctrl Pts',(-25.8524137212495,-2.74845261285917,
-4.41025204380892));
#49872=CARTESIAN_POINT('Ctrl Pts',(-25.9319596096226,-4.12616417492674,
-3.15896893551255));
#49873=CARTESIAN_POINT('Ctrl Pts',(-26.0115054979957,-4.661115178591,-1.61557869862796));
#49874=CARTESIAN_POINT('Ctrl Pts',(-26.0380564900293,-4.83967223700271,
-1.10042269594398));
#49875=CARTESIAN_POINT('Ctrl Pts',(-26.0646074820628,-4.92433693997005,
-0.552722898855101));
#49876=CARTESIAN_POINT('Ctrl Pts',(-26.0911584740964,-4.92036739665688,
-0.00383377046079936));
#49877=CARTESIAN_POINT('Ctrl Pts',(-26.3088415259036,-4.92121007081632,
-0.00410983607026228));
#49878=CARTESIAN_POINT('Ctrl Pts',(-26.283918580046,-4.92525123130941,-0.519119599791246));
#49879=CARTESIAN_POINT('Ctrl Pts',(-26.2589956341884,-4.85087080801869,
-1.03299143706225));
#49880=CARTESIAN_POINT('Ctrl Pts',(-26.2340726883308,-4.69319011704004,
-1.5198867036229));
#49881=CARTESIAN_POINT('Ctrl Pts',(-26.1545267999577,-4.18992494466251,
-3.07389708203135));
#49882=CARTESIAN_POINT('Ctrl Pts',(-26.0749809115847,-2.83809866641343,
-4.35310319738077));
#49883=CARTESIAN_POINT('Ctrl Pts',(-25.9954350232116,-1.25869311650182,
-4.76988247643117));
#49884=CARTESIAN_POINT('Ctrl Pts',(-25.9158891348386,0.320712433409791,
-5.18666175548156));
#49885=CARTESIAN_POINT('Ctrl Pts',(-25.8363432464654,2.12769725498392,-4.74101419823293));
#49886=CARTESIAN_POINT('Ctrl Pts',(-25.7567973580924,3.33219893892002,-3.63765499595275));
#49887=CARTESIAN_POINT('Ctrl Pts',(-25.6772514697193,4.53670062285612,-2.53429579367258));
#49888=CARTESIAN_POINT('Ctrl Pts',(-25.5977055813462,5.13871916915418,-0.773224946360884));
#49889=CARTESIAN_POINT('Ctrl Pts',(-25.5181596929732,4.86170857536212,0.836585847286859));
#49890=CARTESIAN_POINT('Ctrl Pts',(-25.4386138046001,4.58469798157006,2.44639664093459));
#49891=CARTESIAN_POINT('Ctrl Pts',(-25.359067916227,3.4286582476879,3.90494738091836));
#49892=CARTESIAN_POINT('Ctrl Pts',(-25.2795220278539,1.92463240018136,4.54223247168555));
#49893=CARTESIAN_POINT('Ctrl Pts',(-25.1999761394808,0.420606552674816,
5.17951756245273));
#49894=CARTESIAN_POINT('Ctrl Pts',(-25.1204302511078,-1.43140540845612,
4.99553700400332));
#49895=CARTESIAN_POINT('Ctrl Pts',(-25.0408843627347,-2.78065642310143,
4.07480491924754));
#49896=CARTESIAN_POINT('Ctrl Pts',(-24.9635367504577,-4.09262045392238,
3.17951756047544));
#49897=CARTESIAN_POINT('Ctrl Pts',(-24.8861891381806,-4.92922749371504,
1.58763673888852));
#49898=CARTESIAN_POINT('Ctrl Pts',(-24.8088415259036,-4.93298564037245,
-0.000844910194652536));
#49899=CARTESIAN_POINT('Origin',(-14.75,0.,0.));
#49900=CARTESIAN_POINT('',(-23.0911584740964,-4.92477578693879,0.00455121266192807));
#49901=CARTESIAN_POINT('',(-23.3088415259036,-4.92376359828451,0.00452755087589233));
#49902=CARTESIAN_POINT('',(-14.75,-4.925,-6.03138548580071E-16));
#49903=CARTESIAN_POINT('Ctrl Pts',(-23.0911584740964,-4.92477578693879,
0.00455121266192807));
#49904=CARTESIAN_POINT('Ctrl Pts',(-23.1100568215859,-4.92836778419939,
0.39435127717714));
#49905=CARTESIAN_POINT('Ctrl Pts',(-23.1289551690754,-4.88600126774917,
0.783379637951124));
#49906=CARTESIAN_POINT('Ctrl Pts',(-23.147853516565,-4.7947032911263,1.1605640760821));
#49907=CARTESIAN_POINT('Ctrl Pts',(-23.227399404938,-4.41041685226391,2.74818813835895));
#49908=CARTESIAN_POINT('Ctrl Pts',(-23.3069452933111,-3.15921646993337,
4.12597456962399));
#49909=CARTESIAN_POINT('Ctrl Pts',(-23.3864911816842,-1.6158582674624,4.66101820240316));
#49910=CARTESIAN_POINT('Ctrl Pts',(-23.4660370700573,-0.0725000649914348,
5.19606183518233));
#49911=CARTESIAN_POINT('Ctrl Pts',(-23.5455829584304,1.76301595761996,4.88836266947564));
#49912=CARTESIAN_POINT('Ctrl Pts',(-23.6251288468034,3.04752024302872,3.87926655341467));
#49913=CARTESIAN_POINT('Ctrl Pts',(-23.7046747351765,4.33202452843749,2.87017043735369));
#49914=CARTESIAN_POINT('Ctrl Pts',(-23.7842206235496,5.06551707664363,1.1596773709384));
#49915=CARTESIAN_POINT('Ctrl Pts',(-23.8637665119226,4.91105798552202,-0.46647410387683));
#49916=CARTESIAN_POINT('Ctrl Pts',(-23.9433124002957,4.75659889440041,-2.09262557869207));
#49917=CARTESIAN_POINT('Ctrl Pts',(-24.0228582886688,3.71418816395107,-3.63443546190725));
#49918=CARTESIAN_POINT('Ctrl Pts',(-24.1024041770419,2.26267151748941,-4.38365215585762));
#49919=CARTESIAN_POINT('Ctrl Pts',(-24.181950065415,0.811154871027751,-5.132868849808));
#49920=CARTESIAN_POINT('Ctrl Pts',(-24.261495953788,-1.04946769144621,-5.08949235449356));
#49921=CARTESIAN_POINT('Ctrl Pts',(-24.3410418421611,-2.4644935804178,-4.2734482583492));
#49922=CARTESIAN_POINT('Ctrl Pts',(-24.4205877305342,-3.87951946938938,
-3.45740416220484));
#49923=CARTESIAN_POINT('Ctrl Pts',(-24.5001336189073,-4.84894868485859,
-1.86869246523057));
#49924=CARTESIAN_POINT('Ctrl Pts',(-24.5796795072803,-4.92746056304542,
-0.237109763727941));
#49925=CARTESIAN_POINT('Ctrl Pts',(-24.5835058295524,-4.93123714728213,
-0.158627250588653));
#49926=CARTESIAN_POINT('Ctrl Pts',(-24.5873321518244,-4.93295231843154,
-0.0800455421075516));
#49927=CARTESIAN_POINT('Ctrl Pts',(-24.5911584740964,-4.93264761214373,
-0.00145024765580815));
#49928=CARTESIAN_POINT('Ctrl Pts',(-24.8088415259036,-4.93298564037245,
-0.000844910194652536));
#49929=CARTESIAN_POINT('Ctrl Pts',(-24.8066432498076,-4.93309244966778,
-0.0459907283445572));
#49930=CARTESIAN_POINT('Ctrl Pts',(-24.8044449737115,-4.93252653505162,
-0.0911338008527958));
#49931=CARTESIAN_POINT('Ctrl Pts',(-24.8022466976155,-4.93127968975541,
-0.136258058327248));
#49932=CARTESIAN_POINT('Ctrl Pts',(-24.7227008092424,-4.88616187360439,
-1.76910534008413));
#49933=CARTESIAN_POINT('Ctrl Pts',(-24.6431549208693,-3.94943617314267,
-3.37731629253574));
#49934=CARTESIAN_POINT('Ctrl Pts',(-24.5636090324963,-2.55140047284839,
-4.22213703896742));
#49935=CARTESIAN_POINT('Ctrl Pts',(-24.4840631441232,-1.15336477255412,
-5.06695778539909));
#49936=CARTESIAN_POINT('Ctrl Pts',(-24.4045172557501,0.705980927572705,
-5.14838832581082));
#49937=CARTESIAN_POINT('Ctrl Pts',(-24.324971367377,2.17252059826335,-4.42902243726831));
#49938=CARTESIAN_POINT('Ctrl Pts',(-24.2454254790039,3.63906026895399,-3.70965654872581));
#49939=CARTESIAN_POINT('Ctrl Pts',(-24.1658795906309,4.71279391020846,-2.18949423122905));
#49940=CARTESIAN_POINT('Ctrl Pts',(-24.0863337022578,4.90048718004666,-0.566842967216153));
#49941=CARTESIAN_POINT('Ctrl Pts',(-24.0067878138847,5.08818044988486,1.05580829679675));
#49942=CARTESIAN_POINT('Ctrl Pts',(-23.9272419255116,4.3898333483068,2.78094850732579));
#49943=CARTESIAN_POINT('Ctrl Pts',(-23.8476960371386,3.12624123694881,3.81611075100284));
#49944=CARTESIAN_POINT('Ctrl Pts',(-23.7681501487655,1.86264912559084,4.85127299467987));
#49945=CARTESIAN_POINT('Ctrl Pts',(-23.6886042603924,0.0338120044529563,
5.19645727150491));
#49946=CARTESIAN_POINT('Ctrl Pts',(-23.6090583720193,-1.52016861672953,
4.69309843356272));
#49947=CARTESIAN_POINT('Ctrl Pts',(-23.5295124836463,-3.07414923791204,
4.18973959562053));
#49948=CARTESIAN_POINT('Ctrl Pts',(-23.4499665952732,-4.35327335913915,
2.83783764291109));
#49949=CARTESIAN_POINT('Ctrl Pts',(-23.3704207069001,-4.76995770197036,
1.25840735017577));
#49950=CARTESIAN_POINT('Ctrl Pts',(-23.3498943132346,-4.8774808817366,0.850843758656771));
#49951=CARTESIAN_POINT('Ctrl Pts',(-23.3293679195691,-4.92757673294028,
0.428129724095519));
#49952=CARTESIAN_POINT('Ctrl Pts',(-23.3088415259036,-4.92376359828451,
0.00452755087589233));
#49953=CARTESIAN_POINT('Origin',(-14.75,0.,0.));
#49954=CARTESIAN_POINT('',(-21.5911584740964,-4.91693164693359,-0.000632398697534842));
#49955=CARTESIAN_POINT('',(-21.8088415259036,-4.91711569616659,-0.00117946379282014));
#49956=CARTESIAN_POINT('',(-14.75,-4.925,-6.03138548580071E-16));
#49957=CARTESIAN_POINT('Ctrl Pts',(-21.5911584740964,-4.91693164693359,
-0.000632398697534842));
#49958=CARTESIAN_POINT('Ctrl Pts',(-21.6327814913475,-4.91594750340395,
0.861347871439622));
#49959=CARTESIAN_POINT('Ctrl Pts',(-21.6744045085985,-4.70055318639053,
1.72378817794021));
#49960=CARTESIAN_POINT('Ctrl Pts',(-21.7160275258496,-4.27359604091789,
2.46423730661521));
#49961=CARTESIAN_POINT('Ctrl Pts',(-21.7955734142227,-3.4576368030521,3.87931212880427));
#49962=CARTESIAN_POINT('Ctrl Pts',(-21.8751193025958,-1.86898324578976,
4.84883661113057));
#49963=CARTESIAN_POINT('Ctrl Pts',(-21.9546651909688,-0.237405254457672,
4.92744633348781));
#49964=CARTESIAN_POINT('Ctrl Pts',(-22.0342110793419,1.39417273687441,5.00605605584506));
#49965=CARTESIAN_POINT('Ctrl Pts',(-22.113756967715,3.06867516227623,4.19375101823326));
#49966=CARTESIAN_POINT('Ctrl Pts',(-22.1933028560881,4.01689627682146,2.86367472410927));
#49967=CARTESIAN_POINT('Ctrl Pts',(-22.2728487444611,4.9651173913667,1.53359842998527));
#49968=CARTESIAN_POINT('Ctrl Pts',(-22.3523946328342,5.18705719505533,-0.314249120650923));
#49969=CARTESIAN_POINT('Ctrl Pts',(-22.4319405212073,4.58076458321006,-1.83103371282965));
#49970=CARTESIAN_POINT('Ctrl Pts',(-22.5114864095804,3.97447197136479,-3.34781830500836));
#49971=CARTESIAN_POINT('Ctrl Pts',(-22.5910322979534,2.53994694398564,-4.5335399387296));
#49972=CARTESIAN_POINT('Ctrl Pts',(-22.6705781863265,0.936158324065459,
-4.84352105564377));
#49973=CARTESIAN_POINT('Ctrl Pts',(-22.7501240746996,-0.667630295854733,
-5.15350217255794));
#49974=CARTESIAN_POINT('Ctrl Pts',(-22.8296699630727,-2.44068250831595,
-4.58774277266501));
#49975=CARTESIAN_POINT('Ctrl Pts',(-22.9092158514458,-3.56852236684944,
-3.40613222607422));
#49976=CARTESIAN_POINT('Ctrl Pts',(-22.9698633923293,-4.42841236656523,
-2.50524626705758));
#49977=CARTESIAN_POINT('Ctrl Pts',(-23.0305109332129,-4.9132485462191,-1.24637378817277));
#49978=CARTESIAN_POINT('Ctrl Pts',(-23.0911584740964,-4.92477578693879,
0.00455121266192807));
#49979=CARTESIAN_POINT('Ctrl Pts',(-23.3088415259036,-4.92376359828451,
0.00452755087589233));
#49980=CARTESIAN_POINT('Ctrl Pts',(-23.249822031196,-4.9127997005681,-1.2134548491438));
#49981=CARTESIAN_POINT('Ctrl Pts',(-23.1908025364885,-4.4561520233695,-2.43877979118426));
#49982=CARTESIAN_POINT('Ctrl Pts',(-23.1317830417809,-3.63745529283231,
-3.33241721991151));
#49983=CARTESIAN_POINT('Ctrl Pts',(-23.0522371534078,-2.53402397642775,
-4.53685286450225));
#49984=CARTESIAN_POINT('Ctrl Pts',(-22.9726912650347,-0.77291677918332,
-5.13876552092253));
#49985=CARTESIAN_POINT('Ctrl Pts',(-22.8931453766617,0.83687745995922,-4.86165832319329));
#49986=CARTESIAN_POINT('Ctrl Pts',(-22.8135994882886,2.44667169910178,-4.58455112546405));
#49987=CARTESIAN_POINT('Ctrl Pts',(-22.7340535999155,3.90515298014245,-3.42842407358526));
#49988=CARTESIAN_POINT('Ctrl Pts',(-22.6545077115424,4.5423478449547,-1.92436004709929));
#49989=CARTESIAN_POINT('Ctrl Pts',(-22.5749618231694,5.17954270976695,-0.42029602061334));
#49990=CARTESIAN_POINT('Ctrl Pts',(-22.4954159347963,4.9954511583508,1.43170498047977));
#49991=CARTESIAN_POINT('Ctrl Pts',(-22.4158700464232,4.07463817966522,2.78090079647325));
#49992=CARTESIAN_POINT('Ctrl Pts',(-22.3363241580501,3.15382520097963,4.13009661246674));
#49993=CARTESIAN_POINT('Ctrl Pts',(-22.2567782696771,1.4962907950246,4.97648724336059));
#49994=CARTESIAN_POINT('Ctrl Pts',(-22.177232381304,-0.136553786680188,
4.93127149915006));
#49995=CARTESIAN_POINT('Ctrl Pts',(-22.0976864929309,-1.76939836838497,
4.88605575493953));
#49996=CARTESIAN_POINT('Ctrl Pts',(-22.0181406045578,-3.37755312583951,
3.94923363562461));
#49997=CARTESIAN_POINT('Ctrl Pts',(-21.9385947161848,-4.22229002887781,
2.55114728056903));
#49998=CARTESIAN_POINT('Ctrl Pts',(-21.8953436527577,-4.68159433887712,
1.79097321179257));
#49999=CARTESIAN_POINT('Ctrl Pts',(-21.8520925893307,-4.91520443767987,
0.894432581458181));
#50000=CARTESIAN_POINT('Ctrl Pts',(-21.8088415259036,-4.91711569616659,
-0.00117946379282014));
#50001=CARTESIAN_POINT('Origin',(-14.75,0.,0.));
#50002=CARTESIAN_POINT('',(-20.0911584740964,-4.92710437571252,-0.00432825790191715));
#50003=CARTESIAN_POINT('',(-20.3088415259036,-4.92810468982102,-0.00410855472338207));
#50004=CARTESIAN_POINT('',(-14.75,-4.925,-6.03138548580071E-16));
#50005=CARTESIAN_POINT('Ctrl Pts',(-20.0911584740964,-4.92710437571252,
-0.00432825790191715));
#50006=CARTESIAN_POINT('Ctrl Pts',(-20.155506161109,-4.91490963574447,1.32130828947872));
#50007=CARTESIAN_POINT('Ctrl Pts',(-20.2198538481216,-4.36214110397647,
2.65590833175386));
#50008=CARTESIAN_POINT('Ctrl Pts',(-20.2842015351343,-3.40634621717809,
3.56831810142706));
#50009=CARTESIAN_POINT('Ctrl Pts',(-20.3637474235073,-2.22480330705116,
4.69622881676794));
#50010=CARTESIAN_POINT('Ctrl Pts',(-20.4432933118804,-0.427370559254853,
5.1789641106682));
#50011=CARTESIAN_POINT('Ctrl Pts',(-20.5228392002535,1.16027654508549,4.79477287920708));
#50012=CARTESIAN_POINT('Ctrl Pts',(-20.6023850886266,2.74792364942585,4.41058164774596));
#50013=CARTESIAN_POINT('Ctrl Pts',(-20.6819309769996,4.12578511031025,3.15946389092347));
#50014=CARTESIAN_POINT('Ctrl Pts',(-20.7614768653727,4.66092129423408,1.61613777667943));
#50015=CARTESIAN_POINT('Ctrl Pts',(-20.8410227537458,5.19605747815791,0.0728116624353919));
#50016=CARTESIAN_POINT('Ctrl Pts',(-20.9205686421189,4.88846838512118,-1.76272280923018));
#50017=CARTESIAN_POINT('Ctrl Pts',(-21.0001145304919,3.87944930013121,-3.04728760571889));
#50018=CARTESIAN_POINT('Ctrl Pts',(-21.079660418865,2.87043021514126,-4.33185240220757));
#50019=CARTESIAN_POINT('Ctrl Pts',(-21.1592063072381,1.1599811381981,-5.06544752351941));
#50020=CARTESIAN_POINT('Ctrl Pts',(-21.2387521956112,-0.466179596436317,
-4.91108594998304));
#50021=CARTESIAN_POINT('Ctrl Pts',(-21.3182980839842,-2.09234033107078,
-4.75672437644668));
#50022=CARTESIAN_POINT('Ctrl Pts',(-21.3978439723573,-3.6342127233965,-3.71440610806206));
#50023=CARTESIAN_POINT('Ctrl Pts',(-21.4773898607304,-4.38351646032473,
-2.26293439284383));
#50024=CARTESIAN_POINT('Ctrl Pts',(-21.5153127318524,-4.74074107152647,
-1.57095676937065));
#50025=CARTESIAN_POINT('Ctrl Pts',(-21.5532356029744,-4.9178283034161,-0.785985524275935));
#50026=CARTESIAN_POINT('Ctrl Pts',(-21.5911584740964,-4.91693164693359,
-0.000632398697534842));
#50027=CARTESIAN_POINT('Ctrl Pts',(-21.8088415259036,-4.91711569616659,
-0.00117946379282014));
#50028=CARTESIAN_POINT('Ctrl Pts',(-21.7725467009576,-4.91871955944082,
-0.752746704602252));
#50029=CARTESIAN_POINT('Ctrl Pts',(-21.7362518760116,-4.75716117024752,
-1.50366003608004));
#50030=CARTESIAN_POINT('Ctrl Pts',(-21.6999570510655,-4.42889215011132,
-2.17278619696736));
#50031=CARTESIAN_POINT('Ctrl Pts',(-21.6204111626925,-3.70943831968447,
-3.63928272865185));
#50032=CARTESIAN_POINT('Ctrl Pts',(-21.5408652743194,-2.18921161020874,
-4.71292520122458));
#50033=CARTESIAN_POINT('Ctrl Pts',(-21.4613193859463,-0.566549092315044,
-4.90052116218762));
#50034=CARTESIAN_POINT('Ctrl Pts',(-21.3817734975732,1.05611342557867,-5.08811712315067));
#50035=CARTESIAN_POINT('Ctrl Pts',(-21.3022276092002,2.78121175189034,-4.38966657250399));
#50036=CARTESIAN_POINT('Ctrl Pts',(-21.2226817208271,3.81629821795521,-3.12601238748351));
#50037=CARTESIAN_POINT('Ctrl Pts',(-21.143135832454,4.85138468402006,-1.86235820246306));
#50038=CARTESIAN_POINT('Ctrl Pts',(-21.0635899440809,5.19645928983812,-0.0335003830688158));
#50039=CARTESIAN_POINT('Ctrl Pts',(-20.9840440557079,4.69300726397856,1.52045005024925));
#50040=CARTESIAN_POINT('Ctrl Pts',(-20.9044981673348,4.189555238119,3.07440048356732));
#50041=CARTESIAN_POINT('Ctrl Pts',(-20.8249522789617,2.83757658058181,4.35344353080922));
#50042=CARTESIAN_POINT('Ctrl Pts',(-20.7454063905886,1.25812130277897,4.77003315738511));
#50043=CARTESIAN_POINT('Ctrl Pts',(-20.6658605022155,-0.321333975023885,
5.186622783961));
#50044=CARTESIAN_POINT('Ctrl Pts',(-20.5863146138425,-2.1282658730924,4.74075898987086));
#50045=CARTESIAN_POINT('Ctrl Pts',(-20.5067687254694,-3.33263534483166,
3.63725544792229));
#50046=CARTESIAN_POINT('Ctrl Pts',(-20.4407929922808,-4.33154503775366,
2.72200443061253));
#50047=CARTESIAN_POINT('Ctrl Pts',(-20.3748172590922,-4.91594471882842,
1.3543550430017));
#50048=CARTESIAN_POINT('Ctrl Pts',(-20.3088415259036,-4.92810468982102,
-0.00410855472338207));
#50049=CARTESIAN_POINT('Origin',(-14.75,0.,0.));
#50050=CARTESIAN_POINT('',(-18.5911584740964,-4.93133925263252,0.00269369058761092));
#50051=CARTESIAN_POINT('',(-18.8088415259036,-4.93057297854711,0.00316028518611533));
#50052=CARTESIAN_POINT('',(-14.75,-4.925,-6.03138548580071E-16));
#50053=CARTESIAN_POINT('Ctrl Pts',(-18.5911584740964,-4.93133925263252,
0.00269369058761092));
#50054=CARTESIAN_POINT('Ctrl Pts',(-18.5986849424975,-4.93235666587827,
0.157401246761113));
#50055=CARTESIAN_POINT('Ctrl Pts',(-18.6062114108986,-4.92571004477723,
0.312020226781154));
#50056=CARTESIAN_POINT('Ctrl Pts',(-18.6137378792997,-4.91111389702246,
0.465885087471429));
#50057=CARTESIAN_POINT('Ctrl Pts',(-18.6932837676727,-4.75684984141161,
2.0920550759408));
#50058=CARTESIAN_POINT('Ctrl Pts',(-18.7728296560458,-3.7146240379434,3.63398997126305));
#50059=CARTESIAN_POINT('Ctrl Pts',(-18.8523755444189,-2.26319725960073,
4.3833807487362));
#50060=CARTESIAN_POINT('Ctrl Pts',(-18.931921432792,-0.811770481258054,
5.13277152620935));
#50061=CARTESIAN_POINT('Ctrl Pts',(-19.0114673211651,1.04885727195908,5.08961818583339));
#50062=CARTESIAN_POINT('Ctrl Pts',(-19.0910132095381,2.46398102306833,4.27374380867811));
#50063=CARTESIAN_POINT('Ctrl Pts',(-19.1705590979112,3.87910477417757,3.45786943152285));
#50064=CARTESIAN_POINT('Ctrl Pts',(-19.2501049862843,4.84872452317893,1.86927401758828));
#50065=CARTESIAN_POINT('Ctrl Pts',(-19.3296508746573,4.92743208790438,0.237700743258566));
#50066=CARTESIAN_POINT('Ctrl Pts',(-19.4091967630304,5.00613965262983,-1.39387253107114));
#50067=CARTESIAN_POINT('Ctrl Pts',(-19.4887426514035,4.19393503307937,-3.068423665796));
#50068=CARTESIAN_POINT('Ctrl Pts',(-19.5682885397766,2.86391560429619,-4.01672454068289));
#50069=CARTESIAN_POINT('Ctrl Pts',(-19.6478344281497,1.53389617551299,-4.9650254155698));
#50070=CARTESIAN_POINT('Ctrl Pts',(-19.7273803165227,-0.313938062502946,
-5.18707603061872));
#50071=CARTESIAN_POINT('Ctrl Pts',(-19.8069262048958,-1.8307590101278,-4.58087437844472));
#50072=CARTESIAN_POINT('Ctrl Pts',(-19.8864720932689,-3.34757995775264,
-3.97467272627071));
#50073=CARTESIAN_POINT('Ctrl Pts',(-19.9660179816419,-4.5333876149864,-2.54021880687379));
#50074=CARTESIAN_POINT('Ctrl Pts',(-20.045563870015,-4.84346490737449,-0.936448778784566));
#50075=CARTESIAN_POINT('Ctrl Pts',(-20.0607620713755,-4.90270891386442,
-0.630029172173884));
#50076=CARTESIAN_POINT('Ctrl Pts',(-20.0759602727359,-4.92998463640529,
-0.317428729934899));
#50077=CARTESIAN_POINT('Ctrl Pts',(-20.0911584740964,-4.92710437571252,
-0.00432825790191715));
#50078=CARTESIAN_POINT('Ctrl Pts',(-20.3088415259036,-4.92810468982102,
-0.00410855472338207));
#50079=CARTESIAN_POINT('Ctrl Pts',(-20.2952713707191,-4.93060580175162,
-0.283522832407918));
#50080=CARTESIAN_POINT('Ctrl Pts',(-20.2817012155346,-4.90889778438975,
-0.562548496769959));
#50081=CARTESIAN_POINT('Ctrl Pts',(-20.2681310603502,-4.86160812861449,
-0.837169002561447));
#50082=CARTESIAN_POINT('Ctrl Pts',(-20.1885851719771,-4.58440439524805,
-2.44694662128967));
#50083=CARTESIAN_POINT('Ctrl Pts',(-20.109039283604,-3.42818988310517,-3.90535856893913));
#50084=CARTESIAN_POINT('Ctrl Pts',(-20.0294933952309,-1.9240876479818,-4.54246323682914));
#50085=CARTESIAN_POINT('Ctrl Pts',(-19.9499475068579,-0.419985412858412,
-5.17956790471916));
#50086=CARTESIAN_POINT('Ctrl Pts',(-19.8704016184848,1.43200454524547,-4.9953652928497));
#50087=CARTESIAN_POINT('Ctrl Pts',(-19.7908557301117,2.78114513946445,-4.07447140722498));
#50088=CARTESIAN_POINT('Ctrl Pts',(-19.7113098417387,4.13028573368341,-3.15357752160028));
#50089=CARTESIAN_POINT('Ctrl Pts',(-19.6317639533656,4.97657696401748,-1.49599236222033));
#50090=CARTESIAN_POINT('Ctrl Pts',(-19.5522180649925,4.93126330142958,0.136849505056872));
#50091=CARTESIAN_POINT('Ctrl Pts',(-19.4726721766194,4.88594963884169,1.76969137233409));
#50092=CARTESIAN_POINT('Ctrl Pts',(-19.3931262882463,3.94903108333184,3.37778994750857));
#50093=CARTESIAN_POINT('Ctrl Pts',(-19.3135803998733,2.55089407358275,4.22244300854623));
#50094=CARTESIAN_POINT('Ctrl Pts',(-19.2340345115002,1.15275706383363,5.06709606958391));
#50095=CARTESIAN_POINT('Ctrl Pts',(-19.1544886231271,-0.706598400154735,
5.14830361648474));
#50096=CARTESIAN_POINT('Ctrl Pts',(-19.074942734754,-2.17305178497508,4.42876184445237));
#50097=CARTESIAN_POINT('Ctrl Pts',(-18.995396846381,-3.63950516979541,3.70922007242002));
#50098=CARTESIAN_POINT('Ctrl Pts',(-18.9158509580079,-4.71305647544771,
2.18892898145449));
#50099=CARTESIAN_POINT('Ctrl Pts',(-18.8363050696348,-4.90055512820742,
0.566255216718109));
#50100=CARTESIAN_POINT('Ctrl Pts',(-18.8271505550577,-4.92213335412174,
0.379510295806119));
#50101=CARTESIAN_POINT('Ctrl Pts',(-18.8179960404807,-4.93197626646748,
0.191409368818455));
#50102=CARTESIAN_POINT('Ctrl Pts',(-18.8088415259036,-4.93057297854711,
0.00316028518611533));
#50103=CARTESIAN_POINT('Origin',(-14.75,0.,0.));
#50104=CARTESIAN_POINT('',(-17.0911584740964,-4.91873477802609,0.00299898967114021));
#50105=CARTESIAN_POINT('',(-17.3088415259036,-4.91816086074912,0.00255430743475421));
#50106=CARTESIAN_POINT('',(-14.75,-4.925,-6.03138548580071E-16));
#50107=CARTESIAN_POINT('Ctrl Pts',(-17.0911584740964,-4.91873477802609,
0.00299898967114021));
#50108=CARTESIAN_POINT('Ctrl Pts',(-17.121409612259,-4.92219933969977,0.628902743871938));
#50109=CARTESIAN_POINT('Ctrl Pts',(-17.1516607504217,-4.81148680932676,
1.25362658234333));
#50110=CARTESIAN_POINT('Ctrl Pts',(-17.1819118885843,-4.58098415721058,
1.83048430084528));
#50111=CARTESIAN_POINT('Ctrl Pts',(-17.2614577769574,-3.97487346688356,
3.34734159845876));
#50112=CARTESIAN_POINT('Ctrl Pts',(-17.3410036653305,-2.54049066060951,
4.53323527492929));
#50113=CARTESIAN_POINT('Ctrl Pts',(-17.4205495537035,-0.936739230126934,
4.84340874168148));
#50114=CARTESIAN_POINT('Ctrl Pts',(-17.5000954420766,0.667012200355664,
5.15358220843367));
#50115=CARTESIAN_POINT('Ctrl Pts',(-17.5796413304497,2.44013225504679,4.58803546546751));
#50116=CARTESIAN_POINT('Ctrl Pts',(-17.6591872188228,3.56811382315476,3.40656019604341));
#50117=CARTESIAN_POINT('Ctrl Pts',(-17.7387331071958,4.69609539126271,2.22508492661932));
#50118=CARTESIAN_POINT('Ctrl Pts',(-17.8182789955689,5.17893847278751,0.427681130737319));
#50119=CARTESIAN_POINT('Ctrl Pts',(-17.897824883942,4.79484245007892,-1.15998900993782));
#50120=CARTESIAN_POINT('Ctrl Pts',(-17.9773707723151,4.41074642737033,-2.74765915061299));
#50121=CARTESIAN_POINT('Ctrl Pts',(-18.0569166606881,3.15971130042833,-4.12559563608129));
#50122=CARTESIAN_POINT('Ctrl Pts',(-18.1364625490612,1.61641728001955,-4.66082436926233));
#50123=CARTESIAN_POINT('Ctrl Pts',(-18.2160084374343,0.0731232596108,-5.19605310244336));
#50124=CARTESIAN_POINT('Ctrl Pts',(-18.2955543258074,-1.76242965426471,
-4.88857408333716));
#50125=CARTESIAN_POINT('Ctrl Pts',(-18.3751002141804,-3.04705495732574,
-3.87963203297581));
#50126=CARTESIAN_POINT('Ctrl Pts',(-18.4471196341524,-4.21013165556918,
-2.96615400490252));
#50127=CARTESIAN_POINT('Ctrl Pts',(-18.5191390541244,-4.92160380860666,
-1.47767503842927));
#50128=CARTESIAN_POINT('Ctrl Pts',(-18.5911584740964,-4.93133925263252,
0.00269369058761092));
#50129=CARTESIAN_POINT('Ctrl Pts',(-18.8088415259036,-4.93057297854711,
0.00316028518611533));
#50130=CARTESIAN_POINT('Ctrl Pts',(-18.7384501521076,-4.91978274344346,
-1.4443344455465));
#50131=CARTESIAN_POINT('Ctrl Pts',(-18.6680587783116,-4.24406537670826,
-2.90058887915162));
#50132=CARTESIAN_POINT('Ctrl Pts',(-18.5976674045156,-3.12578352599411,
-3.8164856718825));
#50133=CARTESIAN_POINT('Ctrl Pts',(-18.5181215161425,-1.86206727115392,
-4.85149635723954));
#50134=CARTESIAN_POINT('Ctrl Pts',(-18.4385756277694,-0.0331887616064278,
-5.19646128944632));
#50135=CARTESIAN_POINT('Ctrl Pts',(-18.3590297393964,1.52073147789346,-4.69291607715336));
#50136=CARTESIAN_POINT('Ctrl Pts',(-18.2794838510233,3.07465171739332,-4.18937086486042));
#50137=CARTESIAN_POINT('Ctrl Pts',(-18.1999379626502,4.35361368684558,-2.83731550806776));
#50138=CARTESIAN_POINT('Ctrl Pts',(-18.1203920742771,4.77010859585846,-1.2578352510475));
#50139=CARTESIAN_POINT('Ctrl Pts',(-18.0408461859041,5.18660350487135,0.321645005972764));
#50140=CARTESIAN_POINT('Ctrl Pts',(-17.961300297531,4.74063135344486,2.12855016322063));
#50141=CARTESIAN_POINT('Ctrl Pts',(-17.8817544091579,3.63705558982148,3.33285345786593));
#50142=CARTESIAN_POINT('Ctrl Pts',(-17.8022085207848,2.53347982619808,4.53715675251125));
#50143=CARTESIAN_POINT('Ctrl Pts',(-17.7226626324118,0.772300450377784,
5.13885818455397));
#50144=CARTESIAN_POINT('Ctrl Pts',(-17.6431167440387,-0.837460542095409,
4.86155791650103));
#50145=CARTESIAN_POINT('Ctrl Pts',(-17.5635708556656,-2.44722153456857,
4.58425764844809));
#50146=CARTESIAN_POINT('Ctrl Pts',(-17.4840249672925,-3.90556414369463,
3.42795568029952));
#50147=CARTESIAN_POINT('Ctrl Pts',(-17.4044790789195,-4.5425786123982,1.92381524197179));
#50148=CARTESIAN_POINT('Ctrl Pts',(-17.3725998945808,-4.79787152683423,
1.32100884574773));
#50149=CARTESIAN_POINT('Ctrl Pts',(-17.3407207102422,-4.92124900075768,
0.662335296357207));
#50150=CARTESIAN_POINT('Ctrl Pts',(-17.3088415259036,-4.91816086074912,
0.00255430743475421));
#50151=CARTESIAN_POINT('Origin',(-14.75,0.,0.));
#50152=CARTESIAN_POINT('',(-15.5911584740964,-4.92035796642718,-0.00383015064837622));
#50153=CARTESIAN_POINT('',(-15.8088415259036,-4.92120003017842,-0.00410675641256026));
#50154=CARTESIAN_POINT('',(-14.75,-4.925,-6.03138548580071E-16));
#50155=CARTESIAN_POINT('Ctrl Pts',(-15.5911584740964,-4.92035796642718,
-0.00383015064837622));
#50156=CARTESIAN_POINT('Ctrl Pts',(-15.6441342820206,-4.9124462735778,1.09134504077847));
#50157=CARTESIAN_POINT('Ctrl Pts',(-15.6971100899448,-4.55169660768519,
2.19124987504687));
#50158=CARTESIAN_POINT('Ctrl Pts',(-15.750085897869,-3.87981475186871,3.04682229797494));
#50159=CARTESIAN_POINT('Ctrl Pts',(-15.829631786242,-2.87094973976422,4.33150810298851));
#50160=CARTESIAN_POINT('Ctrl Pts',(-15.9091776746151,-1.16058865962495,
5.06530836353102));
#50161=CARTESIAN_POINT('Ctrl Pts',(-15.9887235629882,0.465590576831222,
4.91114182640059));
#50162=CARTESIAN_POINT('Ctrl Pts',(-16.0682694513612,2.0917698132874,4.75697528927016));
#50163=CARTESIAN_POINT('Ctrl Pts',(-16.1478153397343,3.63376720606049,3.71484195446679));
#50164=CARTESIAN_POINT('Ctrl Pts',(-16.2273612281074,4.38324502138396,2.26346011821903));
#50165=CARTESIAN_POINT('Ctrl Pts',(-16.3069071164805,5.13272283670744,0.812078281971235));
#50166=CARTESIAN_POINT('Ctrl Pts',(-16.3864530048536,5.08968107458128,-1.04855205572096));
#50167=CARTESIAN_POINT('Ctrl Pts',(-16.4659988932266,4.27389156106992,-2.46372473066101));
#50168=CARTESIAN_POINT('Ctrl Pts',(-16.5455447815997,3.45810204755859,-3.87889740560104));
#50169=CARTESIAN_POINT('Ctrl Pts',(-16.6250906699728,1.86956478266209,-4.84861241778893));
#50170=CARTESIAN_POINT('Ctrl Pts',(-16.7046365583459,0.237996231203316,
-4.92741782460026));
#50171=CARTESIAN_POINT('Ctrl Pts',(-16.7841824467189,-1.39357232025546,
-5.00622323141159));
#50172=CARTESIAN_POINT('Ctrl Pts',(-16.863728335092,-3.06817215827651,-4.19411903284637));
#50173=CARTESIAN_POINT('Ctrl Pts',(-16.9432742234651,-4.01655279009705,
-2.86415647418555));
#50174=CARTESIAN_POINT('Ctrl Pts',(-16.9925689736755,-4.60426621320643,
-2.03997594821106));
#50175=CARTESIAN_POINT('Ctrl Pts',(-17.041863723886,-4.91308921515918,-1.01692194861672));
#50176=CARTESIAN_POINT('Ctrl Pts',(-17.0911584740964,-4.91873477802609,
0.00299898967114021));
#50177=CARTESIAN_POINT('Ctrl Pts',(-17.3088415259036,-4.91816086074912,
0.00255430743475421));
#50178=CARTESIAN_POINT('Ctrl Pts',(-17.2611748218691,-4.91354338201311,
-0.983969839246001));
#50179=CARTESIAN_POINT('Ctrl Pts',(-17.2135081178347,-4.62618522137736,
-1.9729699017009));
#50180=CARTESIAN_POINT('Ctrl Pts',(-17.1658414138002,-4.07430462011665,
-2.78138947246816));
#50181=CARTESIAN_POINT('Ctrl Pts',(-17.0862955254271,-3.15332983085048,
-4.13047484007342));
#50182=CARTESIAN_POINT('Ctrl Pts',(-17.0067496370541,-1.4956939240371,-4.97666666677702));
#50183=CARTESIAN_POINT('Ctrl Pts',(-16.927203748681,0.137145222933267,-4.93125508596819));
#50184=CARTESIAN_POINT('Ctrl Pts',(-16.8476578603079,1.76998436990362,-4.88584350515936));
#50185=CARTESIAN_POINT('Ctrl Pts',(-16.7681119719349,3.37802675703098,-3.94882851683809));
#50186=CARTESIAN_POINT('Ctrl Pts',(-16.6885660835618,4.2225959730343,-2.55064085742682));
#50187=CARTESIAN_POINT('Ctrl Pts',(-16.6090201951887,5.06716518903764,-1.15245319801552));
#50188=CARTESIAN_POINT('Ctrl Pts',(-16.5294743068156,5.14826123391693,0.706907132485781));
#50189=CARTESIAN_POINT('Ctrl Pts',(-16.4499284184425,4.42863152286466,2.17331736517013));
#50190=CARTESIAN_POINT('Ctrl Pts',(-16.3703825300695,3.7090018118124,3.63972759785445));
#50191=CARTESIAN_POINT('Ctrl Pts',(-16.2908366416964,2.18864634482861,4.71318773272181));
#50192=CARTESIAN_POINT('Ctrl Pts',(-16.2112907533233,0.565961339085978,
4.90058907660299));
#50193=CARTESIAN_POINT('Ctrl Pts',(-16.1317448649502,-1.05672366665665,
5.08799042048417));
#50194=CARTESIAN_POINT('Ctrl Pts',(-16.0521989765772,-2.78173821115814,
4.38933297337918));
#50195=CARTESIAN_POINT('Ctrl Pts',(-15.9726530882041,-3.81667311208576,
3.12555465326431));
#50196=CARTESIAN_POINT('Ctrl Pts',(-15.9180492341039,-4.52709869773482,
2.25804071360155));
#50197=CARTESIAN_POINT('Ctrl Pts',(-15.8634453800038,-4.91235438239858,
1.1242382374886));
#50198=CARTESIAN_POINT('Ctrl Pts',(-15.8088415259036,-4.92120003017842,
-0.00410675641256026));
#50199=CARTESIAN_POINT('Origin',(-14.75,0.,0.));
#50200=CARTESIAN_POINT('',(-14.0911584740964,-4.93264269199776,-0.00145718338004752));
#50201=CARTESIAN_POINT('',(-14.3088415259036,-4.93298263358733,-0.000852151517113329));
#50202=CARTESIAN_POINT('',(-14.75,-4.925,-6.03138548580071E-16));
#50203=CARTESIAN_POINT('Ctrl Pts',(-14.0911584740964,-4.93264269199776,
-0.00145718338004752));
#50204=CARTESIAN_POINT('Ctrl Pts',(-14.1668589517821,-4.92658863837471,
1.55348689693233));
#50205=CARTESIAN_POINT('Ctrl Pts',(-14.2425594294679,-4.13001266093176,
3.11377115163446));
#50206=CARTESIAN_POINT('Ctrl Pts',(-14.3182599071536,-2.86439733377493,
4.01638102506703));
#50207=CARTESIAN_POINT('Ctrl Pts',(-14.3978057955267,-1.5344916500192,4.96484141041069));
#50208=CARTESIAN_POINT('Ctrl Pts',(-14.4773516838997,0.313315942832746,
5.18711364580286));
#50209=CARTESIAN_POINT('Ctrl Pts',(-14.5568975722728,1.83020958498003,4.58109391950248));
#50210=CARTESIAN_POINT('Ctrl Pts',(-14.6364434606459,3.3471032271273,3.97507419320211));
#50211=CARTESIAN_POINT('Ctrl Pts',(-14.715989349019,4.53308291856992,2.5407625052092));
#50212=CARTESIAN_POINT('Ctrl Pts',(-14.7955352373921,4.84335255857077,0.937029678100604));
#50213=CARTESIAN_POINT('Ctrl Pts',(-14.8750811257651,5.15362219857162,-0.666703149008015));
#50214=CARTESIAN_POINT('Ctrl Pts',(-14.9546270141382,4.58818178713068,-2.43985711523233));
#50215=CARTESIAN_POINT('Ctrl Pts',(-15.0341729025113,3.40677416265819,-3.56790953205094));
#50216=CARTESIAN_POINT('Ctrl Pts',(-15.1137187908843,2.22536653818572,-4.69596194886955));
#50217=CARTESIAN_POINT('Ctrl Pts',(-15.1932646792574,0.427991700681723,
-5.17891281628248));
#50218=CARTESIAN_POINT('Ctrl Pts',(-15.2728105676305,-1.15970147061867,
-4.79491200370771));
#50219=CARTESIAN_POINT('Ctrl Pts',(-15.3523564560036,-2.74739464191907,
-4.41091119113294));
#50220=CARTESIAN_POINT('Ctrl Pts',(-15.4319023443767,-4.12540614701586,
-3.15995869857046));
#50221=CARTESIAN_POINT('Ctrl Pts',(-15.5114482327497,-4.6607274275294,-1.61669677754691));
#50222=CARTESIAN_POINT('Ctrl Pts',(-15.5380183131986,-4.83953653734212,
-1.10121327193814));
#50223=CARTESIAN_POINT('Ctrl Pts',(-15.5645883936475,-4.92432608553159,
-0.553116590668242));
#50224=CARTESIAN_POINT('Ctrl Pts',(-15.5911584740964,-4.92035796642718,
-0.00383015064837622));
#50225=CARTESIAN_POINT('Ctrl Pts',(-15.8088415259036,-4.92120003017842,
-0.00410675641256026));
#50226=CARTESIAN_POINT('Ctrl Pts',(-15.7838994916307,-4.92524055907015,
-0.519513955654037));
#50227=CARTESIAN_POINT('Ctrl Pts',(-15.7589574573578,-4.85074335816441,
-1.03378245448552));
#50228=CARTESIAN_POINT('Ctrl Pts',(-15.7340154230849,-4.69282487345136,
-1.52101290006915));
#50229=CARTESIAN_POINT('Ctrl Pts',(-15.6544695347118,-4.18918647653558,
-3.07490294016289));
#50230=CARTESIAN_POINT('Ctrl Pts',(-15.5749236463387,-2.83705442535027,
-4.35378382722562));
#50231=CARTESIAN_POINT('Ctrl Pts',(-15.4953777579656,-1.25754919479281,
-4.77018401717759));
#50232=CARTESIAN_POINT('Ctrl Pts',(-15.4158318695926,0.321956035764672,
-5.18658420712955));
#50233=CARTESIAN_POINT('Ctrl Pts',(-15.3362859812195,2.12883444569431,-4.74050369997076));
#50234=CARTESIAN_POINT('Ctrl Pts',(-15.2567400928464,3.33307155891485,-3.63685571864124));
#50235=CARTESIAN_POINT('Ctrl Pts',(-15.1771942044733,4.5373086721354,-2.53320773731172));
#50236=CARTESIAN_POINT('Ctrl Pts',(-15.0976483161003,5.13890448864684,-0.771992281811449));
#50237=CARTESIAN_POINT('Ctrl Pts',(-15.0181024277272,4.86150768690456,0.837752078617765));
#50238=CARTESIAN_POINT('Ctrl Pts',(-14.9385565393541,4.58411088516229,2.44749643904697));
#50239=CARTESIAN_POINT('Ctrl Pts',(-14.859010650981,3.42772146516635,3.90576970440512));
#50240=CARTESIAN_POINT('Ctrl Pts',(-14.779464762608,1.92354282904339,4.5426939716314));
#50241=CARTESIAN_POINT('Ctrl Pts',(-14.6999188742349,0.419364192920443,
5.17961823885768));
#50242=CARTESIAN_POINT('Ctrl Pts',(-14.6203729858618,-1.43260365932953,
4.99519350795208));
#50243=CARTESIAN_POINT('Ctrl Pts',(-14.5408270974887,-2.78163379546954,
4.07413781835645));
#50244=CARTESIAN_POINT('Ctrl Pts',(-14.463498573627,-4.09305932865878,3.17875682095258));
#50245=CARTESIAN_POINT('Ctrl Pts',(-14.3861700497653,-4.92919541411866,
1.58724007886021));
#50246=CARTESIAN_POINT('Ctrl Pts',(-14.3088415259036,-4.93298263358733,
-0.000852151517113329));
#50247=CARTESIAN_POINT('Origin',(-14.75,0.,0.));
#50248=CARTESIAN_POINT('',(-12.5911584740964,-4.92478776395509,0.00455105250847659));
#50249=CARTESIAN_POINT('',(-12.8088415259036,-4.92377532403654,0.00452825219503028));
#50250=CARTESIAN_POINT('',(-14.75,-4.925,-6.03138548580071E-16));
#50251=CARTESIAN_POINT('Ctrl Pts',(-12.5911584740964,-4.92478776395509,
0.00455105250847659));
#50252=CARTESIAN_POINT('Ctrl Pts',(-12.6100377331706,-4.92837678960448,
0.393954978247036));
#50253=CARTESIAN_POINT('Ctrl Pts',(-12.6289169922448,-4.88609691325311,
0.78258860004133));
#50254=CARTESIAN_POINT('Ctrl Pts',(-12.647796251319,-4.79498154009321,1.15941392712904));
#50255=CARTESIAN_POINT('Ctrl Pts',(-12.7273421396921,-4.41107593903318,
2.74713012334508));
#50256=CARTESIAN_POINT('Ctrl Pts',(-12.8068880280651,-3.16020608534884,
4.12521664311483));
#50257=CARTESIAN_POINT('Ctrl Pts',(-12.8864339164382,-1.61697626926029,
4.66063046903576));
#50258=CARTESIAN_POINT('Ctrl Pts',(-12.9659798048113,-0.0737464531717311,
5.19604429495669));
#50259=CARTESIAN_POINT('Ctrl Pts',(-13.0455256931844,1.76184332532101,4.8887854270288));
#50260=CARTESIAN_POINT('Ctrl Pts',(-13.1250715815575,3.04658962766721,3.87999745680921));
#50261=CARTESIAN_POINT('Ctrl Pts',(-13.2046174699305,4.33133593001341,2.87120948658962));
#50262=CARTESIAN_POINT('Ctrl Pts',(-13.2841633583036,5.06523875621307,1.16089241407827));
#50263=CARTESIAN_POINT('Ctrl Pts',(-13.3637092466767,4.91116973811745,-0.465296064516709));
#50264=CARTESIAN_POINT('Ctrl Pts',(-13.4432551350498,4.75710072002183,-2.09148454311171));
#50265=CARTESIAN_POINT('Ctrl Pts',(-13.5228010234228,3.71505985763101,-3.63354442779033));
#50266=CARTESIAN_POINT('Ctrl Pts',(-13.6023469117959,2.26372296869752,-4.38310927826887));
#50267=CARTESIAN_POINT('Ctrl Pts',(-13.681892800169,0.812386079764056,-5.13267412874741));
#50268=CARTESIAN_POINT('Ctrl Pts',(-13.7614386885421,-1.0482468357121,-5.08974394502581));
#50269=CARTESIAN_POINT('Ctrl Pts',(-13.8409845769151,-2.46346842939373,
-4.27403929809212));
#50270=CARTESIAN_POINT('Ctrl Pts',(-13.9205304652882,-3.87869002307536,
-3.45833465115842));
#50271=CARTESIAN_POINT('Ctrl Pts',(-14.0000763536613,-4.84850029496252,
-1.86985554101265));
#50272=CARTESIAN_POINT('Ctrl Pts',(-14.0796222420344,-4.92740354357634,
-0.238291718292194));
#50273=CARTESIAN_POINT('Ctrl Pts',(-14.0834676527217,-4.93121788774538,
-0.159418591229293));
#50274=CARTESIAN_POINT('Ctrl Pts',(-14.0873130634091,-4.93295022404004,
-0.0804447772164642));
#50275=CARTESIAN_POINT('Ctrl Pts',(-14.0911584740964,-4.93264269199776,
-0.00145718338004752));
#50276=CARTESIAN_POINT('Ctrl Pts',(-14.3088415259036,-4.93298263358733,
-0.000852151517113329));
#50277=CARTESIAN_POINT('Ctrl Pts',(-14.3066241613922,-4.93309123059174,
-0.0463900614183807));
#50278=CARTESIAN_POINT('Ctrl Pts',(-14.3044067968809,-4.93251544314009,
-0.0919251555741316));
#50279=CARTESIAN_POINT('Ctrl Pts',(-14.3021894323695,-4.93124685277319,
-0.137440940316469));
#50280=CARTESIAN_POINT('Ctrl Pts',(-14.2226435439964,-4.88573735390672,
-1.77027736110802));
#50281=CARTESIAN_POINT('Ctrl Pts',(-14.1430976556234,-3.94862593614372,
-3.37826355440545));
#50282=CARTESIAN_POINT('Ctrl Pts',(-14.0635517672503,-2.55038763209838,
-4.22274892233722));
#50283=CARTESIAN_POINT('Ctrl Pts',(-13.9840058788772,-1.15214932805305,
-5.06723429026899));
#50284=CARTESIAN_POINT('Ctrl Pts',(-13.9044599905041,0.707215862274635,
-5.14821883283511));
#50285=CARTESIAN_POINT('Ctrl Pts',(-13.8249141021311,2.17358293754952,-4.42850118535088));
#50286=CARTESIAN_POINT('Ctrl Pts',(-13.745368213758,3.6399500128244,-3.70878353786665));
#50287=CARTESIAN_POINT('Ctrl Pts',(-13.6658223253849,4.71331897304647,-2.18836370033207));
#50288=CARTESIAN_POINT('Ctrl Pts',(-13.5862764370118,4.90062300737523,-0.565667459418628));
#50289=CARTESIAN_POINT('Ctrl Pts',(-13.5067305486388,5.08792704170398,1.05702878149484));
#50290=CARTESIAN_POINT('Ctrl Pts',(-13.4271846602657,4.38916615013937,2.78200142578717));
#50291=CARTESIAN_POINT('Ctrl Pts',(-13.3476387718926,3.12532576929452,3.81686053856362));
#50292=CARTESIAN_POINT('Ctrl Pts',(-13.2680928835195,1.86148538844969,4.85171965134006));
#50293=CARTESIAN_POINT('Ctrl Pts',(-13.1885469951465,0.0325655183246379,
5.19646523260064));
#50294=CARTESIAN_POINT('Ctrl Pts',(-13.1090011067734,-1.52129431677496,
4.69273365287321));
#50295=CARTESIAN_POINT('Ctrl Pts',(-13.0294552184003,-3.07515415187458,
4.18900207314577));
#50296=CARTESIAN_POINT('Ctrl Pts',(-12.9499093300272,-4.35395395194874,
2.8367933324303));
#50297=CARTESIAN_POINT('Ctrl Pts',(-12.8703634416541,-4.77025942134235,
1.25726313401576));
#50298=CARTESIAN_POINT('Ctrl Pts',(-12.849856136404,-4.87758493511541,0.850052798028952));
#50299=CARTESIAN_POINT('Ctrl Pts',(-12.8293488311538,-4.92758625344338,
0.427733934129015));
#50300=CARTESIAN_POINT('Ctrl Pts',(-12.8088415259036,-4.92377532403654,
0.00452825219503028));
#50301=CARTESIAN_POINT('Origin',(-14.75,0.,0.));
#50302=CARTESIAN_POINT('',(-11.0911584740964,-4.91693014897725,-0.000625914149278983));
#50303=CARTESIAN_POINT('',(-11.3088415259036,-4.91711289028958,-0.00117313378838655));
#50304=CARTESIAN_POINT('',(-14.75,-4.925,-6.03138548580071E-16));
#50305=CARTESIAN_POINT('Ctrl Pts',(-11.0911584740964,-4.91693014897725,
-0.000625914149278983));
#50306=CARTESIAN_POINT('Ctrl Pts',(-11.1327624029322,-4.91595655984975,
0.8609597041095));
#50307=CARTESIAN_POINT('Ctrl Pts',(-11.1743663317679,-4.70077081773724,
1.72300021548812));
#50308=CARTESIAN_POINT('Ctrl Pts',(-11.2159702606036,-4.27418701974417,
2.46321211926741));
#50309=CARTESIAN_POINT('Ctrl Pts',(-11.2955161489767,-3.45856724232153,
3.87848262660126));
#50310=CARTESIAN_POINT('Ctrl Pts',(-11.3750620373498,-1.87014629263889,
4.84838815470011));
#50311=CARTESIAN_POINT('Ctrl Pts',(-11.4546079257229,-0.238587204524135,
4.92738924483267));
#50312=CARTESIAN_POINT('Ctrl Pts',(-11.5341538140959,1.39297188359064,5.00639033496524));
#50313=CARTESIAN_POINT('Ctrl Pts',(-11.613699702469,3.06766911013748,4.19448698713153));
#50314=CARTESIAN_POINT('Ctrl Pts',(-11.6932455908421,4.01620924559344,2.86463818306347));
#50315=CARTESIAN_POINT('Ctrl Pts',(-11.7727914792152,4.96474938104939,1.53478937899541));
#50316=CARTESIAN_POINT('Ctrl Pts',(-11.8523373675882,5.18713242541439,-0.313004881306989));
#50317=CARTESIAN_POINT('Ctrl Pts',(-11.9318832559613,4.58120366532001,-1.82993486253306));
#50318=CARTESIAN_POINT('Ctrl Pts',(-12.0114291443344,3.97527490522564,-3.34686484375911));
#50319=CARTESIAN_POINT('Ctrl Pts',(-12.0909750327075,2.54103434067188,-4.53293054590886));
#50320=CARTESIAN_POINT('Ctrl Pts',(-12.1705209210806,0.937320122704561,
-4.84329635804258));
#50321=CARTESIAN_POINT('Ctrl Pts',(-12.2500668094536,-0.666394095262762,
-5.1536621701763));
#50322=CARTESIAN_POINT('Ctrl Pts',(-12.3296126978267,-2.43958196664368,
-4.588328092294));
#50323=CARTESIAN_POINT('Ctrl Pts',(-12.4091585861998,-3.56770522811629,
-3.4069881170217));
#50324=CARTESIAN_POINT('Ctrl Pts',(-12.4698252154987,-4.42808201322696,
-2.50602496453717));
#50325=CARTESIAN_POINT('Ctrl Pts',(-12.5304918447975,-4.91325478547539,
-1.24675989764379));
#50326=CARTESIAN_POINT('Ctrl Pts',(-12.5911584740964,-4.92478776395509,
0.00455105250847659));
#50327=CARTESIAN_POINT('Ctrl Pts',(-12.8088415259036,-4.92377532403654,
0.00452825219503028));
#50328=CARTESIAN_POINT('Ctrl Pts',(-12.7498029427807,-4.91280402040514,
-1.21384069126802));
#50329=CARTESIAN_POINT('Ctrl Pts',(-12.6907643596578,-4.45583175677877,
-2.43955966583319));
#50330=CARTESIAN_POINT('Ctrl Pts',(-12.6317257765349,-3.63665583438227,
-3.33328964797749));
#50331=CARTESIAN_POINT('Ctrl Pts',(-12.5521798881619,-2.53293563931553,
-4.53746057544264));
#50332=CARTESIAN_POINT('Ctrl Pts',(-12.4726339997888,-0.771684110468958,
-5.13895077425935));
#50333=CARTESIAN_POINT('Ctrl Pts',(-12.3930881114157,0.838043612127357,
-4.86145743982533));
#50334=CARTESIAN_POINT('Ctrl Pts',(-12.3135422230426,2.44777133472372,-4.58396410539131));
#50335=CARTESIAN_POINT('Ctrl Pts',(-12.2339963346695,3.90597525106984,-3.42748723770652));
#50336=CARTESIAN_POINT('Ctrl Pts',(-12.1544504462965,4.54280931452835,-1.92327040919758));
#50337=CARTESIAN_POINT('Ctrl Pts',(-12.0749045579234,5.17964337798684,-0.419053580688679));
#50338=CARTESIAN_POINT('Ctrl Pts',(-11.9953586695503,4.99510758855781,1.43290320864429));
#50339=CARTESIAN_POINT('Ctrl Pts',(-11.9158127811772,4.07397100194497,2.78187810846774));
#50340=CARTESIAN_POINT('Ctrl Pts',(-11.8362668928042,3.15283441533213,4.13085300829118));
#50341=CARTESIAN_POINT('Ctrl Pts',(-11.7567210044311,1.49509703153545,4.97684601860504));
#50342=CARTESIAN_POINT('Ctrl Pts',(-11.677175116058,-0.137736657205341,
4.93123860184462));
#50343=CARTESIAN_POINT('Ctrl Pts',(-11.5976292276849,-1.77057034594614,
4.88563118508419));
#50344=CARTESIAN_POINT('Ctrl Pts',(-11.5180833393119,-3.37850033963107,
3.94842334124948));
#50345=CARTESIAN_POINT('Ctrl Pts',(-11.4385374509388,-4.22290185645441,
2.55013439759839));
#50346=CARTESIAN_POINT('Ctrl Pts',(-11.3953054759271,-4.68182117990154,
1.79018572008053));
#50347=CARTESIAN_POINT('Ctrl Pts',(-11.3520735009153,-4.91521278868756,
0.894044916314203));
#50348=CARTESIAN_POINT('Ctrl Pts',(-11.3088415259036,-4.91711289028958,
-0.00117313378838655));
#50349=CARTESIAN_POINT('Origin',(-14.75,0.,0.));
#50350=CARTESIAN_POINT('',(-9.59115847409641,-4.92709248349153,-0.00433039759252629));
#50351=CARTESIAN_POINT('',(-9.80884152590359,-4.92809314710804,-0.00411155299795817));
#50352=CARTESIAN_POINT('',(-14.75,-4.925,-6.03138548580071E-16));
#50353=CARTESIAN_POINT('Ctrl Pts',(-9.59115847409641,-4.92709248349153,
-0.00433039759252629));
#50354=CARTESIAN_POINT('Ctrl Pts',(-9.6554870726937,-4.91489864183716,1.32092114795559));
#50355=CARTESIAN_POINT('Ctrl Pts',(-9.71981567129099,-4.36249459000914,
2.65513262914084));
#50356=CARTESIAN_POINT('Ctrl Pts',(-9.78414426988828,-3.40720205913308,
3.56750091135165));
#50357=CARTESIAN_POINT('Ctrl Pts',(-9.86369015826136,-2.2259297373092,4.69569501342137));
#50358=CARTESIAN_POINT('Ctrl Pts',(-9.94323604663443,-0.428612835952052,
5.17886144739986));
#50359=CARTESIAN_POINT('Ctrl Pts',(-10.0227819350075,1.15912637946997,4.79505105923515));
#50360=CARTESIAN_POINT('Ctrl Pts',(-10.1023278233806,2.74686559489197,4.41124067107045));
#50361=CARTESIAN_POINT('Ctrl Pts',(-10.1818737117537,4.12502712437884,3.16045346076258));
#50362=CARTESIAN_POINT('Ctrl Pts',(-10.2614196001267,4.66053349378172,1.61725575515876));
#50363=CARTESIAN_POINT('Ctrl Pts',(-10.3409654884998,5.19603986318461,0.0740580495549087));
#50364=CARTESIAN_POINT('Ctrl Pts',(-10.4205113768729,4.88889107250348,-1.76155015134491));
#50365=CARTESIAN_POINT('Ctrl Pts',(-10.500057265246,3.88018014779652,-3.04635694640356));
#50366=CARTESIAN_POINT('Ctrl Pts',(-10.579603153619,2.87146922308957,-4.3311637414622));
#50367=CARTESIAN_POINT('Ctrl Pts',(-10.6591490419921,1.16119616435681,-5.06516913067968));
#50368=CARTESIAN_POINT('Ctrl Pts',(-10.7386949303652,-0.465001550528919,
-4.91119763217294));
#50369=CARTESIAN_POINT('Ctrl Pts',(-10.8182408187383,-2.09119926541465,
-4.75722613366619));
#50370=CARTESIAN_POINT('Ctrl Pts',(-10.8977867071114,-3.63332163645336,
-3.71527774743521));
#50371=CARTESIAN_POINT('Ctrl Pts',(-10.9773325954844,-4.3829735193914,-2.26398581103529));
#50372=CARTESIAN_POINT('Ctrl Pts',(-11.0152745550218,-4.74054399840997,
-1.5717456330203));
#50373=CARTESIAN_POINT('Ctrl Pts',(-11.0532165145591,-4.91781804298907,
-0.786374942684098));
#50374=CARTESIAN_POINT('Ctrl Pts',(-11.0911584740964,-4.91693014897725,
-0.000625914149278983));
#50375=CARTESIAN_POINT('Ctrl Pts',(-11.3088415259036,-4.91711289028958,
-0.00117313378838655));
#50376=CARTESIAN_POINT('Ctrl Pts',(-11.2725276125423,-4.91870893407279,
-0.753136714034694));
#50377=CARTESIAN_POINT('Ctrl Pts',(-11.2362136991809,-4.7569730771308,-1.5044492332048));
#50378=CARTESIAN_POINT('Ctrl Pts',(-11.1998997858196,-4.42837083191147,
-2.1738485021124));
#50379=CARTESIAN_POINT('Ctrl Pts',(-11.1203538974465,-3.70856525058346,
-3.64017241470453));
#50380=CARTESIAN_POINT('Ctrl Pts',(-11.0408080090734,-2.18808104796575,
-4.71345019642131));
#50381=CARTESIAN_POINT('Ctrl Pts',(-10.9612621207003,-0.565373577716975,
-4.90065692052403));
#50382=CARTESIAN_POINT('Ctrl Pts',(-10.8817162323273,1.05733389253182,-5.08786364462675));
#50383=CARTESIAN_POINT('Ctrl Pts',(-10.8021703439542,2.78226463041168,-4.38899931111538));
#50384=CARTESIAN_POINT('Ctrl Pts',(-10.7226244555811,3.81704795131542,-3.12509687408555));
#50385=CARTESIAN_POINT('Ctrl Pts',(-10.643078567208,4.85183127221915,-1.86119443705574));
#50386=CARTESIAN_POINT('Ctrl Pts',(-10.563532678835,5.1964671761468,-0.0322538965074959));
#50387=CARTESIAN_POINT('Ctrl Pts',(-10.4839867904619,4.6926424154192,1.52157572801001));
#50388=CARTESIAN_POINT('Ctrl Pts',(-10.4044409020888,4.1888176546916,3.07540535252754));
#50389=CARTESIAN_POINT('Ctrl Pts',(-10.3248950137157,2.83653222930873,4.35412406101433));
#50390=CARTESIAN_POINT('Ctrl Pts',(-10.2453491253427,1.25697706871738,4.77033480835247));
#50391=CARTESIAN_POINT('Ctrl Pts',(-10.1658032369696,-0.322578091873937,
5.1865455556906));
#50392=CARTESIAN_POINT('Ctrl Pts',(-10.0862573485965,-2.12940298767373,
4.74024834188012));
#50393=CARTESIAN_POINT('Ctrl Pts',(-10.0067114602234,-3.33350772505308,
3.6364559370453));
#50394=CARTESIAN_POINT('Ctrl Pts',(-9.94075481545016,-4.33190890024233,
2.72123020963015));
#50395=CARTESIAN_POINT('Ctrl Pts',(-9.87479817067687,-4.91593144188893,
1.35396723904141));
#50396=CARTESIAN_POINT('Ctrl Pts',(-9.80884152590359,-4.92809314710804,
-0.00411155299795817));
#50397=CARTESIAN_POINT('Origin',(-14.75,0.,0.));
#50398=CARTESIAN_POINT('',(-8.09115847409641,-4.93134763236354,0.00268789096151988));
#50399=CARTESIAN_POINT('',(-8.3088415259036,-4.93058250867777,0.00315514943839852));
#50400=CARTESIAN_POINT('',(-14.75,-4.925,-6.03138548580071E-16));
#50401=CARTESIAN_POINT('Ctrl Pts',(-8.09115847409641,-4.93134763236354,
0.00268789096151988));
#50402=CARTESIAN_POINT('Ctrl Pts',(-8.09866585408217,-4.93236070319556,
0.157002391239283));
#50403=CARTESIAN_POINT('Ctrl Pts',(-8.10617323406794,-4.92574782328456,
0.311228913952019));
#50404=CARTESIAN_POINT('Ctrl Pts',(-8.11368061405371,-4.91122550856618,
0.464707034867637));
#50405=CARTESIAN_POINT('Ctrl Pts',(-8.19322650242678,-4.7573515302013,2.09091398019483));
#50406=CARTESIAN_POINT('Ctrl Pts',(-8.27277239079985,-3.71549562387871,
3.63309883205044));
#50407=CARTESIAN_POINT('Ctrl Pts',(-8.35231827917293,-2.2642486452318,4.38283774475274));
#50408=CARTESIAN_POINT('Ctrl Pts',(-8.431864167546,-0.813001666584828,5.13257665745506));
#50409=CARTESIAN_POINT('Ctrl Pts',(-8.51141005591908,1.0476363843865,5.089869631004));
#50410=CARTESIAN_POINT('Ctrl Pts',(-8.59095594429216,2.46295580028325,4.27433472602514));
#50411=CARTESIAN_POINT('Ctrl Pts',(-8.67050183266523,3.87827521617993,3.45879982104632));
#50412=CARTESIAN_POINT('Ctrl Pts',(-8.75004772103831,4.84827599700209,1.87043703753978));
#50413=CARTESIAN_POINT('Ctrl Pts',(-8.82959360941138,4.9273749283692,0.238882689898267));
#50414=CARTESIAN_POINT('Ctrl Pts',(-8.90913949778446,5.0064738597363,-1.39267165774325));
#50415=CARTESIAN_POINT('Ctrl Pts',(-8.98868538615753,4.19467094164835,-3.06741756951973));
#50416=CARTESIAN_POINT('Ctrl Pts',(-9.0682312745306,2.86487902205042,-4.01603745167696));
#50417=CARTESIAN_POINT('Ctrl Pts',(-9.14777716290368,1.53508710245243,-4.96465733383422));
#50418=CARTESIAN_POINT('Ctrl Pts',(-9.22732305127675,-0.312693818655589,
-5.18715118637216));
#50419=CARTESIAN_POINT('Ctrl Pts',(-9.30686893964983,-1.82966013350537,
-4.58131339466273));
#50420=CARTESIAN_POINT('Ctrl Pts',(-9.38641482802291,-3.3466264483551,-3.97547560295332));
#50421=CARTESIAN_POINT('Ctrl Pts',(-9.46596071639599,-4.53277815694662,
-2.54130616699661));
#50422=CARTESIAN_POINT('Ctrl Pts',(-9.54550660476906,-4.84324014009708,
-0.937610563937788));
#50423=CARTESIAN_POINT('Ctrl Pts',(-9.56072389454484,-4.9026321471334,-0.630820342557176));
#50424=CARTESIAN_POINT('Ctrl Pts',(-9.57594118432063,-4.9299770049327,-0.317826062571257));
#50425=CARTESIAN_POINT('Ctrl Pts',(-9.59115847409641,-4.92709248349153,
-0.00433039759252629));
#50426=CARTESIAN_POINT('Ctrl Pts',(-9.80884152590359,-4.92809314710804,
-0.00411155299795817));
#50427=CARTESIAN_POINT('Ctrl Pts',(-9.7952522823038,-4.93059885938888,-0.283920563844114));
#50428=CARTESIAN_POINT('Ctrl Pts',(-9.781663038704,-4.90882931597747,-0.563339710114124));
#50429=CARTESIAN_POINT('Ctrl Pts',(-9.7680737951042,-4.86140717526349,-0.838335142623281));
#50430=CARTESIAN_POINT('Ctrl Pts',(-9.68852790673113,-4.58381730913562,
-2.44804622159789));
#50431=CARTESIAN_POINT('Ctrl Pts',(-9.60898201835805,-3.42725299792094,
-3.90618078368793));
#50432=CARTESIAN_POINT('Ctrl Pts',(-9.52943612998497,-1.9229979824355,-4.54292464108855));
#50433=CARTESIAN_POINT('Ctrl Pts',(-9.4498902416119,-0.418742966950077,
-5.17966849848915));
#50434=CARTESIAN_POINT('Ctrl Pts',(-9.37034435323882,1.43320275280612,-4.99502165120035));
#50435=CARTESIAN_POINT('Ctrl Pts',(-9.29079846486575,2.78212241146185,-4.07380417088284));
#50436=CARTESIAN_POINT('Ctrl Pts',(-9.21125257649268,4.1310420701176,-3.15258669056531));
#50437=CARTESIAN_POINT('Ctrl Pts',(-9.13170668811961,4.97693566767287,-1.49479857721911));
#50438=CARTESIAN_POINT('Ctrl Pts',(-9.05216079974653,4.93123033318249,0.138032373598989));
#50439=CARTESIAN_POINT('Ctrl Pts',(-8.97261491137345,4.8855249986921,1.77086332441709));
#50440=CARTESIAN_POINT('Ctrl Pts',(-8.89306902300037,3.94822073215603,3.37873711270705));
#50441=CARTESIAN_POINT('Ctrl Pts',(-8.8135231346273,2.54988115392759,4.22305477538536));
#50442=CARTESIAN_POINT('Ctrl Pts',(-8.73397724625422,1.15154157569918,5.06737243806365));
#50443=CARTESIAN_POINT('Ctrl Pts',(-8.65443135788115,-0.707833314221602,
5.14813397513033));
#50444=CARTESIAN_POINT('Ctrl Pts',(-8.57488546950808,-2.17411405885781,
4.428240462547));
#50445=CARTESIAN_POINT('Ctrl Pts',(-8.495339581135,-3.64039480349401,3.70834694996368));
#50446=CARTESIAN_POINT('Ctrl Pts',(-8.41579369276192,-4.71358140284566,
2.18779838773033));
#50447=CARTESIAN_POINT('Ctrl Pts',(-8.33624780438885,-4.90069081604919,
0.565079693981939));
#50448=CARTESIAN_POINT('Ctrl Pts',(-8.3271123782271,-4.92217934629819,0.378719001918263));
#50449=CARTESIAN_POINT('Ctrl Pts',(-8.31797695206535,-4.93198112784769,
0.191010756085821));
#50450=CARTESIAN_POINT('Ctrl Pts',(-8.3088415259036,-4.93058250867777,0.00315514943839852));
#50451=CARTESIAN_POINT('Origin',(-14.75,0.,0.));
#50452=CARTESIAN_POINT('',(-6.5911584740964,-4.91874206214364,0.00300395193210873));
#50453=CARTESIAN_POINT('',(-6.8088415259036,-4.91816702752264,0.00255975366377111));
#50454=CARTESIAN_POINT('',(-14.75,-4.925,-6.03138548580071E-16));
#50455=CARTESIAN_POINT('Ctrl Pts',(-6.5911584740964,-4.91874206214364,0.00300395193210873));
#50456=CARTESIAN_POINT('Ctrl Pts',(-6.62139052384371,-4.92221047690888,
0.628510441243254));
#50457=CARTESIAN_POINT('Ctrl Pts',(-6.65162257359103,-4.81164202146414,
1.2528364358832));
#50458=CARTESIAN_POINT('Ctrl Pts',(-6.68185462333834,-4.5814231074921,1.8293853978311));
#50459=CARTESIAN_POINT('Ctrl Pts',(-6.76140051171141,-3.97567628631209,
3.34638804078933));
#50460=CARTESIAN_POINT('Ctrl Pts',(-6.84094640008449,-2.54157798418442,
4.53262575168735));
#50461=CARTESIAN_POINT('Ctrl Pts',(-6.92049228845757,-0.937901001819111,
4.8431839047693));
#50462=CARTESIAN_POINT('Ctrl Pts',(-7.00003817683064,0.665775980546221,
5.15374205785124));
#50463=CARTESIAN_POINT('Ctrl Pts',(-7.07958406520371,2.43903164314918,4.58862065311707));
#50464=CARTESIAN_POINT('Ctrl Pts',(-7.15912995357679,3.5672965817681,3.40741598897341));
#50465=CARTESIAN_POINT('Ctrl Pts',(-7.23867584194987,4.69556152038701,2.22621132482977));
#50466=CARTESIAN_POINT('Ctrl Pts',(-7.31822173032295,5.17883573502188,0.428923401276672));
#50467=CARTESIAN_POINT('Ctrl Pts',(-7.39776761869602,4.79512056112791,-1.15883882763304));
#50468=CARTESIAN_POINT('Ctrl Pts',(-7.4773135070691,4.41140538723394,-2.74660105654276));
#50469=CARTESIAN_POINT('Ctrl Pts',(-7.55685939544217,3.16070082481106,-4.12483759080913));
#50470=CARTESIAN_POINT('Ctrl Pts',(-7.63640528381525,1.61753523524406,-4.66043650177258));
#50471=CARTESIAN_POINT('Ctrl Pts',(-7.71595117218832,0.0743696456770546,
-5.19603541273603));
#50472=CARTESIAN_POINT('Ctrl Pts',(-7.7954970605614,-1.76125697103409,-4.88899670039663));
#50473=CARTESIAN_POINT('Ctrl Pts',(-7.87504294893448,-3.04612425418612,
-3.88036282482753));
#50474=CARTESIAN_POINT('Ctrl Pts',(-7.94708145732179,-4.20972836304737,
-2.96692177349214));
#50475=CARTESIAN_POINT('Ctrl Pts',(-8.0191199657091,-4.92162651637264,-1.47806657246253));
#50476=CARTESIAN_POINT('Ctrl Pts',(-8.09115847409641,-4.93134763236354,
0.00268789096151988));
#50477=CARTESIAN_POINT('Ctrl Pts',(-8.3088415259036,-4.93058250867777,0.00315514943839852));
#50478=CARTESIAN_POINT('Ctrl Pts',(-8.23843106369227,-4.91980277925207,
-1.44472476977317));
#50479=CARTESIAN_POINT('Ctrl Pts',(-8.16802060148095,-4.24367279446414,
-2.90135853255996));
#50480=CARTESIAN_POINT('Ctrl Pts',(-8.09761013926962,-3.12486796763837,
-3.8172353503401));
#50481=CARTESIAN_POINT('Ctrl Pts',(-8.01806425089654,-1.86090347896865,
-4.85194287565023));
#50482=CARTESIAN_POINT('Ctrl Pts',(-7.93851836252347,-0.0319422745738374,
-5.19646910100704));
#50483=CARTESIAN_POINT('Ctrl Pts',(-7.85897247415039,1.52185713377351,-4.69255116109043));
#50484=CARTESIAN_POINT('Ctrl Pts',(-7.77942658577732,3.07565654212083,-4.18863322117384));
#50485=CARTESIAN_POINT('Ctrl Pts',(-7.69988069740424,4.35429415442072,-2.83627111598379));
#50486=CARTESIAN_POINT('Ctrl Pts',(-7.62033480903117,4.77041017820713,-1.25669099889733));
#50487=CARTESIAN_POINT('Ctrl Pts',(-7.54078892065809,5.18652620199355,0.322889118189166));
#50488=CARTESIAN_POINT('Ctrl Pts',(-7.46124303228501,4.7401206372665,2.12968724717213));
#50489=CARTESIAN_POINT('Ctrl Pts',(-7.38169714391194,3.63625602663207,3.33372579013805));
#50490=CARTESIAN_POINT('Ctrl Pts',(-7.30215125553886,2.53239141599764,4.53776433310397));
#50491=CARTESIAN_POINT('Ctrl Pts',(-7.22260536716579,0.771067759455849,
5.13904329005283));
#50492=CARTESIAN_POINT('Ctrl Pts',(-7.14305947879271,-0.838626670106471,
4.86135689322456));
#50493=CARTESIAN_POINT('Ctrl Pts',(-7.06351359041964,-2.44832109966874,
4.58367049639629));
#50494=CARTESIAN_POINT('Ctrl Pts',(-6.98396770204656,-3.90638630225154,
3.42701874579095));
#50495=CARTESIAN_POINT('Ctrl Pts',(-6.90442181367349,-4.54303995130782,
1.92272554874775));
#50496=CARTESIAN_POINT('Ctrl Pts',(-6.87256171775019,-4.79803548588176,
1.32021891346095));
#50497=CARTESIAN_POINT('Ctrl Pts',(-6.8407016218269,-4.92126012648956,0.661943615096396));
#50498=CARTESIAN_POINT('Ctrl Pts',(-6.8088415259036,-4.91816702752264,0.00255975366377111));
#50499=CARTESIAN_POINT('Origin',(-14.75,0.,0.));
#50500=CARTESIAN_POINT('',(-5.0911584740964,-4.92034850444268,-0.00382654489779644));
#50501=CARTESIAN_POINT('',(-5.30884152590359,-4.92118977299025,-0.00410386901592228));
#50502=CARTESIAN_POINT('',(-14.75,-4.925,-6.03138548580071E-16));
#50503=CARTESIAN_POINT('Ctrl Pts',(-5.0911584740964,-4.92034850444268,-0.00382654489779644));
#50504=CARTESIAN_POINT('Ctrl Pts',(-5.14411519360526,-4.91244809502025,
1.09095932864311));
#50505=CARTESIAN_POINT('Ctrl Pts',(-5.19707191311412,-4.55198007497204,
2.19046632634003));
#50506=CARTESIAN_POINT('Ctrl Pts',(-5.25002863262299,-3.88054548599257,
3.0458915476704));
#50507=CARTESIAN_POINT('Ctrl Pts',(-5.32957452099606,-2.87198866147391,
4.3308193112958));
#50508=CARTESIAN_POINT('Ctrl Pts',(-5.40912040936913,-1.16180365248812,
5.06502982514693));
#50509=CARTESIAN_POINT('Ctrl Pts',(-5.4886662977422,0.464412516539281,4.91125336903979));
#50510=CARTESIAN_POINT('Ctrl Pts',(-5.56821218611528,2.09062868556668,4.75747691293265));
#50511=CARTESIAN_POINT('Ctrl Pts',(-5.64775807448836,3.63287601463573,3.71571348686722));
#50512=CARTESIAN_POINT('Ctrl Pts',(-5.72730396286143,4.38270195487139,2.26451147037829));
#50513=CARTESIAN_POINT('Ctrl Pts',(-5.80684985123451,5.13252789510707,0.813309453889311));
#50514=CARTESIAN_POINT('Ctrl Pts',(-5.88639573960759,5.08993244650934,-1.04733115302316));
#50515=CARTESIAN_POINT('Ctrl Pts',(-5.96594162798066,4.27448241666476,-2.46269947196908));
#50516=CARTESIAN_POINT('Ctrl Pts',(-6.04548751635374,3.45903238682021,-3.87806779091495));
#50517=CARTESIAN_POINT('Ctrl Pts',(-6.12503340472681,1.87072777572881,-4.84816382189425));
#50518=CARTESIAN_POINT('Ctrl Pts',(-6.20457929309989,0.239178174554097,
-4.92736059443231));
#50519=CARTESIAN_POINT('Ctrl Pts',(-6.28412518147296,-1.39237142662062,
-5.00655736697037));
#50520=CARTESIAN_POINT('Ctrl Pts',(-6.36367106984604,-3.06716601787869,
-4.19485488106719));
#50521=CARTESIAN_POINT('Ctrl Pts',(-6.44321695821912,-4.01586564339155,
-2.86511985060641));
#50522=CARTESIAN_POINT('Ctrl Pts',(-6.49253079684488,-4.604004404473,-2.04076123134479));
#50523=CARTESIAN_POINT('Ctrl Pts',(-6.54184463547064,-4.91308446209832,
-1.01730814503372));
#50524=CARTESIAN_POINT('Ctrl Pts',(-6.5911584740964,-4.91874206214364,0.00300395193210873));
#50525=CARTESIAN_POINT('Ctrl Pts',(-6.8088415259036,-4.91816702752264,0.00255975366377111));
#50526=CARTESIAN_POINT('Ctrl Pts',(-6.76115573345382,-4.91353750990542,
-0.984356357220146));
#50527=CARTESIAN_POINT('Ctrl Pts',(-6.71346994100404,-4.62593290938502,
-1.97375585426302));
#50528=CARTESIAN_POINT('Ctrl Pts',(-6.66578414855426,-4.07363732517796,
-2.78236670443132));
#50529=CARTESIAN_POINT('Ctrl Pts',(-6.58623826018119,-3.15233895446205,
-4.13123111708606));
#50530=CARTESIAN_POINT('Ctrl Pts',(-6.5066923718081,-1.49450011750048,-4.97702529891446));
#50531=CARTESIAN_POINT('Ctrl Pts',(-6.42714648343503,0.138328089510376,
-4.93122204682461));
#50532=CARTESIAN_POINT('Ctrl Pts',(-6.34760059506195,1.77115629652118,-4.88541879473476));
#50533=CARTESIAN_POINT('Ctrl Pts',(-6.26805470668888,3.37897387358129,-3.94801810872673));
#50534=CARTESIAN_POINT('Ctrl Pts',(-6.18850881831581,4.22320767910246,-2.54962790101466));
#50535=CARTESIAN_POINT('Ctrl Pts',(-6.10896292994273,5.06744148462366,-1.15123769330255));
#50536=CARTESIAN_POINT('Ctrl Pts',(-6.02941704156966,5.14809151860588,0.708142036113649));
#50537=CARTESIAN_POINT('Ctrl Pts',(-5.94987115319658,4.42811007730965,2.17437960764566));
#50538=CARTESIAN_POINT('Ctrl Pts',(-5.8703252648235,3.70812863601341,3.64061717917766));
#50539=CARTESIAN_POINT('Ctrl Pts',(-5.79077937645043,2.18751571943878,4.71371259282546));
#50540=CARTESIAN_POINT('Ctrl Pts',(-5.71123348807735,0.564785808115402,
4.9007246942176));
#50541=CARTESIAN_POINT('Ctrl Pts',(-5.63168759970428,-1.05794410320798,
5.08773679560975));
#50542=CARTESIAN_POINT('Ctrl Pts',(-5.5521417113312,-2.78279100928007,4.38866558474619));
#50543=CARTESIAN_POINT('Ctrl Pts',(-5.47259582295812,-3.81742273544663,
3.1246390494413));
#50544=CARTESIAN_POINT('Ctrl Pts',(-5.41801105727328,-4.5273919305612,2.25725804886157));
#50545=CARTESIAN_POINT('Ctrl Pts',(-5.36342629158844,-4.9123547098068,1.12385261058705));
#50546=CARTESIAN_POINT('Ctrl Pts',(-5.30884152590359,-4.92118977299025,
-0.00410386901592228));
#50547=CARTESIAN_POINT('Origin',(-14.75,0.,0.));
#50548=CARTESIAN_POINT('',(-3.5911584740964,-4.93263795678916,-0.00146375725000258));
#50549=CARTESIAN_POINT('',(-3.80884152590359,-4.93297963225018,-0.000859328946059894));
#50550=CARTESIAN_POINT('',(-14.75,-4.925,-6.03138548580071E-16));
#50551=CARTESIAN_POINT('Ctrl Pts',(-3.5911584740964,-4.93263795678916,-0.00146375725000258));
#50552=CARTESIAN_POINT('Ctrl Pts',(-3.66683986336681,-4.9265598841513,1.55309257837791));
#50553=CARTESIAN_POINT('Ctrl Pts',(-3.74252125263721,-4.13044035554753,
3.11300803879703));
#50554=CARTESIAN_POINT('Ctrl Pts',(-3.81820264190762,-2.8653605731944,4.01569365331712));
#50555=CARTESIAN_POINT('Ctrl Pts',(-3.8977485302807,-1.53568235084381,4.96447286866741));
#50556=CARTESIAN_POINT('Ctrl Pts',(-3.97729441865377,0.31207168483266,5.18718866129924));
#50557=CARTESIAN_POINT('Ctrl Pts',(-4.05684030702685,1.82911060574424,4.58153289102084));
#50558=CARTESIAN_POINT('Ctrl Pts',(-4.13638619539992,3.34614952665579,3.97587712074245));
#50559=CARTESIAN_POINT('Ctrl Pts',(-4.215932083773,4.53247333280247,2.54184978755386));
#50560=CARTESIAN_POINT('Ctrl Pts',(-4.29547797214607,4.84312767798418,0.938191390916231));
#50561=CARTESIAN_POINT('Ctrl Pts',(-4.37502386051915,5.15378202316589,-0.665467005721419));
#50562=CARTESIAN_POINT('Ctrl Pts',(-4.45456974889223,4.58876690738262,-2.43875646580811));
#50563=CARTESIAN_POINT('Ctrl Pts',(-4.53411563726531,3.40762989303727,-3.56709221570014));
#50564=CARTESIAN_POINT('Ctrl Pts',(-4.61366152563838,2.22649287869195,-4.69542796559215));
#50565=CARTESIAN_POINT('Ctrl Pts',(-4.69320741401145,0.429233965784571,
-5.17881000528951));
#50566=CARTESIAN_POINT('Ctrl Pts',(-4.77275330238453,-1.15855126458436,
-4.79519005809945));
#50567=CARTESIAN_POINT('Ctrl Pts',(-4.8522991907576,-2.74633649495327,-4.4115701109094));
#50568=CARTESIAN_POINT('Ctrl Pts',(-4.93184507913068,-4.12464804278375,
-3.16094817683195));
#50569=CARTESIAN_POINT('Ctrl Pts',(-5.01139096750375,-4.66033949667325,
-1.6178147030934));
#50570=CARTESIAN_POINT('Ctrl Pts',(-5.03798013636797,-4.83940080100846,
-1.10200380007321));
#50571=CARTESIAN_POINT('Ctrl Pts',(-5.06456930523218,-4.92431524033904,
-0.553510262690519));
#50572=CARTESIAN_POINT('Ctrl Pts',(-5.0911584740964,-4.92034850444268,-0.00382654489779644));
#50573=CARTESIAN_POINT('Ctrl Pts',(-5.30884152590359,-4.92118977299025,
-0.00410386901592228));
#50574=CARTESIAN_POINT('Ctrl Pts',(-5.28388040321536,-4.92522996796614,
-0.519908227999806));
#50575=CARTESIAN_POINT('Ctrl Pts',(-5.25891928052713,-4.85061618972318,
-1.03457312761624));
#50576=CARTESIAN_POINT('Ctrl Pts',(-5.2339581578389,-4.69245989025258,-1.52213853308082));
#50577=CARTESIAN_POINT('Ctrl Pts',(-5.15441226946583,-4.18844877263093,
-3.07590772055185));
#50578=CARTESIAN_POINT('Ctrl Pts',(-5.07486638109275,-2.83600999112659,
-4.35446423574767));
#50579=CARTESIAN_POINT('Ctrl Pts',(-4.99532049271967,-1.25640492385531,
-4.77048553279394));
#50580=CARTESIAN_POINT('Ctrl Pts',(-4.9157746043466,0.323200143415984,-5.18650682984021));
#50581=CARTESIAN_POINT('Ctrl Pts',(-4.83622871597352,2.1299714964542,-4.73999290873692));
#50582=CARTESIAN_POINT('Ctrl Pts',(-4.75668282760045,3.33394384188576,-3.63605609952002));
#50583=CARTESIAN_POINT('Ctrl Pts',(-4.67713693922737,4.53791618731733,-2.53211929030309));
#50584=CARTESIAN_POINT('Ctrl Pts',(-4.5975910508543,5.13908952514219,-0.770759592972526));
#50585=CARTESIAN_POINT('Ctrl Pts',(-4.51804516248122,4.86130659629173,0.83891818762146));
#50586=CARTESIAN_POINT('Ctrl Pts',(-4.43849927410815,4.58352366744127,2.44859596821542));
#50587=CARTESIAN_POINT('Ctrl Pts',(-4.35895338573507,3.42678447191547,3.90659183207286));
#50588=CARTESIAN_POINT('Ctrl Pts',(-4.27940749736199,1.92245310317772,4.54315525853296));
#50589=CARTESIAN_POINT('Ctrl Pts',(-4.19986160898891,0.418121734439937,
5.17971868499307));
#50590=CARTESIAN_POINT('Ctrl Pts',(-4.12031572061584,-1.43380180750975,
4.99484967405592));
#50591=CARTESIAN_POINT('Ctrl Pts',(-4.04076983224277,-2.78261097786045,
4.07347043921392));
#50592=CARTESIAN_POINT('Ctrl Pts',(-3.96346039679638,-4.09349803459511,
3.17799601640553));
#50593=CARTESIAN_POINT('Ctrl Pts',(-3.88615096134998,-4.92916340173032,
1.58684352759606));
#50594=CARTESIAN_POINT('Ctrl Pts',(-3.80884152590359,-4.93297963225018,
-0.000859328946059894));
#50595=CARTESIAN_POINT('Origin',(-14.75,0.,0.));
#50596=CARTESIAN_POINT('',(-2.09115847409639,-4.92479967433243,0.00455076259524401));
#50597=CARTESIAN_POINT('',(-2.3088415259036,-4.92378694620037,0.00452865572044409));
#50598=CARTESIAN_POINT('',(-14.75,-4.925,-6.03138548580071E-16));
#50599=CARTESIAN_POINT('Ctrl Pts',(-2.09115847409639,-4.92479967433243,
0.00455076259524401));
#50600=CARTESIAN_POINT('Ctrl Pts',(-2.11001864475527,-4.92838960899571,
0.393565332838783));
#50601=CARTESIAN_POINT('Ctrl Pts',(-2.12887881541415,-4.8861997157664,0.781810208141141));
#50602=CARTESIAN_POINT('Ctrl Pts',(-2.14773898607303,-4.79526872833564,
1.15827977445631));
#50603=CARTESIAN_POINT('Ctrl Pts',(-2.22728487444611,-4.41175225297358,
2.74610242143037));
#50604=CARTESIAN_POINT('Ctrl Pts',(-2.30683076281919,-3.16119502426286,
4.12445761712042));
#50605=CARTESIAN_POINT('Ctrl Pts',(-2.38637665119226,-1.61808937757221,
4.66023409988841));
#50606=CARTESIAN_POINT('Ctrl Pts',(-2.46592253956534,-0.0749837308815521,
5.19601058265641));
#50607=CARTESIAN_POINT('Ctrl Pts',(-2.54546842793841,1.76067033378902,4.88920835250233));
#50608=CARTESIAN_POINT('Ctrl Pts',(-2.62501431631149,3.04565633625721,3.88073249588954));
#50609=CARTESIAN_POINT('Ctrl Pts',(-2.70456020468456,4.33064233872542,2.87225663927674));
#50610=CARTESIAN_POINT('Ctrl Pts',(-2.78410609305764,5.06496027899121,1.16210715620522));
#50611=CARTESIAN_POINT('Ctrl Pts',(-2.86365198143071,4.91128251100273,-0.464120269161797));
#50612=CARTESIAN_POINT('Ctrl Pts',(-2.94319786980379,4.75760474301426,-2.09034769452876));
#50613=CARTESIAN_POINT('Ctrl Pts',(-3.02274375817687,3.71593126677153,-3.63265306219127));
#50614=CARTESIAN_POINT('Ctrl Pts',(-3.10228964654994,2.26477361062453,-4.38256496537029));
#50615=CARTESIAN_POINT('Ctrl Pts',(-3.18183553492302,0.813615954477467,
-5.13247686854935));
#50616=CARTESIAN_POINT('Ctrl Pts',(-3.26138142329609,-1.04702588157384,
-5.08999530724491));
#50617=CARTESIAN_POINT('Ctrl Pts',(-3.34092731166917,-2.46244278226107,
-4.27463070863102));
#50618=CARTESIAN_POINT('Ctrl Pts',(-3.42047320004224,-3.87785968294825,
-3.45926611001717));
#50619=CARTESIAN_POINT('Ctrl Pts',(-3.50001908841532,-4.84805164827134,
-1.87101847409385));
#50620=CARTESIAN_POINT('Ctrl Pts',(-3.57956497678839,-4.92734642642051,
-0.239473337097873));
#50621=CARTESIAN_POINT('Ctrl Pts',(-3.58342947589106,-4.93119872608391,
-0.160209595792822));
#50622=CARTESIAN_POINT('Ctrl Pts',(-3.58729397499373,-4.93294831983193,
-0.0808436632215555));
#50623=CARTESIAN_POINT('Ctrl Pts',(-3.5911584740964,-4.93263795678916,-0.00146375725000258));
#50624=CARTESIAN_POINT('Ctrl Pts',(-3.80884152590359,-4.93297963225018,
-0.000859328946059894));
#50625=CARTESIAN_POINT('Ctrl Pts',(-3.80660507297691,-4.93309003041654,
-0.0467893332167884));
#50626=CARTESIAN_POINT('Ctrl Pts',(-3.80436862005022,-4.93250428457465,
-0.0927164506168972));
#50627=CARTESIAN_POINT('Ctrl Pts',(-3.80213216712354,-4.93121376103269,
-0.138623755771863));
#50628=CARTESIAN_POINT('Ctrl Pts',(-3.72258627875046,-4.8853125751026,-1.77144925716878));
#50629=CARTESIAN_POINT('Ctrl Pts',(-3.64304039037739,-3.94781540449082,
-3.37921080121581));
#50630=CARTESIAN_POINT('Ctrl Pts',(-3.56349450200431,-2.54937460381079,
-4.2233606619699));
#50631=CARTESIAN_POINT('Ctrl Pts',(-3.48394861363124,-1.15093380313076,
-5.06751052272398));
#50632=CARTESIAN_POINT('Ctrl Pts',(-3.40440272525816,0.708450627617543,
-5.14804870018514));
#50633=CARTESIAN_POINT('Ctrl Pts',(-3.32485683688509,2.17464508120495,-4.42797949508699));
#50634=CARTESIAN_POINT('Ctrl Pts',(-3.24531094851201,3.64083953479237,-3.70791028998884));
#50635=CARTESIAN_POINT('Ctrl Pts',(-3.16576506013894,4.71384401121892,-2.18723370233138));
#50636=CARTESIAN_POINT('Ctrl Pts',(-3.08621917176586,4.90075868413978,-0.564492267726287));
#50637=CARTESIAN_POINT('Ctrl Pts',(-3.00667328339279,5.08767335706064,1.05824916687883));
#50638=CARTESIAN_POINT('Ctrl Pts',(-2.92712739501971,4.38849822647583,2.78305544843154));
#50639=CARTESIAN_POINT('Ctrl Pts',(-2.84758150664664,3.12440987169467,3.8176107737941));
#50640=CARTESIAN_POINT('Ctrl Pts',(-2.76803561827356,1.86032151691353,4.85216609915665));
#50641=CARTESIAN_POINT('Ctrl Pts',(-2.68848972990048,0.0313199379360557,
5.19647046832902));
#50642=CARTESIAN_POINT('Ctrl Pts',(-2.60894384152741,-1.5224194503301,4.69236732243377));
#50643=CARTESIAN_POINT('Ctrl Pts',(-2.52939795315433,-3.07615883859628,
4.18826417653852));
#50644=CARTESIAN_POINT('Ctrl Pts',(-2.44985206478126,-4.35463603615115,
2.8357535155756));
#50645=CARTESIAN_POINT('Ctrl Pts',(-2.37030617640818,-4.77056178492771,
1.25612130118806));
#50646=CARTESIAN_POINT('Ctrl Pts',(-2.34981795957332,-4.87768959633853,
0.849263725144446));
#50647=CARTESIAN_POINT('Ctrl Pts',(-2.32932974273846,-4.92759608937386,
0.427338996020449));
#50648=CARTESIAN_POINT('Ctrl Pts',(-2.3088415259036,-4.92378694620037,0.00452865572044409));
#50649=CARTESIAN_POINT('Origin',(-14.75,0.,0.));
#50650=CARTESIAN_POINT('',(-0.591158474096391,-4.91621514884034,-0.00190685489401573));
#50651=CARTESIAN_POINT('',(-0.808841525903593,-4.91703434725887,-0.0013692803956027));
#50652=CARTESIAN_POINT('',(-14.75,-4.925,-6.03138548580071E-16));
#50653=CARTESIAN_POINT('Ctrl Pts',(-0.591158474096391,-4.91617236260859,
-0.00191614214703012));
#50654=CARTESIAN_POINT('Ctrl Pts',(-0.632743314516819,-4.91557730725517,
0.859927749670198));
#50655=CARTESIAN_POINT('Ctrl Pts',(-0.674328154937247,-4.70120063118156,
1.72260089528099));
#50656=CARTESIAN_POINT('Ctrl Pts',(-0.715912995357675,-4.27522171387068,
2.46297048332456));
#50657=CARTESIAN_POINT('Ctrl Pts',(-0.795458883730751,-3.46038459863554,
3.87919226053746));
#50658=CARTESIAN_POINT('Ctrl Pts',(-0.875004772103829,-1.87128956129306,
4.84790224489492));
#50659=CARTESIAN_POINT('Ctrl Pts',(-0.954550660476906,-0.23953077630217,
4.92691531448512));
#50660=CARTESIAN_POINT('Ctrl Pts',(-1.03409654884998,1.39222800868875,5.00592838407533));
#50661=CARTESIAN_POINT('Ctrl Pts',(-1.11364243722306,3.06665054132806,4.19524453889832));
#50662=CARTESIAN_POINT('Ctrl Pts',(-1.19318832559614,4.01539704249259,2.86581937781023));
#50663=CARTESIAN_POINT('Ctrl Pts',(-1.27273421396921,4.96414354365708,1.53639421672219));
#50664=CARTESIAN_POINT('Ctrl Pts',(-1.35228010234228,5.1872140133468,-0.311772260276884));
#50665=CARTESIAN_POINT('Ctrl Pts',(-1.43182599071535,4.58170765220235,-1.82894951483846));
#50666=CARTESIAN_POINT('Ctrl Pts',(-1.51137187908843,3.9762012910579,-3.34612676940009));
#50667=CARTESIAN_POINT('Ctrl Pts',(-1.59091776746151,2.54211809907922,-4.53231480152423));
#50668=CARTESIAN_POINT('Ctrl Pts',(-1.67046365583459,0.938447910619046,
-4.84301219015054));
#50669=CARTESIAN_POINT('Ctrl Pts',(-1.75000954420766,-0.665222277841155,
-5.15370957877686));
#50670=CARTESIAN_POINT('Ctrl Pts',(-1.82955543258074,-2.43847946278283,
-4.58891632390535));
#50671=CARTESIAN_POINT('Ctrl Pts',(-1.90910132095381,-3.56687019424698,
-3.40787464734053));
#50672=CARTESIAN_POINT('Ctrl Pts',(-1.96978703866801,-4.42772174548972,
-2.50685558452536));
#50673=CARTESIAN_POINT('Ctrl Pts',(-2.0304727563822,-4.91324846594047,-1.24716794257944));
#50674=CARTESIAN_POINT('Ctrl Pts',(-2.09115847409639,-4.92479967433243,
0.00455076259524401));
#50675=CARTESIAN_POINT('Ctrl Pts',(-2.3088415259036,-4.92378694620037,0.00452865572044409));
#50676=CARTESIAN_POINT('Ctrl Pts',(-2.24978385436538,-4.912807019143,-1.21423012654258));
#50677=CARTESIAN_POINT('Ctrl Pts',(-2.19072618282717,-4.45550843625236,
-2.44034737679679));
#50678=CARTESIAN_POINT('Ctrl Pts',(-2.13166851128896,-3.63585440375436,
-3.33416659713051));
#50679=CARTESIAN_POINT('Ctrl Pts',(-2.05212262291588,-2.53184697380615,
-4.53806851324942));
#50680=CARTESIAN_POINT('Ctrl Pts',(-1.9725767345428,-0.770457813911437,
-5.13911857767506));
#50681=CARTESIAN_POINT('Ctrl Pts',(-1.89303084616973,0.839206332661352,
-4.86124723150085));
#50682=CARTESIAN_POINT('Ctrl Pts',(-1.81348495779665,2.4488704792341,-4.58337588532665));
#50683=CARTESIAN_POINT('Ctrl Pts',(-1.73393906942358,3.90680961248493,-3.42658312855265));
#50684=CARTESIAN_POINT('Ctrl Pts',(-1.65439318105051,4.54327701636474,-1.9221980209477));
#50685=CARTESIAN_POINT('Ctrl Pts',(-1.57484729267743,5.17974442024456,-0.417812913342702));
#50686=CARTESIAN_POINT('Ctrl Pts',(-1.49530140430435,4.99474009475331,1.43416454509326));
#50687=CARTESIAN_POINT('Ctrl Pts',(-1.41575551593128,4.0732911268349,2.78288857953561));
#50688=CARTESIAN_POINT('Ctrl Pts',(-1.3362096275582,3.15184215891648,4.13161261397798));
#50689=CARTESIAN_POINT('Ctrl Pts',(-1.25666373918512,1.49394854857088,4.97708322442672));
#50690=CARTESIAN_POINT('Ctrl Pts',(-1.17711785081204,-0.138895601305483,
4.93114147431309));
#50691=CARTESIAN_POINT('Ctrl Pts',(-1.09757196243897,-1.77173975118177,
4.88519972419945));
#50692=CARTESIAN_POINT('Ctrl Pts',(-1.0180260740659,-3.37953444058883,3.94784561352353));
#50693=CARTESIAN_POINT('Ctrl Pts',(-0.938480185692825,-4.22355933348682,
2.54924407639987));
#50694=CARTESIAN_POINT('Ctrl Pts',(-0.895267299096415,-4.6820714291754,
1.7894611277975));
#50695=CARTESIAN_POINT('Ctrl Pts',(-0.852054412500004,-4.91518370582573,
0.893557208022445));
#50696=CARTESIAN_POINT('Ctrl Pts',(-0.808841525903593,-4.91703434725887,
-0.0013692803956027));
#50697=CARTESIAN_POINT('Origin',(-32.3478126690739,0.,0.));
#50698=CARTESIAN_POINT('',(-0.0978126690738565,-4.06323934281354,-0.00157601073016207));
#50699=CARTESIAN_POINT('',(0.,-4.0705,-4.82875428449296E-13));
#50700=CARTESIAN_POINT('',(-32.3478126690739,-4.0705,-4.82875428449296E-13));
#50701=CARTESIAN_POINT('',(0.,-3.73359974356529,-1.6214817929441));
#50702=CARTESIAN_POINT('Ctrl Pts',(-0.0978126690738567,-4.06320398010117,
-0.00158368662129781));
#50703=CARTESIAN_POINT('Ctrl Pts',(-0.0652084460492417,-4.06358958070638,
-0.560065388179513));
#50704=CARTESIAN_POINT('Ctrl Pts',(-0.0326042230246268,-3.95536025262438,
-1.1181257750272));
#50705=CARTESIAN_POINT('Ctrl Pts',(-1.16714363868065E-14,-3.73764785372991,
-1.62671566533116));
#50706=CARTESIAN_POINT('Origin',(0.,0.,0.));
#50707=CARTESIAN_POINT('Origin',(-32.3478126690739,0.,0.));
#50708=CARTESIAN_POINT('',(-1.59781266907385,-4.07033443134419,0.00376119373461055));
#50709=CARTESIAN_POINT('',(-1.30218733092609,-4.06391640822685,-0.00113170677241647));
#50710=CARTESIAN_POINT('',(-32.3478126690739,-4.0705,-4.82875428449296E-13));
#50711=CARTESIAN_POINT('Ctrl Pts',(-1.59781266907385,-4.07033443134419,
0.00376119373461031));
#50712=CARTESIAN_POINT('Ctrl Pts',(-1.53712695135966,-4.06078738692598,
-1.0307811391412));
#50713=CARTESIAN_POINT('Ctrl Pts',(-1.3968953452724,-3.13350059127503,-3.43660489264461));
#50714=CARTESIAN_POINT('Ctrl Pts',(-1.17711785081205,0.915788038447374,
-4.72632807804377));
#50715=CARTESIAN_POINT('Ctrl Pts',(-0.938480185692821,4.47158639354322,
-1.78518388428051));
#50716=CARTESIAN_POINT('Ctrl Pts',(-0.699842520573601,3.91848486245357,
2.79733082310517));
#50717=CARTESIAN_POINT('Ctrl Pts',(-0.461204855454373,-0.233233057815519,
4.80741524450186));
#50718=CARTESIAN_POINT('Ctrl Pts',(-0.260528238287788,-3.54660683376317,
2.78758749144531));
#50719=CARTESIAN_POINT('Ctrl Pts',(-0.139397509494285,-4.06271216836188,
0.7107281025446));
#50720=CARTESIAN_POINT('Ctrl Pts',(-0.0978126690738567,-4.06320398010117,
-0.00158368662129781));
#50721=CARTESIAN_POINT('',(0.,-2.75129702511903,2.99988915288068));
#50722=CARTESIAN_POINT('Origin',(0.,0.,0.));
#50723=CARTESIAN_POINT('Ctrl Pts',(-1.30218733092609,-4.06391640822685,
-0.00113170677241654));
#50724=CARTESIAN_POINT('Ctrl Pts',(-1.26585432914943,-4.06520244032274,
-0.623026454755739));
#50725=CARTESIAN_POINT('Ctrl Pts',(-1.1499754389997,-3.63835675138479,-2.6046490156767));
#50726=CARTESIAN_POINT('Ctrl Pts',(-0.9545506604769,-0.551158953576692,
-4.78140835552346));
#50727=CARTESIAN_POINT('Ctrl Pts',(-0.715912995357679,3.72696190987269,
-3.05177387808086));
#50728=CARTESIAN_POINT('Ctrl Pts',(-0.477275330238447,4.57725222884596,
1.49154630755727));
#50729=CARTESIAN_POINT('Ctrl Pts',(-0.278410609305757,1.78830202401348,
4.11849926473408));
#50730=CARTESIAN_POINT('Ctrl Pts',(-0.119318832559607,-1.02190788268887,
4.1117895186236));
#50731=CARTESIAN_POINT('Ctrl Pts',(-0.0397729441865359,-2.25151393523441,
3.45825666525491));
#50732=CARTESIAN_POINT('Ctrl Pts',(0.,-2.75129702511903,2.99988915288068));
#50733=CARTESIAN_POINT('Origin',(-32.3478126690739,0.,0.));
#50734=CARTESIAN_POINT('',(-3.09781266907385,-4.07681275190056,-0.00120979165237837));
#50735=CARTESIAN_POINT('',(-2.8021873309261,-4.06949741411341,0.00374292245829216));
#50736=CARTESIAN_POINT('',(-32.3478126690739,-4.0705,-4.82875428449296E-13));
#50737=CARTESIAN_POINT('Ctrl Pts',(-3.09781266907385,-4.07681275190056,
-0.00120979165237874));
#50738=CARTESIAN_POINT('Ctrl Pts',(-3.09394816997118,-4.07706926616768,
-0.0668170824659285));
#50739=CARTESIAN_POINT('Ctrl Pts',(-3.01053778249544,-4.04585841086343,
-1.48261925960601));
#50740=CARTESIAN_POINT('Ctrl Pts',(-2.84758150664664,-2.40317998874982,
-4.17175730007125));
#50741=CARTESIAN_POINT('Ctrl Pts',(-2.60894384152741,2.21026727641583,-4.27709000786183));
#50742=CARTESIAN_POINT('Ctrl Pts',(-2.37030617640818,4.79308872923565,-0.452955592184536));
#50743=CARTESIAN_POINT('Ctrl Pts',(-2.13166851128895,2.97235298759993,3.78734702964848));
#50744=CARTESIAN_POINT('Ctrl Pts',(-1.89303084616973,-1.57913728868941,
4.54806082325786));
#50745=CARTESIAN_POINT('Ctrl Pts',(-1.71507889876469,-3.89136234884321,
1.99954296889815));
#50746=CARTESIAN_POINT('Ctrl Pts',(-1.61667283973273,-4.0733015032319,0.325280748694308));
#50747=CARTESIAN_POINT('Ctrl Pts',(-1.59781266907385,-4.07033443134419,
0.00376119373461031));
#50748=CARTESIAN_POINT('Ctrl Pts',(-2.8021873309261,-4.06949741411341,0.00374292245829196));
#50749=CARTESIAN_POINT('Ctrl Pts',(-2.7431296593879,-4.06042253226819,-1.00355811778553));
#50750=CARTESIAN_POINT('Ctrl Pts',(-2.60452609947661,-3.17339021123584,
-3.38188525686312));
#50751=CARTESIAN_POINT('Ctrl Pts',(-2.38637665119226,0.819002242401078,
-4.74423481374027));
#50752=CARTESIAN_POINT('Ctrl Pts',(-2.14773898607304,4.43395122223712,-1.87597598138563));
#50753=CARTESIAN_POINT('Ctrl Pts',(-1.90910132095381,3.97523440584382,2.71598802545506));
#50754=CARTESIAN_POINT('Ctrl Pts',(-1.67046365583458,-0.135500177452599,
4.81232596646912));
#50755=CARTESIAN_POINT('Ctrl Pts',(-1.46815899249201,-3.51506103565612,
2.84202137248833));
#50756=CARTESIAN_POINT('Ctrl Pts',(-1.34540021752251,-4.06238685777956,
0.738522764518305));
#50757=CARTESIAN_POINT('Ctrl Pts',(-1.30218733092609,-4.06391640822685,
-0.00113170677241654));
#50758=CARTESIAN_POINT('Origin',(-32.3478126690739,0.,0.));
#50759=CARTESIAN_POINT('',(-4.59781266907386,-4.0666555507277,-0.00316262964624325));
#50760=CARTESIAN_POINT('',(-4.30218733092609,-4.0770951458019,-0.000710233193596532));
#50761=CARTESIAN_POINT('',(-32.3478126690739,-4.0705,-4.82875428449296E-13));
#50762=CARTESIAN_POINT('Ctrl Pts',(-4.59781266907386,-4.0666555507277,-0.00316262964624277));
#50763=CARTESIAN_POINT('Ctrl Pts',(-4.57122350020965,-4.06993404787816,
-0.457474827265511));
#50764=CARTESIAN_POINT('Ctrl Pts',(-4.46508844297236,-3.78979273029454,
-2.26701044287803));
#50765=CARTESIAN_POINT('Ctrl Pts',(-4.27940749736198,-1.13066914665236,
-4.67978735413588));
#50766=CARTESIAN_POINT('Ctrl Pts',(-4.04076983224278,3.32562064318893,-3.48124526728007));
#50767=CARTESIAN_POINT('Ctrl Pts',(-3.80213216712354,4.72657132062792,0.915612446800854));
#50768=CARTESIAN_POINT('Ctrl Pts',(-3.56349450200431,1.78509047620951,4.4712723004521));
#50769=CARTESIAN_POINT('Ctrl Pts',(-3.32872133598775,-2.72220888913037,
3.92799287505321));
#50770=CARTESIAN_POINT('Ctrl Pts',(-3.17349405834426,-4.07178924029207,
1.28362707416973));
#50771=CARTESIAN_POINT('Ctrl Pts',(-3.09781266907385,-4.07681275190056,
-0.00120979165237874));
#50772=CARTESIAN_POINT('Ctrl Pts',(-4.30218733092609,-4.0770951458019,-0.000710233193597031));
#50773=CARTESIAN_POINT('Ctrl Pts',(-4.29995087799942,-4.07718638960619,
-0.038671265149509));
#50774=CARTESIAN_POINT('Ctrl Pts',(-4.21816853669967,-4.05948324093355,
-1.42673845965056));
#50775=CARTESIAN_POINT('Ctrl Pts',(-4.05684030702684,-2.48802037989938,
-4.12171998606955));
#50776=CARTESIAN_POINT('Ctrl Pts',(-3.81820264190762,2.12230915839156,-4.32141378384957));
#50777=CARTESIAN_POINT('Ctrl Pts',(-3.5795649767884,4.78281558760628,-0.550907763508576));
#50778=CARTESIAN_POINT('Ctrl Pts',(-3.34092731166917,3.04921617498962,3.72573627855867));
#50779=CARTESIAN_POINT('Ctrl Pts',(-3.10228964654994,-1.48577931367711,
4.57943634031457));
#50780=CARTESIAN_POINT('Ctrl Pts',(-2.92270965296892,-3.87125352580713,
2.05582519611215));
#50781=CARTESIAN_POINT('Ctrl Pts',(-2.82267554776097,-4.07264566127848,
0.35319459559373));
#50782=CARTESIAN_POINT('Ctrl Pts',(-2.8021873309261,-4.06949741411341,0.00374292245829196));
#50783=CARTESIAN_POINT('Origin',(-32.3478126690739,0.,0.));
#50784=CARTESIAN_POINT('',(-6.09781266907385,-4.06532783024481,0.00248275864732798));
#50785=CARTESIAN_POINT('',(-5.80218733092609,-4.06735085704707,-0.00339183732646908));
#50786=CARTESIAN_POINT('',(-32.3478126690739,-4.0705,-4.82875428449296E-13));
#50787=CARTESIAN_POINT('Ctrl Pts',(-6.09781266907385,-4.06532783024481,
0.00248275864732861));
#50788=CARTESIAN_POINT('Ctrl Pts',(-6.0484988304481,-4.06065183816668,-0.840802599870245));
#50789=CARTESIAN_POINT('Ctrl Pts',(-5.91963910344927,-3.39313702767653,
-3.05113638265515));
#50790=CARTESIAN_POINT('Ctrl Pts',(-5.71123348807733,0.233422028762872,
-4.80877700124299));
#50791=CARTESIAN_POINT('Ctrl Pts',(-5.47259582295814,4.171611218274,-2.40343127894775));
#50792=CARTESIAN_POINT('Ctrl Pts',(-5.23395815783889,4.27722630874114,2.21001293857749));
#50793=CARTESIAN_POINT('Ctrl Pts',(-4.99532049271968,0.453235799314355,
4.7930574212978));
#50794=CARTESIAN_POINT('Ctrl Pts',(-4.78327199646466,-3.31468772914499,
3.17542596303663));
#50795=CARTESIAN_POINT('Ctrl Pts',(-4.65076938858272,-4.06012588239192,
0.901675116191023));
#50796=CARTESIAN_POINT('Ctrl Pts',(-4.59781266907386,-4.0666555507277,-0.00316262964624277));
#50797=CARTESIAN_POINT('Ctrl Pts',(-5.80218733092609,-4.06735085704707,
-0.00339183732646849));
#50798=CARTESIAN_POINT('Ctrl Pts',(-5.77722620823787,-4.07069006794027,
-0.429702830878314));
#50799=CARTESIAN_POINT('Ctrl Pts',(-5.67271919717658,-3.81249861092392,
-2.21063503182293));
#50800=CARTESIAN_POINT('Ctrl Pts',(-5.48866629774222,-1.22616783934351,
-4.65567735364785));
#50801=CARTESIAN_POINT('Ctrl Pts',(-5.25002863262297,3.25370797337249,-3.54854948612432));
#50802=CARTESIAN_POINT('Ctrl Pts',(-5.01139096750376,4.74431268704714,0.818728472038551));
#50803=CARTESIAN_POINT('Ctrl Pts',(-4.77275330238453,1.87618665939981,4.43381811498155));
#50804=CARTESIAN_POINT('Ctrl Pts',(-4.53635209019197,-2.67261016863284,
3.97973264573628));
#50805=CARTESIAN_POINT('Ctrl Pts',(-4.3794967663725,-4.07394104096335,1.31152214803601));
#50806=CARTESIAN_POINT('Ctrl Pts',(-4.30218733092609,-4.0770951458019,-0.000710233193597031));
#50807=CARTESIAN_POINT('Origin',(-32.3478126690739,0.,0.));
#50808=CARTESIAN_POINT('',(-7.59781266907386,-4.07574630203772,0.00222153505732406));
#50809=CARTESIAN_POINT('',(-7.3021873309261,-4.06485256559003,0.00211562990566405));
#50810=CARTESIAN_POINT('',(-32.3478126690739,-4.0705,-4.82875428449296E-13));
#50811=CARTESIAN_POINT('Ctrl Pts',(-7.59781266907386,-4.07574630203772,
0.00222153505732401));
#50812=CARTESIAN_POINT('Ctrl Pts',(-7.52577416068655,-4.06771182434402,
-1.22161827070251));
#50813=CARTESIAN_POINT('Ctrl Pts',(-7.37418976392616,-2.82963048299844,
-3.81092663700425));
#50814=CARTESIAN_POINT('Ctrl Pts',(-7.14305947879272,1.57860706315775,-4.5482767971816));
#50815=CARTESIAN_POINT('Ctrl Pts',(-6.90442181367349,4.6797195025539,-1.13094980465497));
#50816=CARTESIAN_POINT('Ctrl Pts',(-6.66578414855425,3.48144476711953,3.32541191686152));
#50817=CARTESIAN_POINT('Ctrl Pts',(-6.42714648343504,-0.91532914635784,
4.72662613694493));
#50818=CARTESIAN_POINT('Ctrl Pts',(-6.23782265694156,-3.7363609545651,2.39316384250277));
#50819=CARTESIAN_POINT('Ctrl Pts',(-6.12804471882117,-4.06819446624524,
0.519462284483144));
#50820=CARTESIAN_POINT('Ctrl Pts',(-6.09781266907385,-4.06532783024481,
0.00248275864732861));
#50821=CARTESIAN_POINT('Ctrl Pts',(-7.3021873309261,-4.06485256559003,0.0021156299056644));
#50822=CARTESIAN_POINT('Ctrl Pts',(-7.25450153847633,-4.06102628102932,
-0.813568030876496));
#50823=CARTESIAN_POINT('Ctrl Pts',(-7.12726985765349,-3.42680090686785,
-2.99539080099765));
#50824=CARTESIAN_POINT('Ctrl Pts',(-6.92049228845756,0.134999037069343,
-4.81254552210429));
#50825=CARTESIAN_POINT('Ctrl Pts',(-6.68185462333835,4.1215704771241,-2.48826765871595));
#50826=CARTESIAN_POINT('Ctrl Pts',(-6.44321695821911,4.32154162229638,2.12205022265777));
#50827=CARTESIAN_POINT('Ctrl Pts',(-6.20457929309988,0.551193473920355,
4.78278213002022));
#50828=CARTESIAN_POINT('Ctrl Pts',(-5.99090275066888,-3.27821055126197,
3.23074519309206));
#50829=CARTESIAN_POINT('Ctrl Pts',(-5.85677209661095,-4.06004869975013,
0.928861330231892));
#50830=CARTESIAN_POINT('Ctrl Pts',(-5.80218733092609,-4.06735085704707,
-0.00339183732646849));
#50831=CARTESIAN_POINT('Origin',(-32.3478126690739,0.,0.));
#50832=CARTESIAN_POINT('',(-9.09781266907386,-4.07222943229488,-0.00357906261956567));
#50833=CARTESIAN_POINT('',(-8.8021873309261,-4.07511392925337,0.00260772300212458));
#50834=CARTESIAN_POINT('',(-32.3478126690739,-4.0705,-4.82875428449296E-13));
#50835=CARTESIAN_POINT('Ctrl Pts',(-9.09781266907386,-4.07222943229488,
-0.003579062619565));
#50836=CARTESIAN_POINT('Ctrl Pts',(-9.08259537929808,-4.07461348194488,
-0.262682434050171));
#50837=CARTESIAN_POINT('Ctrl Pts',(-8.98783220114923,-3.93387284883695,
-1.87362564859038));
#50838=CARTESIAN_POINT('Ctrl Pts',(-8.8135231346273,-1.78562688897607,-4.47105789459565));
#50839=CARTESIAN_POINT('Ctrl Pts',(-8.57488546950807,2.79593183551325,-3.91938608134342));
#50840=CARTESIAN_POINT('Ctrl Pts',(-8.33624780438884,4.80879098967182,0.233133655034067));
#50841=CARTESIAN_POINT('Ctrl Pts',(-8.09761013926962,2.40368143941586,4.17146708260569));
#50842=CARTESIAN_POINT('Ctrl Pts',(-7.85897247415039,-2.20975644067261,
4.27735882951057));
#50843=CARTESIAN_POINT('Ctrl Pts',(-7.69237331741847,-4.01320701615423,
1.60783980898199));
#50844=CARTESIAN_POINT('Ctrl Pts',(-7.60532004905963,-4.07658360250915,
0.129762077875785));
#50845=CARTESIAN_POINT('Ctrl Pts',(-7.59781266907386,-4.07574630203772,
0.00222153505732401));
#50846=CARTESIAN_POINT('Ctrl Pts',(-8.8021873309261,-4.07511392925337,0.00260772300212448));
#50847=CARTESIAN_POINT('Ctrl Pts',(-8.73177686871478,-4.06620451024253,
-1.1940613554039));
#50848=CARTESIAN_POINT('Ctrl Pts',(-8.58182051813039,-2.87606084879853,
-3.7580704643467));
#50849=CARTESIAN_POINT('Ctrl Pts',(-8.35231827917293,1.48523158453539,-4.57961857379977));
#50850=CARTESIAN_POINT('Ctrl Pts',(-8.1136806140537,4.65560380841346,-1.22644703115444));
#50851=CARTESIAN_POINT('Ctrl Pts',(-7.87504294893448,3.54874460969979,3.25349517231261));
#50852=CARTESIAN_POINT('Ctrl Pts',(-7.63640528381524,-0.818443985601727,
4.74436176780107));
#50853=CARTESIAN_POINT('Ctrl Pts',(-7.44545341114579,-3.71128559220026,
2.44953276936589));
#50854=CARTESIAN_POINT('Ctrl Pts',(-7.33404742684941,-4.06740900403576,
0.547094717816802));
#50855=CARTESIAN_POINT('Ctrl Pts',(-7.3021873309261,-4.06485256559003,0.0021156299056644));
#50856=CARTESIAN_POINT('Origin',(-32.3478126690739,0.,0.));
#50857=CARTESIAN_POINT('',(-10.5978126690739,-4.06383028861155,-0.000517316456022591));
#50858=CARTESIAN_POINT('',(-10.3021873309261,-4.07305647823417,-0.00339818811806003));
#50859=CARTESIAN_POINT('',(-32.3478126690739,-4.0705,-4.82875428449296E-13));
#50860=CARTESIAN_POINT('Ctrl Pts',(-10.5978126690739,-4.06383028861155,
-0.000517316456022585));
#50861=CARTESIAN_POINT('Ctrl Pts',(-10.5598707095365,-4.06456413075875,
-0.649936894253117));
#50862=CARTESIAN_POINT('Ctrl Pts',(-10.4423828616261,-3.6108734382595,-2.65990611006904));
#50863=CARTESIAN_POINT('Ctrl Pts',(-10.2453491253427,-0.453810659605433,
-4.79300302197796));
#50864=CARTESIAN_POINT('Ctrl Pts',(-10.0067114602234,3.78679836713871,-2.97304224828663));
#50865=CARTESIAN_POINT('Ctrl Pts',(-9.76807379510421,4.54837145493611,1.57833430913225));
#50866=CARTESIAN_POINT('Ctrl Pts',(-9.52943612998497,1.131230436189,4.67965167333008));
#50867=CARTESIAN_POINT('Ctrl Pts',(-9.30601575464153,-3.04102820872573,
3.55803793366217));
#50868=CARTESIAN_POINT('Ctrl Pts',(-9.16214126767116,-4.06215125311643,
1.09173797619339));
#50869=CARTESIAN_POINT('Ctrl Pts',(-9.09781266907386,-4.07222943229488,
-0.003579062619565));
#50870=CARTESIAN_POINT('Ctrl Pts',(-10.3021873309261,-4.07305647823417,
-0.00339818811806027));
#50871=CARTESIAN_POINT('Ctrl Pts',(-10.2885980873263,-4.07512744307457,
-0.234659625407061));
#50872=CARTESIAN_POINT('Ctrl Pts',(-10.1954629553534,-3.95181437733735,
-1.8174227959994));
#50873=CARTESIAN_POINT('Ctrl Pts',(-10.0227819350075,-1.8767184363934,-4.43359301827195));
#50874=CARTESIAN_POINT('Ctrl Pts',(-9.78414426988828,2.71516687463254,-3.97576256635973));
#50875=CARTESIAN_POINT('Ctrl Pts',(-9.54550660476906,4.8125536089566,0.134710437930172));
#50876=CARTESIAN_POINT('Ctrl Pts',(-9.30686893964983,2.48851481691486,4.12142125330121));
#50877=CARTESIAN_POINT('Ctrl Pts',(-9.06823127453061,-2.12179106496689,
4.32166886952238));
#50878=CARTESIAN_POINT('Ctrl Pts',(-8.9000040716227,-3.99762873478501,1.66388105000583));
#50879=CARTESIAN_POINT('Ctrl Pts',(-8.81132275708786,-4.07626988444755,
0.157869905105551));
#50880=CARTESIAN_POINT('Ctrl Pts',(-8.8021873309261,-4.07511392925337,0.00260772300212448));
#50881=CARTESIAN_POINT('Origin',(-32.3478126690739,0.,0.));
#50882=CARTESIAN_POINT('',(-12.0978126690739,-4.07032458744755,0.00376143334710477));
#50883=CARTESIAN_POINT('',(-11.8021873309261,-4.06398132384238,-0.00096959209926889));
#50884=CARTESIAN_POINT('',(-32.3478126690739,-4.0705,-4.82875428449296E-13));
#50885=CARTESIAN_POINT('Ctrl Pts',(-12.0978126690739,-4.07032458744755,
0.00376143334710491));
#50886=CARTESIAN_POINT('Ctrl Pts',(-12.037146039775,-4.06079261000553,-1.03044389103757));
#50887=CARTESIAN_POINT('Ctrl Pts',(-11.8969335221031,-3.13401642257978,
-3.43588983608773));
#50888=CARTESIAN_POINT('Ctrl Pts',(-11.677175116058,0.914762246840484,-4.7267358838015));
#50889=CARTESIAN_POINT('Ctrl Pts',(-11.4385374509388,4.47095080603802,-1.78589500627826));
#50890=CARTESIAN_POINT('Ctrl Pts',(-11.1998997858196,3.91955374080681,2.79569679264203));
#50891=CARTESIAN_POINT('Ctrl Pts',(-10.9612621207003,-0.232845280914501,
4.80880496159049));
#50892=CARTESIAN_POINT('Ctrl Pts',(-10.7605664151184,-3.54512857250201,
2.78629205291713));
#50893=CARTESIAN_POINT('Ctrl Pts',(-10.6394165979096,-4.06302561966876,
0.711581010269389));
#50894=CARTESIAN_POINT('Ctrl Pts',(-10.5978126690739,-4.06383028861155,
-0.000517316456022585));
#50895=CARTESIAN_POINT('Ctrl Pts',(-11.8021873309261,-4.06398132384238,
-0.000969592099269029));
#50896=CARTESIAN_POINT('Ctrl Pts',(-11.7658734175648,-4.06530044997824,
-0.622465582635642));
#50897=CARTESIAN_POINT('Ctrl Pts',(-11.6500136158304,-3.63881171341208,
-2.60363619702803));
#50898=CARTESIAN_POINT('Ctrl Pts',(-11.4546079257229,-0.551767098271795,
-4.78271598680431));
#50899=CARTESIAN_POINT('Ctrl Pts',(-11.2159702606036,3.72518553231084,-3.04988719316482));
#50900=CARTESIAN_POINT('Ctrl Pts',(-10.9773325954844,4.57970763196809,1.48495695118139));
#50901=CARTESIAN_POINT('Ctrl Pts',(-10.7386949303652,1.22672621632081,4.65553025243742));
#50902=CARTESIAN_POINT('Ctrl Pts',(-10.5136465088458,-2.99816785865763,
3.6119546083943));
#50903=CARTESIAN_POINT('Ctrl Pts',(-10.3681439756994,-4.06300485973803,
1.11905048660218));
#50904=CARTESIAN_POINT('Ctrl Pts',(-10.3021873309261,-4.07305647823417,
-0.00339818811806027));
#50905=CARTESIAN_POINT('Origin',(-32.3478126690739,0.,0.));
#50906=CARTESIAN_POINT('',(-13.5978126690739,-4.07681666553846,-0.0012043583654883));
#50907=CARTESIAN_POINT('',(-13.3021873309261,-4.06948780842451,0.00374258894561955));
#50908=CARTESIAN_POINT('',(-32.3478126690739,-4.0705,-4.82875428449296E-13));
#50909=CARTESIAN_POINT('Ctrl Pts',(-13.5978126690739,-4.07681666553846,
-0.00120435836548843));
#50910=CARTESIAN_POINT('Ctrl Pts',(-13.5939672583865,-4.07707083999085,
-0.0664874041950833));
#50911=CARTESIAN_POINT('Ctrl Pts',(-13.5105759593261,-4.04602154531668,
-1.48196385087443));
#50912=CARTESIAN_POINT('Ctrl Pts',(-13.3476387718926,-2.40418173141341,
-4.17117876454601));
#50913=CARTESIAN_POINT('Ctrl Pts',(-13.1090011067734,2.20924341525388,-4.27762382820403));
#50914=CARTESIAN_POINT('Ctrl Pts',(-12.8703634416541,4.79297579923065,-0.454098085715957));
#50915=CARTESIAN_POINT('Ctrl Pts',(-12.6317257765349,2.97326932976115,3.78662007285696));
#50916=CARTESIAN_POINT('Ctrl Pts',(-12.3930881114157,-1.57806154943975,
4.54846609634954));
#50917=CARTESIAN_POINT('Ctrl Pts',(-12.2151170755953,-3.89111272737449,
2.00017169269057));
#50918=CARTESIAN_POINT('Ctrl Pts',(-12.1166919281481,-4.07329090803759,
0.325602789635245));
#50919=CARTESIAN_POINT('Ctrl Pts',(-12.0978126690739,-4.07032458744755,
0.00376143334710491));
#50920=CARTESIAN_POINT('Ctrl Pts',(-13.3021873309261,-4.06948780842451,
0.00374258894561951));
#50921=CARTESIAN_POINT('Ctrl Pts',(-13.2431487478032,-4.06042005381897,
-1.00323625051947));
#50922=CARTESIAN_POINT('Ctrl Pts',(-13.1045642763073,-3.17385622399582,
-3.38123201716333));
#50923=CARTESIAN_POINT('Ctrl Pts',(-12.8864339164382,0.817874959696777,
-4.74445989460021));
#50924=CARTESIAN_POINT('Ctrl Pts',(-12.647796251319,4.43348046720131,-1.87698430683722));
#50925=CARTESIAN_POINT('Ctrl Pts',(-12.4091585861998,3.9759253824068,2.71492845112022));
#50926=CARTESIAN_POINT('Ctrl Pts',(-12.1705209210805,-0.134421838351238,
4.81256167862222));
#50927=CARTESIAN_POINT('Ctrl Pts',(-11.9681971693227,-3.51458600877433,
2.84237865671728));
#50928=CARTESIAN_POINT('Ctrl Pts',(-11.8454193059378,-4.06241089469102,
0.738925854183665));
#50929=CARTESIAN_POINT('Ctrl Pts',(-11.8021873309261,-4.06398132384238,
-0.000969592099269029));
#50930=CARTESIAN_POINT('Origin',(-32.3478126690739,0.,0.));
#50931=CARTESIAN_POINT('',(-15.0978126690739,-4.06666337103388,-0.00316560979000432));
#50932=CARTESIAN_POINT('',(-14.8021873309261,-4.07709762639944,-0.00070430106655972));
#50933=CARTESIAN_POINT('',(-32.3478126690739,-4.0705,-4.82875428449296E-13));
#50934=CARTESIAN_POINT('Ctrl Pts',(-15.0978126690739,-4.06666337103388,
-0.00316560979000423));
#50935=CARTESIAN_POINT('Ctrl Pts',(-15.071242588625,-4.06994301140227,-0.457149458338325));
#50936=CARTESIAN_POINT('Ctrl Pts',(-14.965126619803,-3.79006310537379,-2.26634942371038));
#50937=CARTESIAN_POINT('Ctrl Pts',(-14.7794647626079,-1.13179168699179,
-4.67951596436188));
#50938=CARTESIAN_POINT('Ctrl Pts',(-14.5408270974888,3.32478553700414,-3.48204296590229));
#50939=CARTESIAN_POINT('Ctrl Pts',(-14.3021894323695,4.72679073178803,0.914478792178541));
#50940=CARTESIAN_POINT('Ctrl Pts',(-14.0635517672503,1.78616311715816,4.47084370140194));
#50941=CARTESIAN_POINT('Ctrl Pts',(-13.8287595128184,-2.72163337242562,
3.9286021789031));
#50942=CARTESIAN_POINT('Ctrl Pts',(-13.6735131467596,-4.07181300558473,
1.28395297745419));
#50943=CARTESIAN_POINT('Ctrl Pts',(-13.5978126690739,-4.07681666553846,
-0.00120435836548843));
#50944=CARTESIAN_POINT('Ctrl Pts',(-14.8021873309261,-4.07709762639944,
-0.000704301066560046));
#50945=CARTESIAN_POINT('Ctrl Pts',(-14.7999699664147,-4.07718738154795,
-0.0383412680213716));
#50946=CARTESIAN_POINT('Ctrl Pts',(-14.7182067135303,-4.05963949617112,
-1.42608358607219));
#50947=CARTESIAN_POINT('Ctrl Pts',(-14.5568975722728,-2.48900910600372,
-4.12112276102026));
#50948=CARTESIAN_POINT('Ctrl Pts',(-14.3182599071536,2.12127272581082,-4.32192331767929));
#50949=CARTESIAN_POINT('Ctrl Pts',(-14.0796222420344,4.78268288982128,-0.552053907312987));
#50950=CARTESIAN_POINT('Ctrl Pts',(-13.8409845769151,3.05011057970114,3.72500262990027));
#50951=CARTESIAN_POINT('Ctrl Pts',(-13.6023469117959,-1.48468231248816,
4.57979667366944));
#50952=CARTESIAN_POINT('Ctrl Pts',(-13.4227478297996,-3.8710120869076,2.05648068706029));
#50953=CARTESIAN_POINT('Ctrl Pts',(-13.3226946361763,-4.0726375319069,0.353521010938116));
#50954=CARTESIAN_POINT('Ctrl Pts',(-13.3021873309261,-4.06948780842451,
0.00374258894561951));
#50955=CARTESIAN_POINT('Origin',(-32.3478126690739,0.,0.));
#50956=CARTESIAN_POINT('',(-16.5978126690739,-4.06532180994014,0.00247865735123198));
#50957=CARTESIAN_POINT('',(-16.3021873309261,-4.06735933458706,-0.00339422375240483));
#50958=CARTESIAN_POINT('',(-32.3478126690739,-4.0705,-4.82875428449296E-13));
#50959=CARTESIAN_POINT('Ctrl Pts',(-16.5978126690739,-4.06532180994014,
0.00247865735123177));
#50960=CARTESIAN_POINT('Ctrl Pts',(-16.5485179188634,-4.06065576655941,
-0.840483409511789));
#50961=CARTESIAN_POINT('Ctrl Pts',(-16.4196772802799,-3.39353668499773,
-3.05048344280494));
#50962=CARTESIAN_POINT('Ctrl Pts',(-16.2112907533233,0.232268530165553,
-4.80883285354733));
#50963=CARTESIAN_POINT('Ctrl Pts',(-15.9726530882041,4.17103458301497,-2.40443186444421));
#50964=CARTESIAN_POINT('Ctrl Pts',(-15.7340154230849,4.27775630447756,2.20898689062749));
#50965=CARTESIAN_POINT('Ctrl Pts',(-15.4953777579657,0.454385510193501,
4.79294855924697));
#50966=CARTESIAN_POINT('Ctrl Pts',(-15.2833101732953,-3.31426516276753,
3.17607544524493));
#50967=CARTESIAN_POINT('Ctrl Pts',(-15.1507884769981,-4.06012437697437,
0.9019939062919));
#50968=CARTESIAN_POINT('Ctrl Pts',(-15.0978126690739,-4.06666337103388,
-0.00316560979000423));
#50969=CARTESIAN_POINT('Ctrl Pts',(-16.3021873309261,-4.06735933458706,
-0.0033942237524047));
#50970=CARTESIAN_POINT('Ctrl Pts',(-16.2772452966532,-4.07069882146085,
-0.42937696578519));
#50971=CARTESIAN_POINT('Ctrl Pts',(-16.1727573740072,-3.81276059892577,
-2.20997410073169));
#50972=CARTESIAN_POINT('Ctrl Pts',(-15.9887235629882,-1.22728457340874,
-4.65538309025602));
#50973=CARTESIAN_POINT('Ctrl Pts',(-15.7500858978689,3.25285668605437,-3.54932986930775));
#50974=CARTESIAN_POINT('Ctrl Pts',(-15.5114482327497,4.74450893241555,0.817590442335157));
#50975=CARTESIAN_POINT('Ctrl Pts',(-15.2728105676305,1.8772501705311,4.43336790018713));
#50976=CARTESIAN_POINT('Ctrl Pts',(-15.0363902670226,-2.67202280013241,
3.98033711867999));
#50977=CARTESIAN_POINT('Ctrl Pts',(-14.8795158547878,-4.07396749912098,
1.31184989664949));
#50978=CARTESIAN_POINT('Ctrl Pts',(-14.8021873309261,-4.07709762639944,
-0.000704301066560046));
#50979=CARTESIAN_POINT('Origin',(-32.3478126690739,0.,0.));
#50980=CARTESIAN_POINT('',(-18.0978126690739,-4.0757393762113,0.00222632843356818));
#50981=CARTESIAN_POINT('',(-17.8021873309261,-4.06484746876737,0.00211112861108809));
#50982=CARTESIAN_POINT('',(-32.3478126690739,-4.0705,-4.82875428449296E-13));
#50983=CARTESIAN_POINT('Ctrl Pts',(-18.0978126690739,-4.0757393762113,0.00222632843356826));
#50984=CARTESIAN_POINT('Ctrl Pts',(-18.0257932491019,-4.06769305643308,
-1.22129466881777));
#50985=CARTESIAN_POINT('Ctrl Pts',(-17.8742279407568,-2.83018048694797,
-3.8103087610216));
#50986=CARTESIAN_POINT('Ctrl Pts',(-17.6431167440387,1.5775160130308,-4.54865533010503));
#50987=CARTESIAN_POINT('Ctrl Pts',(-17.4044790789195,4.6794480846352,-1.13207230628853));
#50988=CARTESIAN_POINT('Ctrl Pts',(-17.1658414138002,3.48224234046452,3.3245767197852));
#50989=CARTESIAN_POINT('Ctrl Pts',(-16.927203748681,-0.914195334228,4.72684556277623));
#50990=CARTESIAN_POINT('Ctrl Pts',(-16.7378608337722,-3.73607127850369,
2.39382482140684));
#50991=CARTESIAN_POINT('Ctrl Pts',(-16.6280638072365,-4.06818526137017,
0.519786521610059));
#50992=CARTESIAN_POINT('Ctrl Pts',(-16.5978126690739,-4.06532180994014,
0.00247865735123177));
#50993=CARTESIAN_POINT('Ctrl Pts',(-17.8021873309261,-4.06484746876737,
0.00211112861108823));
#50994=CARTESIAN_POINT('Ctrl Pts',(-17.7545206268917,-4.0610311343114,-0.813248574751964));
#50995=CARTESIAN_POINT('Ctrl Pts',(-17.6273080344841,-3.42719055604098,
-2.99473654818825));
#50996=CARTESIAN_POINT('Ctrl Pts',(-17.4205495537035,0.133844637744424,
-4.81257776603306));
#50997=CARTESIAN_POINT('Ctrl Pts',(-17.1819118885843,4.1209734926491,-2.4892562371223));
#50998=CARTESIAN_POINT('Ctrl Pts',(-16.9432742234651,4.32205051844462,2.12101354478971));
#50999=CARTESIAN_POINT('Ctrl Pts',(-16.7046365583459,0.55234071436891,4.78264977563894));
#51000=CARTESIAN_POINT('Ctrl Pts',(-16.4909409274995,-3.27777761810244,
3.23139288635401));
#51001=CARTESIAN_POINT('Ctrl Pts',(-16.3567911850263,-4.06004842914805,
0.929180049887315));
#51002=CARTESIAN_POINT('Ctrl Pts',(-16.3021873309261,-4.06735933458706,
-0.0033942237524047));
#51003=CARTESIAN_POINT('Origin',(-32.3478126690739,0.,0.));
#51004=CARTESIAN_POINT('',(-19.5978126690739,-4.07223926118534,-0.00357729417079465));
#51005=CARTESIAN_POINT('',(-19.3021873309261,-4.07510605262456,0.00261196768466351));
#51006=CARTESIAN_POINT('',(-32.3478126690739,-4.0705,-4.82875428449296E-13));
#51007=CARTESIAN_POINT('Ctrl Pts',(-19.5978126690739,-4.07223926118534,
-0.00357729417079473));
#51008=CARTESIAN_POINT('Ctrl Pts',(-19.5826144677134,-4.07461978933759,
-0.262354039634738));
#51009=CARTESIAN_POINT('Ctrl Pts',(-19.4878703779799,-3.9340869821028,-1.87296646703573));
#51010=CARTESIAN_POINT('Ctrl Pts',(-19.3135803998733,-1.78669931964703,
-4.4706294438965));
#51011=CARTESIAN_POINT('Ctrl Pts',(-19.074942734754,2.79499160370957,-3.92005663462335));
#51012=CARTESIAN_POINT('Ctrl Pts',(-18.8363050696348,4.80884677358576,0.231980153537627));
#51013=CARTESIAN_POINT('Ctrl Pts',(-18.5976674045156,2.4046819888283,4.1708903864842));
#51014=CARTESIAN_POINT('Ctrl Pts',(-18.3590297393964,-2.20873035805718,
4.27788876536757));
#51015=CARTESIAN_POINT('Ctrl Pts',(-18.1924114942491,-4.01302793193152,
1.60849660347309));
#51016=CARTESIAN_POINT('Ctrl Pts',(-18.1053391374749,-4.07658026567666,
0.130091730952273));
#51017=CARTESIAN_POINT('Ctrl Pts',(-18.0978126690739,-4.0757393762113,0.00222632843356826));
#51018=CARTESIAN_POINT('Ctrl Pts',(-19.3021873309261,-4.07510605262456,
0.00261196768466343));
#51019=CARTESIAN_POINT('Ctrl Pts',(-19.2317959571301,-4.06618795069759,
-1.19373875342118));
#51020=CARTESIAN_POINT('Ctrl Pts',(-19.081858694961,-2.87659949644564,-3.75744888720017));
#51021=CARTESIAN_POINT('Ctrl Pts',(-18.8523755444189,1.48413301908516,-4.57997470766269));
#51022=CARTESIAN_POINT('Ctrl Pts',(-18.6137378792997,4.6553094840529,-1.22756374533297));
#51023=CARTESIAN_POINT('Ctrl Pts',(-18.3751002141804,3.54952493031783,3.25264383390203));
#51024=CARTESIAN_POINT('Ctrl Pts',(-18.1364625490612,-0.817305922033317,
4.74455795316888));
#51025=CARTESIAN_POINT('Ctrl Pts',(-17.9454915879764,-3.71098714745764,
2.45019360063996));
#51026=CARTESIAN_POINT('Ctrl Pts',(-17.8340665152647,-4.06739980864662,
0.547418441384662));
#51027=CARTESIAN_POINT('Ctrl Pts',(-17.8021873309261,-4.06484746876737,
0.00211112861108823));
#51028=CARTESIAN_POINT('Origin',(-32.3478126690739,0.,0.));
#51029=CARTESIAN_POINT('',(-21.0978126690739,-4.06383152666866,-0.000522675918812766));
#51030=CARTESIAN_POINT('',(-20.8021873309261,-4.07306601825716,-0.00339571005182004));
#51031=CARTESIAN_POINT('',(-32.3478126690739,-4.0705,-4.82875428449296E-13));
#51032=CARTESIAN_POINT('Ctrl Pts',(-21.0978126690739,-4.06383152666866,
-0.00052267591881365));
#51033=CARTESIAN_POINT('Ctrl Pts',(-21.0598897979519,-4.06457261097563,
-0.649615040927229));
#51034=CARTESIAN_POINT('Ctrl Pts',(-20.9424210384568,-3.6112055683889,-2.65924661123667));
#51035=CARTESIAN_POINT('Ctrl Pts',(-20.7454063905886,-0.454960354245989,
-4.79289402757069));
#51036=CARTESIAN_POINT('Ctrl Pts',(-20.5067687254694,3.78608510831067,-2.97395051002756));
#51037=CARTESIAN_POINT('Ctrl Pts',(-20.2681310603502,4.54874992244621,1.57724323631644));
#51038=CARTESIAN_POINT('Ctrl Pts',(-20.0294933952309,1.13235292151423,4.67938018808041));
#51039=CARTESIAN_POINT('Ctrl Pts',(-19.8060539314722,-3.04053113635729,
3.55867154707108));
#51040=CARTESIAN_POINT('Ctrl Pts',(-19.6621603560865,-4.06216033955295,
1.09205794767961));
#51041=CARTESIAN_POINT('Ctrl Pts',(-19.5978126690739,-4.07223926118534,
-0.00357729417079473));
#51042=CARTESIAN_POINT('Ctrl Pts',(-20.8021873309261,-4.07306601825716,
-0.0033957100518197));
#51043=CARTESIAN_POINT('Ctrl Pts',(-20.7886171757417,-4.07513318091976,
-0.234330901384573));
#51044=CARTESIAN_POINT('Ctrl Pts',(-20.6955011321841,-3.95202089787016,
-1.81676406404286));
#51045=CARTESIAN_POINT('Ctrl Pts',(-20.5228392002535,-1.87778187766528,
-4.43314271832978));
#51046=CARTESIAN_POINT('Ctrl Pts',(-20.2842015351343,2.71421312200688,-3.97641374475733));
#51047=CARTESIAN_POINT('Ctrl Pts',(-20.045563870015,4.81258578377826,0.133556036718511));
#51048=CARTESIAN_POINT('Ctrl Pts',(-19.8069262048958,2.48950335928912,4.12082420945821));
#51049=CARTESIAN_POINT('Ctrl Pts',(-19.5682885397766,-2.12075435614108,
4.32217770366716));
#51050=CARTESIAN_POINT('Ctrl Pts',(-19.4000422484533,-3.99744242114115,
1.66453839875525));
#51051=CARTESIAN_POINT('Ctrl Pts',(-19.3113418455032,-4.07626586652913,
0.158199357517422));
#51052=CARTESIAN_POINT('Ctrl Pts',(-19.3021873309261,-4.07510605262456,
0.00261196768466343));
#51053=CARTESIAN_POINT('Origin',(-32.3478126690739,0.,0.));
#51054=CARTESIAN_POINT('',(-22.5978126690739,-4.07031468847398,0.00376156571352546));
#51055=CARTESIAN_POINT('',(-22.3021873309261,-4.06398364289261,-0.000974823831897398));
#51056=CARTESIAN_POINT('',(-32.3478126690739,-4.0705,-4.82875428449296E-13));
#51057=CARTESIAN_POINT('Ctrl Pts',(-22.5978126690739,-4.07031468847398,
0.00376156571352537));
#51058=CARTESIAN_POINT('Ctrl Pts',(-22.5371651281903,-4.06078745327604,
-1.03012477253975));
#51059=CARTESIAN_POINT('Ctrl Pts',(-22.3969716989337,-3.13448885277667,
-3.4352501825917));
#51060=CARTESIAN_POINT('Ctrl Pts',(-22.177232381304,0.913628408435968,-4.7269551737383));
#51061=CARTESIAN_POINT('Ctrl Pts',(-21.9385947161847,4.47052229104313,-1.7869674112637));
#51062=CARTESIAN_POINT('Ctrl Pts',(-21.6999570510656,3.92022423769407,2.79475652063351));
#51063=CARTESIAN_POINT('Ctrl Pts',(-21.4613193859463,-0.231691776071347,
4.80886067632815));
#51064=CARTESIAN_POINT('Ctrl Pts',(-21.2606045919491,-3.54477519825892,
2.78695006207459));
#51065=CARTESIAN_POINT('Ctrl Pts',(-21.1394356863249,-4.06301813453931,
0.71190182958246));
#51066=CARTESIAN_POINT('Ctrl Pts',(-21.0978126690739,-4.06383152666866,
-0.00052267591881365));
#51067=CARTESIAN_POINT('Ctrl Pts',(-22.3021873309261,-4.06398364289261,
-0.000974823831896773));
#51068=CARTESIAN_POINT('Ctrl Pts',(-22.2658925059801,-4.06530923181794,
-0.622143240829621));
#51069=CARTESIAN_POINT('Ctrl Pts',(-22.150051792661,-3.63913463819147,-2.60297621081044));
#51070=CARTESIAN_POINT('Ctrl Pts',(-21.9546651909688,-0.552914322524486,
-4.78258349567352));
#51071=CARTESIAN_POINT('Ctrl Pts',(-21.7160275258496,3.72445384229878,-3.05078067349642));
#51072=CARTESIAN_POINT('Ctrl Pts',(-21.4773898607304,4.58006369995296,1.4838583643783));
#51073=CARTESIAN_POINT('Ctrl Pts',(-21.2387521956112,1.22784291284316,4.65523586110807));
#51074=CARTESIAN_POINT('Ctrl Pts',(-21.0136846856764,-2.99765973840581,
3.61258525206308));
#51075=CARTESIAN_POINT('Ctrl Pts',(-20.8681630641147,-4.06301583309485,
1.11937100559103));
#51076=CARTESIAN_POINT('Ctrl Pts',(-20.8021873309261,-4.07306601825716,
-0.0033957100518197));
#51077=CARTESIAN_POINT('Origin',(-32.3478126690739,0.,0.));
#51078=CARTESIAN_POINT('',(-24.0978126690739,-4.07682073202661,-0.00119862600692145));
#51079=CARTESIAN_POINT('',(-23.8021873309261,-4.06947811712022,0.00374200930701507));
#51080=CARTESIAN_POINT('',(-32.3478126690739,-4.0705,-4.82875428449296E-13));
#51081=CARTESIAN_POINT('Ctrl Pts',(-24.0978126690739,-4.07682073202661,
-0.0011986260069221));
#51082=CARTESIAN_POINT('Ctrl Pts',(-24.0939863468019,-4.07707257100012,
-0.0661574373907974));
#51083=CARTESIAN_POINT('Ctrl Pts',(-24.0106141361567,-4.04618464425921,
-1.48130837178561));
#51084=CARTESIAN_POINT('Ctrl Pts',(-23.8476960371386,-2.40518220884904,
-4.17060195021093));
#51085=CARTESIAN_POINT('Ctrl Pts',(-23.6090583720194,2.20821726762825,-4.27815364006511));
#51086=CARTESIAN_POINT('Ctrl Pts',(-23.3704207069001,4.7928667366398,-0.455247774302161));
#51087=CARTESIAN_POINT('Ctrl Pts',(-23.1317830417809,2.97417754833123,3.7859067598156));
#51088=CARTESIAN_POINT('Ctrl Pts',(-22.8931453766616,-1.57697045372341,
4.54884449829819));
#51089=CARTESIAN_POINT('Ctrl Pts',(-22.715155252426,-3.89088098364765,2.00083174485514));
#51090=CARTESIAN_POINT('Ctrl Pts',(-22.6167110165634,-4.07328346509314,
0.325930329695141));
#51091=CARTESIAN_POINT('Ctrl Pts',(-22.5978126690739,-4.07031468847398,
0.00376156571352537));
#51092=CARTESIAN_POINT('Ctrl Pts',(-23.8021873309261,-4.06947811712022,
0.00374200930701521));
#51093=CARTESIAN_POINT('Ctrl Pts',(-23.7431678362185,-4.06041648348459,
-1.00291735298318));
#51094=CARTESIAN_POINT('Ctrl Pts',(-23.6046024531379,-3.17431791098803,
-3.38058997938746));
#51095=CARTESIAN_POINT('Ctrl Pts',(-23.3864911816842,0.816736872430108,
-4.74465594332464));
#51096=CARTESIAN_POINT('Ctrl Pts',(-23.1478535165649,4.43303010358293,-1.87804772118901));
#51097=CARTESIAN_POINT('Ctrl Pts',(-22.9092158514458,3.97657650355884,2.71397465949093));
#51098=CARTESIAN_POINT('Ctrl Pts',(-22.6705781863265,-0.13326743518637,
4.81259378419344));
#51099=CARTESIAN_POINT('Ctrl Pts',(-22.4682353461533,-3.5142230495247,2.84303582389633));
#51100=CARTESIAN_POINT('Ctrl Pts',(-22.3454383943532,-4.06240399260436,
0.739246258441231));
#51101=CARTESIAN_POINT('Ctrl Pts',(-22.3021873309261,-4.06398364289261,
-0.000974823831896773));
#51102=CARTESIAN_POINT('Origin',(-32.3478126690739,0.,0.));
#51103=CARTESIAN_POINT('',(-25.5978126690739,-4.06667116509479,-0.00316860155561062));
#51104=CARTESIAN_POINT('',(-25.3021873309261,-4.07710011149971,-0.000698316132069499));
#51105=CARTESIAN_POINT('',(-32.3478126690739,-4.0705,-4.82875428449296E-13));
#51106=CARTESIAN_POINT('Ctrl Pts',(-25.5978126690739,-4.06667116509479,
-0.00316860155561056));
#51107=CARTESIAN_POINT('Ctrl Pts',(-25.5712616770403,-4.06995198256812,
-0.456824073053871));
#51108=CARTESIAN_POINT('Ctrl Pts',(-25.4651647966337,-3.79033356389561,
-2.26568828448685));
#51109=CARTESIAN_POINT('Ctrl Pts',(-25.2795220278539,-1.132913999441,-4.67924443383647));
#51110=CARTESIAN_POINT('Ctrl Pts',(-25.0408843627347,3.32395012330801,-3.48284034246832));
#51111=CARTESIAN_POINT('Ctrl Pts',(-24.8022466976155,4.72700999182265,0.913344916409211));
#51112=CARTESIAN_POINT('Ctrl Pts',(-24.5636090324962,1.78723547660136,4.47041513471273));
#51113=CARTESIAN_POINT('Ctrl Pts',(-24.3287976896491,-2.72105741290232,
3.9292109076427));
#51114=CARTESIAN_POINT('Ctrl Pts',(-24.1735322351749,-4.07183705933901,
1.28427935068815));
#51115=CARTESIAN_POINT('Ctrl Pts',(-24.0978126690739,-4.07682073202661,
-0.0011986260069221));
#51116=CARTESIAN_POINT('Ctrl Pts',(-25.3021873309261,-4.07710011149971,
-0.000698316132069399));
#51117=CARTESIAN_POINT('Ctrl Pts',(-25.2999890548301,-4.0771883891112,-0.0380112202494885));
#51118=CARTESIAN_POINT('Ctrl Pts',(-25.2182448903609,-4.05979569108433,
-1.42542869581234));
#51119=CARTESIAN_POINT('Ctrl Pts',(-25.0569548375188,-2.48999755919744,
-4.12052561435965));
#51120=CARTESIAN_POINT('Ctrl Pts',(-24.8183171723996,2.12023594681246,-4.32243201928095));
#51121=CARTESIAN_POINT('Ctrl Pts',(-24.5796795072803,4.78255033466597,-0.553201127887688));
#51122=CARTESIAN_POINT('Ctrl Pts',(-24.3410418421611,3.05100401366679,3.72427088853368));
#51123=CARTESIAN_POINT('Ctrl Pts',(-24.1024041770419,-1.48358370303888,
4.58015267461461));
#51124=CARTESIAN_POINT('Ctrl Pts',(-23.9227860066302,-3.87077237514414,
2.05714104990295));
#51125=CARTESIAN_POINT('Ctrl Pts',(-23.8227137245916,-4.07262966323526,
0.353848130340812));
#51126=CARTESIAN_POINT('Ctrl Pts',(-23.8021873309261,-4.06947811712022,
0.00374200930701521));
#51127=CARTESIAN_POINT('Origin',(-32.3478126690739,0.,0.));
#51128=CARTESIAN_POINT('',(-27.0978126690739,-4.06530890290629,0.00247015883041497));
#51129=CARTESIAN_POINT('',(-26.8021873309261,-4.0673676331488,-0.00339676908166275));
#51130=CARTESIAN_POINT('',(-32.3478126690739,-4.0705,-4.82875428449296E-13));
#51131=CARTESIAN_POINT('Ctrl Pts',(-27.0978126690739,-4.06530890290629,
0.0024701588304149));
#51132=CARTESIAN_POINT('Ctrl Pts',(-27.0485370072788,-4.06065548839014,
-0.840166902292313));
#51133=CARTESIAN_POINT('Ctrl Pts',(-26.9197154571106,-3.39394710335117,
-3.04982355875152));
#51134=CARTESIAN_POINT('Ctrl Pts',(-26.7113480185693,0.231122040344854,
-4.80889290141546));
#51135=CARTESIAN_POINT('Ctrl Pts',(-26.4727103534501,4.17045404914302,-2.40542998080026));
#51136=CARTESIAN_POINT('Ctrl Pts',(-26.2340726883308,4.27828796113812,2.20795949931288));
#51137=CARTESIAN_POINT('Ctrl Pts',(-25.9954350232116,0.45553419918425,4.79284005902739));
#51138=CARTESIAN_POINT('Ctrl Pts',(-25.7833483501259,-3.31384212136007,
3.1767246763176));
#51139=CARTESIAN_POINT('Ctrl Pts',(-25.6508075654134,-4.06012276262123,
0.902312619466092));
#51140=CARTESIAN_POINT('Ctrl Pts',(-25.5978126690739,-4.06667116509479,
-0.00316860155561056));
#51141=CARTESIAN_POINT('Ctrl Pts',(-26.8021873309261,-4.0673676331488,-0.00339676908166248));
#51142=CARTESIAN_POINT('Ctrl Pts',(-26.7772643850685,-4.07070764203952,
-0.429051031665485));
#51143=CARTESIAN_POINT('Ctrl Pts',(-26.6727955508379,-3.81302358814286,
-2.20931218578228));
#51144=CARTESIAN_POINT('Ctrl Pts',(-26.4887808282342,-1.22840035655279,
-4.65508935177024));
#51145=CARTESIAN_POINT('Ctrl Pts',(-26.2501431631149,3.25200474977257,-3.55010962682765));
#51146=CARTESIAN_POINT('Ctrl Pts',(-26.0115054979957,4.74470515142096,0.816452129912828));
#51147=CARTESIAN_POINT('Ctrl Pts',(-25.7728678328764,1.87831343359306,4.43291758398628));
#51148=CARTESIAN_POINT('Ctrl Pts',(-25.5364284438533,-2.67143520246076,
3.98094140217226));
#51149=CARTESIAN_POINT('Ctrl Pts',(-25.3795349432031,-4.07399401282602,
1.31217773515604));
#51150=CARTESIAN_POINT('Ctrl Pts',(-25.3021873309261,-4.07710011149971,
-0.000698316132069399));
#51151=CARTESIAN_POINT('Origin',(-32.3478126690739,0.,0.));
#51152=CARTESIAN_POINT('',(-28.5978126690739,-4.07533558288693,0.00197868943318482));
#51153=CARTESIAN_POINT('',(-28.3021873309261,-4.06480101368718,0.00206955444756823));
#51154=CARTESIAN_POINT('',(-32.3478126690739,-4.0705,-4.82875428449296E-13));
#51155=CARTESIAN_POINT('Ctrl Pts',(-28.5978126690739,-4.07533558288693,
0.00197868943318465));
#51156=CARTESIAN_POINT('Ctrl Pts',(-28.5258123375172,-4.0671548117311,-1.22130223361166));
#51157=CARTESIAN_POINT('Ctrl Pts',(-28.3742661175874,-2.83137270070474,
-3.80928172890928));
#51158=CARTESIAN_POINT('Ctrl Pts',(-28.1431740092847,1.57677629758835,-4.54925739906848));
#51159=CARTESIAN_POINT('Ctrl Pts',(-27.9045363441654,4.67899334175034,-1.13307817052668));
#51160=CARTESIAN_POINT('Ctrl Pts',(-27.6658986790463,3.48313507021902,3.32368060727122));
#51161=CARTESIAN_POINT('Ctrl Pts',(-27.4272610139269,-0.913111142894123,
4.72709634916456));
#51162=CARTESIAN_POINT('Ctrl Pts',(-27.2378990106029,-3.7357712242627,2.39447925508501));
#51163=CARTESIAN_POINT('Ctrl Pts',(-27.1280828956518,-4.06816751315389,
0.520105312452931));
#51164=CARTESIAN_POINT('Ctrl Pts',(-27.0978126690739,-4.06530890290629,
0.0024701588304149));
#51165=CARTESIAN_POINT('Ctrl Pts',(-28.3021873309261,-4.06480101368718,
0.00206955444756761));
#51166=CARTESIAN_POINT('Ctrl Pts',(-28.254539715307,-4.06101200920254,-0.812950610202758));
#51167=CARTESIAN_POINT('Ctrl Pts',(-28.1273462113148,-3.42764719991074,
-2.99402214660032));
#51168=CARTESIAN_POINT('Ctrl Pts',(-27.9206068189495,0.132734120902733,
-4.81264906024345));
#51169=CARTESIAN_POINT('Ctrl Pts',(-27.6819691538303,4.12035340306242,-2.4902241816421));
#51170=CARTESIAN_POINT('Ctrl Pts',(-27.4433314887111,4.32257108085691,2.11996606838733));
#51171=CARTESIAN_POINT('Ctrl Pts',(-27.2046938235918,0.55348171480276,4.78252270942354));
#51172=CARTESIAN_POINT('Ctrl Pts',(-26.9909791043302,-3.27734231397027,
3.2320385418624));
#51173=CARTESIAN_POINT('Ctrl Pts',(-26.8568102734416,-4.06004742651346,
0.929498100146529));
#51174=CARTESIAN_POINT('Ctrl Pts',(-26.8021873309261,-4.0673676331488,-0.00339676908166248));
#51175=CARTESIAN_POINT('Ctrl Pts',(-30.0683458050225,-1.79217368492187,
3.65473442716069));
#51176=CARTESIAN_POINT('Ctrl Pts',(-30.028572860836,-2.40105433738203,3.3561573610714));
#51177=CARTESIAN_POINT('Ctrl Pts',(-29.9490269724629,-3.45744192369399,
2.44891896771775));
#51178=CARTESIAN_POINT('Ctrl Pts',(-29.7899351957168,-4.48692818459232,
-0.165939112378094));
#51179=CARTESIAN_POINT('Ctrl Pts',(-29.5910704747841,-3.05580029857719,
-3.71995065683383));
#51180=CARTESIAN_POINT('Ctrl Pts',(-29.3524328096649,1.48524338711596,-4.58231611323432));
#51181=CARTESIAN_POINT('Ctrl Pts',(-29.1137951445456,4.65387018191312,-1.22765401651987));
#51182=CARTESIAN_POINT('Ctrl Pts',(-28.8751574794264,3.55090078994383,3.25125842872222));
#51183=CARTESIAN_POINT('Ctrl Pts',(-28.6365198143072,-0.816478135197904,
4.74503193420896));
#51184=CARTESIAN_POINT('Ctrl Pts',(-28.3978821491879,-4.4326431471991,1.8784345171529));
#51185=CARTESIAN_POINT('Ctrl Pts',(-28.1592444840687,-3.97698621643786,
-2.71342222480818));
#51186=CARTESIAN_POINT('Ctrl Pts',(-27.9206068189495,0.132734120902733,
-4.81264906024345));
#51187=CARTESIAN_POINT('Ctrl Pts',(-27.6819691538303,4.12035340306242,-2.4902241816421));
#51188=CARTESIAN_POINT('Ctrl Pts',(-27.4433314887111,4.32257108085691,2.11996606838733));
#51189=CARTESIAN_POINT('Ctrl Pts',(-27.2046938235918,0.55348171480276,4.78252270942354));
#51190=CARTESIAN_POINT('Ctrl Pts',(-26.9660561584726,-3.72408468243647,
3.05122444962453));
#51191=CARTESIAN_POINT('Ctrl Pts',(-26.7274184933533,-4.58024332037796,
-1.48330752890949));
#51192=CARTESIAN_POINT('Ctrl Pts',(-26.4887808282342,-1.22840035655279,
-4.65508935177024));
#51193=CARTESIAN_POINT('Ctrl Pts',(-26.2501431631149,3.25200474977257,-3.55010962682765));
#51194=CARTESIAN_POINT('Ctrl Pts',(-26.0115054979957,4.74470515142096,0.816452129912828));
#51195=CARTESIAN_POINT('Ctrl Pts',(-25.7728678328764,1.87831343359306,4.43291758398628));
#51196=CARTESIAN_POINT('Ctrl Pts',(-25.5342301677573,-2.71373612241715,
3.97673919017804));
#51197=CARTESIAN_POINT('Ctrl Pts',(-25.295592502638,-4.81260180106317,-0.132978803016981));
#51198=CARTESIAN_POINT('Ctrl Pts',(-25.0569548375188,-2.48999755919744,
-4.12052561435965));
#51199=CARTESIAN_POINT('Ctrl Pts',(-24.8183171723996,2.12023594681246,-4.32243201928095));
#51200=CARTESIAN_POINT('Ctrl Pts',(-24.5796795072803,4.78255033466597,-0.553201127887688));
#51201=CARTESIAN_POINT('Ctrl Pts',(-24.3410418421611,3.05100401366679,3.72427088853368));
#51202=CARTESIAN_POINT('Ctrl Pts',(-24.1024041770419,-1.48358370303888,
4.58015267461461));
#51203=CARTESIAN_POINT('Ctrl Pts',(-23.8637665119226,-4.65516222209766,
1.22812207654118));
#51204=CARTESIAN_POINT('Ctrl Pts',(-23.6251288468034,-3.54991501369184,
-3.25221809482192));
#51205=CARTESIAN_POINT('Ctrl Pts',(-23.3864911816842,0.816736872430108,
-4.74465594332464));
#51206=CARTESIAN_POINT('Ctrl Pts',(-23.1478535165649,4.43303010358293,-1.87804772118901));
#51207=CARTESIAN_POINT('Ctrl Pts',(-22.9092158514458,3.97657650355884,2.71397465949093));
#51208=CARTESIAN_POINT('Ctrl Pts',(-22.6705781863265,-0.13326743518637,
4.81259378419344));
#51209=CARTESIAN_POINT('Ctrl Pts',(-22.4319405212073,-4.12067491146169,
2.48975047251535));
#51210=CARTESIAN_POINT('Ctrl Pts',(-22.1933028560881,-4.32230487333938,
-2.12049515987218));
#51211=CARTESIAN_POINT('Ctrl Pts',(-21.9546651909688,-0.552914322524486,
-4.78258349567352));
#51212=CARTESIAN_POINT('Ctrl Pts',(-21.7160275258496,3.72445384229878,-3.05078067349642));
#51213=CARTESIAN_POINT('Ctrl Pts',(-21.4773898607304,4.58006369995296,1.4838583643783));
#51214=CARTESIAN_POINT('Ctrl Pts',(-21.2387521956112,1.22784291284316,4.65523586110807));
#51215=CARTESIAN_POINT('Ctrl Pts',(-21.0001145304919,-3.25243097005294,
3.54971997856348));
#51216=CARTESIAN_POINT('Ctrl Pts',(-20.7614768653727,-4.74460695685984,
-0.817021398792471));
#51217=CARTESIAN_POINT('Ctrl Pts',(-20.5228392002535,-1.87778187766528,
-4.43314271832978));
#51218=CARTESIAN_POINT('Ctrl Pts',(-20.2842015351343,2.71421312200688,-3.97641374475733));
#51219=CARTESIAN_POINT('Ctrl Pts',(-20.045563870015,4.81258578377826,0.133556036718511));
#51220=CARTESIAN_POINT('Ctrl Pts',(-19.8069262048958,2.48950335928912,4.12082420945821));
#51221=CARTESIAN_POINT('Ctrl Pts',(-19.5682885397766,-2.12075435614108,
4.32217770366716));
#51222=CARTESIAN_POINT('Ctrl Pts',(-19.3296508746574,-4.7826166442574,0.552627519438542));
#51223=CARTESIAN_POINT('Ctrl Pts',(-19.0910132095381,-3.05055731986689,
-3.72463678489262));
#51224=CARTESIAN_POINT('Ctrl Pts',(-18.8523755444189,1.48413301908516,-4.57997470766269));
#51225=CARTESIAN_POINT('Ctrl Pts',(-18.6137378792997,4.6553094840529,-1.22756374533297));
#51226=CARTESIAN_POINT('Ctrl Pts',(-18.3751002141804,3.54952493031783,3.25264383390203));
#51227=CARTESIAN_POINT('Ctrl Pts',(-18.1364625490612,-0.817305922033317,
4.74455795316888));
#51228=CARTESIAN_POINT('Ctrl Pts',(-17.897824883942,-4.43325531722986,1.87751602747407));
#51229=CARTESIAN_POINT('Ctrl Pts',(-17.6591872188228,-3.97625097160617,
-2.71445157480656));
#51230=CARTESIAN_POINT('Ctrl Pts',(-17.4205495537035,0.133844637744424,
-4.81257776603306));
#51231=CARTESIAN_POINT('Ctrl Pts',(-17.1819118885843,4.1209734926491,-2.4892562371223));
#51232=CARTESIAN_POINT('Ctrl Pts',(-16.9432742234651,4.32205051844462,2.12101354478971));
#51233=CARTESIAN_POINT('Ctrl Pts',(-16.7046365583459,0.55234071436891,4.78264977563894));
#51234=CARTESIAN_POINT('Ctrl Pts',(-16.4659988932266,-3.72481971409399,
3.05033395526876));
#51235=CARTESIAN_POINT('Ctrl Pts',(-16.2273612281074,-4.57988569890107,
-1.48440766845576));
#51236=CARTESIAN_POINT('Ctrl Pts',(-15.9887235629882,-1.22728457340874,
-4.65538309025602));
#51237=CARTESIAN_POINT('Ctrl Pts',(-15.7500858978689,3.25285668605437,-3.54932986930775));
#51238=CARTESIAN_POINT('Ctrl Pts',(-15.5114482327497,4.74450893241555,0.817590442335157));
#51239=CARTESIAN_POINT('Ctrl Pts',(-15.2728105676305,1.8772501705311,4.43336790018713));
#51240=CARTESIAN_POINT('Ctrl Pts',(-15.0341729025113,-2.71469001784463,
3.97608818415582));
#51241=CARTESIAN_POINT('Ctrl Pts',(-14.795535237392,-4.81256973098103,-0.134133238289019));
#51242=CARTESIAN_POINT('Ctrl Pts',(-14.5568975722728,-2.48900910600372,
-4.12112276102026));
#51243=CARTESIAN_POINT('Ctrl Pts',(-14.3182599071536,2.12127272581082,-4.32192331767929));
#51244=CARTESIAN_POINT('Ctrl Pts',(-14.0796222420344,4.78268288982128,-0.552053907312987));
#51245=CARTESIAN_POINT('Ctrl Pts',(-13.8409845769151,3.05011057970114,3.72500262990027));
#51246=CARTESIAN_POINT('Ctrl Pts',(-13.6023469117959,-1.48468231248816,
4.57979667366944));
#51247=CARTESIAN_POINT('Ctrl Pts',(-13.3637092466767,-4.65545667971761,
1.22700539707102));
#51248=CARTESIAN_POINT('Ctrl Pts',(-13.1250715815574,-3.5491347955337,-3.25306952650887));
#51249=CARTESIAN_POINT('Ctrl Pts',(-12.8864339164382,0.817874959696777,
-4.74445989460021));
#51250=CARTESIAN_POINT('Ctrl Pts',(-12.647796251319,4.43348046720131,-1.87698430683722));
#51251=CARTESIAN_POINT('Ctrl Pts',(-12.4091585861998,3.9759253824068,2.71492845112022));
#51252=CARTESIAN_POINT('Ctrl Pts',(-12.1705209210805,-0.134421838351238,
4.81256167862222));
#51253=CARTESIAN_POINT('Ctrl Pts',(-11.9318832559613,-4.12127201457121,
2.48876196593426));
#51254=CARTESIAN_POINT('Ctrl Pts',(-11.6932455908421,-4.32179610137161,
-2.12153189920346));
#51255=CARTESIAN_POINT('Ctrl Pts',(-11.4546079257229,-0.551767098271795,
-4.78271598680431));
#51256=CARTESIAN_POINT('Ctrl Pts',(-11.2159702606036,3.72518553231084,-3.04988719316482));
#51257=CARTESIAN_POINT('Ctrl Pts',(-10.9773325954844,4.57970763196809,1.48495695118139));
#51258=CARTESIAN_POINT('Ctrl Pts',(-10.7386949303652,1.22672621632081,4.65553025243742));
#51259=CARTESIAN_POINT('Ctrl Pts',(-10.500057265246,-3.25328235526483,3.54893970899639));
#51260=CARTESIAN_POINT('Ctrl Pts',(-10.2614196001267,-4.74441083972299,
-0.81815947411722));
#51261=CARTESIAN_POINT('Ctrl Pts',(-10.0227819350075,-1.8767184363934,-4.43359301827195));
#51262=CARTESIAN_POINT('Ctrl Pts',(-9.78414426988828,2.71516687463254,-3.97576256635973));
#51263=CARTESIAN_POINT('Ctrl Pts',(-9.54550660476906,4.8125536089566,0.134710437930172));
#51264=CARTESIAN_POINT('Ctrl Pts',(-9.30686893964983,2.48851481691486,4.12142125330121));
#51265=CARTESIAN_POINT('Ctrl Pts',(-9.06823127453061,-2.12179106496689,
4.32166886952238));
#51266=CARTESIAN_POINT('Ctrl Pts',(-8.82959360941138,-4.78274906658767,
0.551480287245675));
#51267=CARTESIAN_POINT('Ctrl Pts',(-8.59095594429215,-3.04966379566106,
-3.72536842132379));
#51268=CARTESIAN_POINT('Ctrl Pts',(-8.35231827917293,1.48523158453539,-4.57961857379977));
#51269=CARTESIAN_POINT('Ctrl Pts',(-8.1136806140537,4.65560380841346,-1.22644703115444));
#51270=CARTESIAN_POINT('Ctrl Pts',(-7.87504294893448,3.54874460969979,3.25349517231261));
#51271=CARTESIAN_POINT('Ctrl Pts',(-7.63640528381524,-0.818443985601727,
4.74436176780107));
#51272=CARTESIAN_POINT('Ctrl Pts',(-7.39776761869602,-4.43370555338651,
1.87645255916802));
#51273=CARTESIAN_POINT('Ctrl Pts',(-7.1591299535768,-3.97559973603849,-2.71540528831811));
#51274=CARTESIAN_POINT('Ctrl Pts',(-6.92049228845756,0.134999037069343,
-4.81254552210429));
#51275=CARTESIAN_POINT('Ctrl Pts',(-6.68185462333835,4.1215704771241,-2.48826765871595));
#51276=CARTESIAN_POINT('Ctrl Pts',(-6.44321695821911,4.32154162229638,2.12205022265777));
#51277=CARTESIAN_POINT('Ctrl Pts',(-6.20457929309988,0.551193473920355,
4.78278213002022));
#51278=CARTESIAN_POINT('Ctrl Pts',(-5.96594162798067,-3.72555129633323,
3.04944038556121));
#51279=CARTESIAN_POINT('Ctrl Pts',(-5.72730396286143,-4.57952950032639,
-1.48550620942175));
#51280=CARTESIAN_POINT('Ctrl Pts',(-5.48866629774222,-1.22616783934351,
-4.65567735364785));
#51281=CARTESIAN_POINT('Ctrl Pts',(-5.25002863262297,3.25370797337249,-3.54854948612432));
#51282=CARTESIAN_POINT('Ctrl Pts',(-5.01139096750376,4.74431268704714,0.818728472038551));
#51283=CARTESIAN_POINT('Ctrl Pts',(-4.77275330238453,1.87618665939981,4.43381811498155));
#51284=CARTESIAN_POINT('Ctrl Pts',(-4.5341156372653,-2.71564366192391,3.97543680999486));
#51285=CARTESIAN_POINT('Ctrl Pts',(-4.29547797214608,-4.812537476128,-0.135287479444116));
#51286=CARTESIAN_POINT('Ctrl Pts',(-4.05684030702684,-2.48802037989938,
-4.12171998606955));
#51287=CARTESIAN_POINT('Ctrl Pts',(-3.81820264190762,2.12230915839156,-4.32141378384957));
#51288=CARTESIAN_POINT('Ctrl Pts',(-3.5795649767884,4.78281558760628,-0.550907763508576));
#51289=CARTESIAN_POINT('Ctrl Pts',(-3.34092731166917,3.04921617498962,3.72573627855867));
#51290=CARTESIAN_POINT('Ctrl Pts',(-3.10228964654994,-1.48577931367711,
4.57943634031457));
#51291=CARTESIAN_POINT('Ctrl Pts',(-2.86365198143072,-4.65575379041631,
1.22589645476151));
#51292=CARTESIAN_POINT('Ctrl Pts',(-2.62501431631149,-3.54834876796527,
-3.25393575552032));
#51293=CARTESIAN_POINT('Ctrl Pts',(-2.38637665119226,0.819002242401078,
-4.74423481374027));
#51294=CARTESIAN_POINT('Ctrl Pts',(-2.14773898607304,4.43395122223712,-1.87597598138563));
#51295=CARTESIAN_POINT('Ctrl Pts',(-1.90910132095381,3.97523440584382,2.71598802545506));
#51296=CARTESIAN_POINT('Ctrl Pts',(-1.67046365583458,-0.135500177452599,
4.81232596646912));
#51297=CARTESIAN_POINT('Ctrl Pts',(-1.43182599071536,-4.12201486774593,
2.48816358626208));
#51298=CARTESIAN_POINT('Ctrl Pts',(-1.19318832559613,-4.32100676816269,
-2.12331775762679));
#51299=CARTESIAN_POINT('Ctrl Pts',(-0.9545506604769,-0.551158953576692,
-4.78140835552346));
#51300=CARTESIAN_POINT('Ctrl Pts',(-0.715912995357679,3.72696190987269,
-3.05177387808086));
#51301=CARTESIAN_POINT('Ctrl Pts',(-0.477275330238447,4.57725222884596,
1.49154630755727));
#51302=CARTESIAN_POINT('Ctrl Pts',(-0.278410609305757,1.78830202401348,
4.11849926473408));
#51303=CARTESIAN_POINT('Ctrl Pts',(-0.119318832559607,-1.02190788268887,
4.1117895186236));
#51304=CARTESIAN_POINT('Ctrl Pts',(-0.0397729441865359,-2.25151393523441,
3.45825666525491));
#51305=CARTESIAN_POINT('Ctrl Pts',(0.,-2.75129702511903,2.99988915288068));
#51306=CARTESIAN_POINT('Ctrl Pts',(-29.9038972033484,-1.91758108071807,
3.91047455474608));
#51307=CARTESIAN_POINT('Ctrl Pts',(-29.8641242591618,-2.56906817116925,
3.59100455142768));
#51308=CARTESIAN_POINT('Ctrl Pts',(-29.7845783707887,-3.69937650370433,
2.62028213013966));
#51309=CARTESIAN_POINT('Ctrl Pts',(-29.6254865940426,-4.80090108994663,
-0.177550705673484));
#51310=CARTESIAN_POINT('Ctrl Pts',(-29.4266218731099,-3.26962999641403,
-3.98025429162597));
#51311=CARTESIAN_POINT('Ctrl Pts',(-29.1879842079907,1.58917332809701,-4.90296379114112));
#51312=CARTESIAN_POINT('Ctrl Pts',(-28.9493465428715,4.97952485746032,-1.31355913522901));
#51313=CARTESIAN_POINT('Ctrl Pts',(-28.7107088777522,3.79937515632038,3.47876531381764));
#51314=CARTESIAN_POINT('Ctrl Pts',(-28.472071212633,-0.873611211930994,
5.07706565551933));
#51315=CARTESIAN_POINT('Ctrl Pts',(-28.2334335475137,-4.74281745578375,
2.00987801671541));
#51316=CARTESIAN_POINT('Ctrl Pts',(-27.9947958823946,-4.25527592056482,
-2.90329400887223));
#51317=CARTESIAN_POINT('Ctrl Pts',(-27.7561582172753,0.142022194137876,
-5.14941429154002));
#51318=CARTESIAN_POINT('Ctrl Pts',(-27.5175205521561,4.40867522944874,-2.66447767738084));
#51319=CARTESIAN_POINT('Ctrl Pts',(-27.2788828870369,4.62504309400783,2.26831074393387));
#51320=CARTESIAN_POINT('Ctrl Pts',(-27.0402452219176,0.59221161082695,5.1171798486122));
#51321=CARTESIAN_POINT('Ctrl Pts',(-26.8016075567984,-3.98467759576748,
3.26473395232318));
#51322=CARTESIAN_POINT('Ctrl Pts',(-26.5629698916792,-4.90074595455584,
-1.58710200816697));
#51323=CARTESIAN_POINT('Ctrl Pts',(-26.3243322265599,-1.31435770042331,
-4.9808293387569));
#51324=CARTESIAN_POINT('Ctrl Pts',(-26.0856945614408,3.47956385870106,-3.79852863154653));
#51325=CARTESIAN_POINT('Ctrl Pts',(-25.8470568963215,5.07671600609805,0.873583386925484));
#51326=CARTESIAN_POINT('Ctrl Pts',(-25.6084192312023,2.00974846033062,4.74311109629157));
#51327=CARTESIAN_POINT('Ctrl Pts',(-25.3697815660831,-2.90362987147378,
4.25501160863666));
#51328=CARTESIAN_POINT('Ctrl Pts',(-25.1311439009638,-5.14936372539749,
-0.14228399788883));
#51329=CARTESIAN_POINT('Ctrl Pts',(-24.8925062358446,-2.66423519702527,
-4.40885949123555));
#51330=CARTESIAN_POINT('Ctrl Pts',(-24.6538685707254,2.26859950710815,-4.62489430159482));
#51331=CARTESIAN_POINT('Ctrl Pts',(-24.4152309056061,5.11720940693162,-0.591911389835893));
#51332=CARTESIAN_POINT('Ctrl Pts',(-24.1765932404869,3.26449809135411,3.98487683164073));
#51333=CARTESIAN_POINT('Ctrl Pts',(-23.9379555753677,-1.58739750758757,
4.90064896585306));
#51334=CARTESIAN_POINT('Ctrl Pts',(-23.6993179102485,-4.9809073081872,1.31405994776134));
#51335=CARTESIAN_POINT('Ctrl Pts',(-23.4606802451292,-3.79832040035196,
-3.47979213257527));
#51336=CARTESIAN_POINT('Ctrl Pts',(-23.22204258001,0.873888054307114,-5.07666335466403));
#51337=CARTESIAN_POINT('Ctrl Pts',(-22.9834049148908,4.74323148944965,-2.00946415469484));
#51338=CARTESIAN_POINT('Ctrl Pts',(-22.7447672497716,4.25483753801745,2.90388510018491));
#51339=CARTESIAN_POINT('Ctrl Pts',(-22.5061295846524,-0.142592827101065,
5.14935514754711));
#51340=CARTESIAN_POINT('Ctrl Pts',(-22.2674919195331,-4.40901923540582,
2.66397082044679));
#51341=CARTESIAN_POINT('Ctrl Pts',(-22.0288542544139,-4.624758258613,-2.26887685860782));
#51342=CARTESIAN_POINT('Ctrl Pts',(-21.7902165892947,-0.591604515260647,
-5.11724488838146));
#51343=CARTESIAN_POINT('Ctrl Pts',(-21.5515789241754,3.98507258759985,-3.26425912295005));
#51344=CARTESIAN_POINT('Ctrl Pts',(-21.3129412590562,4.90055376518737,1.58769138836067));
#51345=CARTESIAN_POINT('Ctrl Pts',(-21.074303593937,1.31376124957698,4.98098610008909));
#51346=CARTESIAN_POINT('Ctrl Pts',(-20.8356659288178,-3.4800199037556,3.7981117176359));
#51347=CARTESIAN_POINT('Ctrl Pts',(-20.5970282636985,-5.0766109403702,-0.874192490408381));
#51348=CARTESIAN_POINT('Ctrl Pts',(-20.3583905985793,-2.00917970876428,
-4.74335198441606));
#51349=CARTESIAN_POINT('Ctrl Pts',(-20.11975293346,2.90414024912104,-4.25466339016496));
#51350=CARTESIAN_POINT('Ctrl Pts',(-19.8811152683409,5.14934658730268,0.142901623532206));
#51351=CARTESIAN_POINT('Ctrl Pts',(-19.6424776032216,2.66370641546674,4.40917898053317));
#51352=CARTESIAN_POINT('Ctrl Pts',(-19.4038399381024,-2.26915419214175,
4.62462219023996));
#51353=CARTESIAN_POINT('Ctrl Pts',(-19.1652022729832,-5.11728035653827,
0.591297643122014));
#51354=CARTESIAN_POINT('Ctrl Pts',(-18.9265646078639,-3.26402014014505,
-3.985268331606));
#51355=CARTESIAN_POINT('Ctrl Pts',(-18.6879269427447,1.58798526203712,-4.90045854565949));
#51356=CARTESIAN_POINT('Ctrl Pts',(-18.4492892776255,4.98106487480121,-1.31346254731367));
#51357=CARTESIAN_POINT('Ctrl Pts',(-18.2106516125063,3.79790302088468,3.48024766275753));
#51358=CARTESIAN_POINT('Ctrl Pts',(-17.9720139473871,-0.874496923169711,
5.07655850764482));
#51359=CARTESIAN_POINT('Ctrl Pts',(-17.7333762822678,-4.74347246242682,
2.00889525569968));
#51360=CARTESIAN_POINT('Ctrl Pts',(-17.4947386171486,-4.25448922695873,
-2.90439538766098));
#51361=CARTESIAN_POINT('Ctrl Pts',(-17.2561009520293,0.143210419421708,
-5.14933800851558));
#51362=CARTESIAN_POINT('Ctrl Pts',(-17.0174632869101,4.40933870981885,-2.66344200092047));
#51363=CARTESIAN_POINT('Ctrl Pts',(-16.7788256217909,4.62448610522848,2.26943151752217));
#51364=CARTESIAN_POINT('Ctrl Pts',(-16.5401879566717,0.590990768860884,
5.11731580628902));
#51365=CARTESIAN_POINT('Ctrl Pts',(-16.3015502915524,-3.98546406128254,
3.2637811456039));
#51366=CARTESIAN_POINT('Ctrl Pts',(-16.0629126264332,-4.90036330850768,
-1.58827913000388));
#51367=CARTESIAN_POINT('Ctrl Pts',(-15.824274961314,-1.31316384032749,-4.98114363160013));
#51368=CARTESIAN_POINT('Ctrl Pts',(-15.5856372961948,3.48047540924424,-3.79769431047581));
#51369=CARTESIAN_POINT('Ctrl Pts',(-15.3469996310755,5.07650605666312,0.874801352786364));
#51370=CARTESIAN_POINT('Ctrl Pts',(-15.1083619659563,2.00861079541087,4.74359292337918));
#51371=CARTESIAN_POINT('Ctrl Pts',(-14.8697243008371,-2.90465051575626,
4.25431504845271));
#51372=CARTESIAN_POINT('Ctrl Pts',(-14.6310866357179,-5.1493294112106,-0.143519214796206));
#51373=CARTESIAN_POINT('Ctrl Pts',(-14.3924489705986,-2.66317757679605,
-4.4094984232478));
#51374=CARTESIAN_POINT('Ctrl Pts',(-14.1538113054794,2.26970883474132,-4.62435000358661));
#51375=CARTESIAN_POINT('Ctrl Pts',(-13.9151736403602,5.11735123763705,-0.590683892474468));
#51376=CARTESIAN_POINT('Ctrl Pts',(-13.676535975241,3.26354213932567,3.98565977662667));
#51377=CARTESIAN_POINT('Ctrl Pts',(-13.4378983101217,-1.58857299225892,
4.90026805373337));
#51378=CARTESIAN_POINT('Ctrl Pts',(-13.1992606450025,-4.98122237048603,
1.31286512861896));
#51379=CARTESIAN_POINT('Ctrl Pts',(-12.9606229798833,-3.79748558640983,
-3.48070314321456));
#51380=CARTESIAN_POINT('Ctrl Pts',(-12.7219853147641,0.87510577925706,-5.0764535874255));
#51381=CARTESIAN_POINT('Ctrl Pts',(-12.4833476496448,4.74371336727283,-2.00832632789875));
#51382=CARTESIAN_POINT('Ctrl Pts',(-12.2447099845256,4.25414085464746,2.90490563340592));
#51383=CARTESIAN_POINT('Ctrl Pts',(-12.0060723194064,-0.143828009654572,
5.14932079538778));
#51384=CARTESIAN_POINT('Ctrl Pts',(-11.7674346542871,-4.40965812081948,
2.66291314309442));
#51385=CARTESIAN_POINT('Ctrl Pts',(-11.5287969891679,-4.6242138853148,-2.26998614379823));
#51386=CARTESIAN_POINT('Ctrl Pts',(-11.2901593240487,-0.590377013963862,
-5.11738665058224));
#51387=CARTESIAN_POINT('Ctrl Pts',(-11.0515216589295,3.98585547763773,-3.26330312131122));
#51388=CARTESIAN_POINT('Ctrl Pts',(-10.8128839938102,4.90017278133687,1.58886684880117));
#51389=CARTESIAN_POINT('Ctrl Pts',(-10.574246328691,1.31256641218918,4.98130109145864));
#51390=CARTESIAN_POINT('Ctrl Pts',(-10.3356086635718,-3.48093086466773,
3.79727684868749));
#51391=CARTESIAN_POINT('Ctrl Pts',(-10.0969709984526,-5.07640109993208,
-0.875410202580779));
#51392=CARTESIAN_POINT('Ctrl Pts',(-9.85833333333333,-2.00804185316436,
-4.74383379410727));
#51393=CARTESIAN_POINT('Ctrl Pts',(-9.61969566821411,2.90516074060913,-4.25396664554368));
#51394=CARTESIAN_POINT('Ctrl Pts',(-9.38105800309488,5.14931216104712,0.14413680399584));
#51395=CARTESIAN_POINT('Ctrl Pts',(-9.14242033797565,2.66264869981656,4.40981780253313));
#51396=CARTESIAN_POINT('Ctrl Pts',(-8.90378267285642,-2.27026344469205,
4.62407775041392));
#51397=CARTESIAN_POINT('Ctrl Pts',(-8.6651450077372,-5.11742204512421,0.590070133329444));
#51398=CARTESIAN_POINT('Ctrl Pts',(-8.42650734261798,-3.26306409156187,
-3.98605116431367));
#51399=CARTESIAN_POINT('Ctrl Pts',(-8.18786967749874,1.58916069963059,-4.90007749132113));
#51400=CARTESIAN_POINT('Ctrl Pts',(-7.94923201237953,4.98137979451584,-1.31226769103422));
#51401=CARTESIAN_POINT('Ctrl Pts',(-7.71059434726029,3.79706809731301,3.48115857359343));
#51402=CARTESIAN_POINT('Ctrl Pts',(-7.47195668214107,-0.875714622763106,
5.07634859420128));
#51403=CARTESIAN_POINT('Ctrl Pts',(-7.23331901702185,-4.74395420386913,
2.00775737117387));
#51404=CARTESIAN_POINT('Ctrl Pts',(-6.99468135190261,-4.25379242116686,
-2.90541583729795));
#51405=CARTESIAN_POINT('Ctrl Pts',(-6.7560436867834,0.144445597866564,-5.14930350831713));
#51406=CARTESIAN_POINT('Ctrl Pts',(-6.51740602166415,4.40997746829655,-2.66238424671687));
#51407=CARTESIAN_POINT('Ctrl Pts',(-6.27876835654495,4.62394159906029,2.27054073694845));
#51408=CARTESIAN_POINT('Ctrl Pts',(-6.04013069142569,0.58976325023493,5.11745742217124));
#51409=CARTESIAN_POINT('Ctrl Pts',(-5.80149302630649,-3.9862468360062,3.26282504833503));
#51410=CARTESIAN_POINT('Ctrl Pts',(-5.56285536118725,-4.89998218492935,
-1.58945454139984));
#51411=CARTESIAN_POINT('Ctrl Pts',(-5.32421769606804,-1.31196896276975,
-4.98145848607974));
#51412=CARTESIAN_POINT('Ctrl Pts',(-5.08558003094879,3.48138626541249,-3.79685931996075));
#51413=CARTESIAN_POINT('Ctrl Pts',(-4.84694236582958,5.07629607902044,0.876019016145047));
#51414=CARTESIAN_POINT('Ctrl Pts',(-4.60830470071035,2.00747286506312,4.74407464196444));
#51415=CARTESIAN_POINT('Ctrl Pts',(-4.36966703559112,-2.90567089110244,
4.25361809436949));
#51416=CARTESIAN_POINT('Ctrl Pts',(-4.1310293704719,-5.14929489932346,-0.144754224003302));
#51417=CARTESIAN_POINT('Ctrl Pts',(-3.89239170535267,-2.66211966455929,
-4.41013743913397));
#51418=CARTESIAN_POINT('Ctrl Pts',(-3.65375404023344,2.27081779171631,-4.62380481511515));
#51419=CARTESIAN_POINT('Ctrl Pts',(-3.41511637511422,5.11749322095267,-0.589457547230361));
#51420=CARTESIAN_POINT('Ctrl Pts',(-3.17647870999498,3.26258514862341,3.98644476236722));
#51421=CARTESIAN_POINT('Ctrl Pts',(-2.93784104487577,-1.58974675613189,
4.89988250604351));
#51422=CARTESIAN_POINT('Ctrl Pts',(-2.69920337975654,-4.98154027151287,
1.31167858804524));
#51423=CARTESIAN_POINT('Ctrl Pts',(-2.46056571463731,-3.79664455654379,
-3.48162998662147));
#51424=CARTESIAN_POINT('Ctrl Pts',(-2.22192804951808,0.876311943595137,
-5.07621275652709));
#51425=CARTESIAN_POINT('Ctrl Pts',(-1.98329038439886,4.74421706340335,-2.00724744484995));
#51426=CARTESIAN_POINT('Ctrl Pts',(-1.74465271927963,4.25340152698323,2.90603935147979));
#51427=CARTESIAN_POINT('Ctrl Pts',(-1.5060150541604,-0.144981805559941,
5.14906858927122));
#51428=CARTESIAN_POINT('Ctrl Pts',(-1.26737738904118,-4.41045295516259,
2.66227289179059));
#51429=CARTESIAN_POINT('Ctrl Pts',(-1.02873972392195,-4.62336931849601,
-2.27189696770677));
#51430=CARTESIAN_POINT('Ctrl Pts',(-0.790102058802722,-0.589726314329404,
-5.11598751777173));
#51431=CARTESIAN_POINT('Ctrl Pts',(-0.551464393683503,3.98775615726128,
-3.26532182704867));
#51432=CARTESIAN_POINT('Ctrl Pts',(-0.312826728564268,4.89754556132347,
1.5959172955446));
#51433=CARTESIAN_POINT('Ctrl Pts',(-0.11396200763158,1.91343850024653,4.40669134774724));
#51434=CARTESIAN_POINT('Ctrl Pts',(0.0451297691145716,-1.09341591083915,
4.39951208699472));
#51435=CARTESIAN_POINT('Ctrl Pts',(0.124675657487642,-2.40906367586066,
3.7002482568252));
#51436=CARTESIAN_POINT('Ctrl Pts',(0.164448601674178,-2.94381909922654,
3.20980646698106));
#51437=CARTESIAN_POINT('Ctrl Pts',(-29.7394486016742,-2.04298847651428,
4.16621468233147));
#51438=CARTESIAN_POINT('Ctrl Pts',(-29.6996756574876,-2.73708200495646,
3.82585174178397));
#51439=CARTESIAN_POINT('Ctrl Pts',(-29.6201297691146,-3.94131108371467,
2.79164529256157));
#51440=CARTESIAN_POINT('Ctrl Pts',(-29.4610379923684,-5.11487399530094,
-0.189162298968872));
#51441=CARTESIAN_POINT('Ctrl Pts',(-29.2621732714358,-3.48345969425087,
-4.2405579264181));
#51442=CARTESIAN_POINT('Ctrl Pts',(-29.0235356063165,1.69310326907807,-5.22361146904792));
#51443=CARTESIAN_POINT('Ctrl Pts',(-28.7848979411973,5.30517953300752,-1.39946425393815));
#51444=CARTESIAN_POINT('Ctrl Pts',(-28.546260276078,4.04784952269694,3.70627219891307));
#51445=CARTESIAN_POINT('Ctrl Pts',(-28.3076226109588,-0.930744288664083,
5.4090993768297));
#51446=CARTESIAN_POINT('Ctrl Pts',(-28.0689849458396,-5.05299176436839,
2.14132151627792));
#51447=CARTESIAN_POINT('Ctrl Pts',(-27.8303472807204,-4.53356562469179,
-3.09316579293629));
#51448=CARTESIAN_POINT('Ctrl Pts',(-27.5917096156012,0.151310267373015,
-5.48617952283658));
#51449=CARTESIAN_POINT('Ctrl Pts',(-27.3530719504819,4.69699705583506,-2.83873117311958));
#51450=CARTESIAN_POINT('Ctrl Pts',(-27.1144342853627,4.92751510715875,2.4166554194804));
#51451=CARTESIAN_POINT('Ctrl Pts',(-26.8757966202434,0.630941506851146,
5.45183698780086));
#51452=CARTESIAN_POINT('Ctrl Pts',(-26.6371589551242,-4.2452705090985,3.47824345502183));
#51453=CARTESIAN_POINT('Ctrl Pts',(-26.398521290005,-5.22124858873371,-1.69089648742445));
#51454=CARTESIAN_POINT('Ctrl Pts',(-26.1598836248858,-1.40031504429382,
-5.30656932574355));
#51455=CARTESIAN_POINT('Ctrl Pts',(-25.9212459597666,3.70712296762955,-4.0469476362654));
#51456=CARTESIAN_POINT('Ctrl Pts',(-25.6826082946473,5.40872686077514,0.930714643938138));
#51457=CARTESIAN_POINT('Ctrl Pts',(-25.4439706295281,2.14118348706817,5.05330460859686));
#51458=CARTESIAN_POINT('Ctrl Pts',(-25.2053329644089,-3.09352362053041,
4.53328402709528));
#51459=CARTESIAN_POINT('Ctrl Pts',(-24.9666952992896,-5.4861256497318,-0.151589192760673));
#51460=CARTESIAN_POINT('Ctrl Pts',(-24.7280576341705,-2.8384728348531,-4.69719336811145));
#51461=CARTESIAN_POINT('Ctrl Pts',(-24.4894199690512,2.41696306740383,-4.92735658390869));
#51462=CARTESIAN_POINT('Ctrl Pts',(-24.250782303932,5.45186847919727,-0.6306216517841));
#51463=CARTESIAN_POINT('Ctrl Pts',(-24.0121446388127,3.47799216904142,4.24548277474778));
#51464=CARTESIAN_POINT('Ctrl Pts',(-23.7735069736936,-1.69121131213625,
5.22114525709151));
#51465=CARTESIAN_POINT('Ctrl Pts',(-23.5348693085742,-5.30665239427673,
1.39999781898149));
#51466=CARTESIAN_POINT('Ctrl Pts',(-23.2962316434551,-4.04672578701207,
-3.70736617032861));
#51467=CARTESIAN_POINT('Ctrl Pts',(-23.0575939783358,0.931039236184116,
-5.40867076600343));
#51468=CARTESIAN_POINT('Ctrl Pts',(-22.8189563132166,5.05343287531637,-2.14088058820066));
#51469=CARTESIAN_POINT('Ctrl Pts',(-22.5803186480974,4.53309857247606,3.09379554087889));
#51470=CARTESIAN_POINT('Ctrl Pts',(-22.3416809829782,-0.151918219015756,
5.48611651090078));
#51471=CARTESIAN_POINT('Ctrl Pts',(-22.1030433178589,-4.69736355934995,
2.83819116837823));
#51472=CARTESIAN_POINT('Ctrl Pts',(-21.8644056527397,-4.92721164388661,
-2.41725855734347));
#51473=CARTESIAN_POINT('Ctrl Pts',(-21.6257679876205,-0.630294707996812,
-5.45190628108939));
#51474=CARTESIAN_POINT('Ctrl Pts',(-21.3871303225012,4.24569133290092,-3.47773757240369));
#51475=CARTESIAN_POINT('Ctrl Pts',(-21.1484926573821,5.22104383042178,1.69152441234305));
#51476=CARTESIAN_POINT('Ctrl Pts',(-20.9098549922628,1.39967958631079,5.3067363390701));
#51477=CARTESIAN_POINT('Ctrl Pts',(-20.6712173271436,-3.70760883745824,
4.04650345670832));
#51478=CARTESIAN_POINT('Ctrl Pts',(-20.4325796620243,-5.40861492388057,
-0.931363582024293));
#51479=CARTESIAN_POINT('Ctrl Pts',(-20.1939419969051,-2.14057753986328,
-5.05356125050234));
#51480=CARTESIAN_POINT('Ctrl Pts',(-19.9553043317859,3.09406737623519,-4.5329130355726));
#51481=CARTESIAN_POINT('Ctrl Pts',(-19.7166666666667,5.48610739082711,0.152247210345901));
#51482=CARTESIAN_POINT('Ctrl Pts',(-19.4780290015475,2.83790947164436,4.69753375160813));
#51483=CARTESIAN_POINT('Ctrl Pts',(-19.2393913364282,-2.41755402814241,
4.92706667681276));
#51484=CARTESIAN_POINT('Ctrl Pts',(-19.000753671309,-5.45194406881915,0.62996776680549));
#51485=CARTESIAN_POINT('Ctrl Pts',(-18.7621160061898,-3.4774829604232,-4.24589987831939));
#51486=CARTESIAN_POINT('Ctrl Pts',(-18.5234783410705,1.69183750498908,-5.22094238365629));
#51487=CARTESIAN_POINT('Ctrl Pts',(-18.2848406759513,5.30682026554953,-1.39936134929439));
#51488=CARTESIAN_POINT('Ctrl Pts',(-18.0462030108321,4.04628111145152,3.70785149161303));
#51489=CARTESIAN_POINT('Ctrl Pts',(-17.8075653457129,-0.931687924306101,
5.40855906212076));
#51490=CARTESIAN_POINT('Ctrl Pts',(-17.5689276805936,-5.05368960762378,
2.14027448392529));
#51491=CARTESIAN_POINT('Ctrl Pts',(-17.3302900154744,-4.53272748231129,
-3.0943392005154));
#51492=CARTESIAN_POINT('Ctrl Pts',(-17.0916523503552,0.152576201098992,
-5.4860982509981));
#51493=CARTESIAN_POINT('Ctrl Pts',(-16.8530146852359,4.6977039269886,-2.83762776471865));
#51494=CARTESIAN_POINT('Ctrl Pts',(-16.6143770201167,4.92692169201234,2.41784949025462));
#51495=CARTESIAN_POINT('Ctrl Pts',(-16.3757393549975,0.62964082335285,5.45198183693909));
#51496=CARTESIAN_POINT('Ctrl Pts',(-16.1371016898783,-4.24610840847109,
3.47722833593904));
#51497=CARTESIAN_POINT('Ctrl Pts',(-15.898464024759,-5.2208409181143,-1.69215059155202));
#51498=CARTESIAN_POINT('Ctrl Pts',(-15.6598263596398,-1.39904310724623,
-5.30690417294424));
#51499=CARTESIAN_POINT('Ctrl Pts',(-15.4211886945206,3.70809413243411,-4.04605875164388));
#51500=CARTESIAN_POINT('Ctrl Pts',(-15.1825510294014,5.40850318091069,0.932012263237568));
#51501=CARTESIAN_POINT('Ctrl Pts',(-14.9439133642821,2.13997142029063,5.05381794657124));
#51502=CARTESIAN_POINT('Ctrl Pts',(-14.7052756991629,-3.09461101366789,
4.53254191274959));
#51503=CARTESIAN_POINT('Ctrl Pts',(-14.4666380340437,-5.48608909144016,
-0.152905191303383));
#51504=CARTESIAN_POINT('Ctrl Pts',(-14.2280003689245,-2.83734604758839,
-4.69787408547534));
#51505=CARTESIAN_POINT('Ctrl Pts',(-13.9893627038052,2.41814494367183,-4.92677668949392));
#51506=CARTESIAN_POINT('Ctrl Pts',(-13.750725038686,5.45201958545282,-0.629313877635948));
#51507=CARTESIAN_POINT('Ctrl Pts',(-13.5120873735668,3.47697369895021,4.24631692335307));
#51508=CARTESIAN_POINT('Ctrl Pts',(-13.2734497084476,-1.69246367202968,
5.2207394337973));
#51509=CARTESIAN_POINT('Ctrl Pts',(-13.0348120433283,-5.30698806125446,
1.3987248601669));
#51510=CARTESIAN_POINT('Ctrl Pts',(-12.7961743782091,-4.04583637728596,
-3.70833675992024));
#51511=CARTESIAN_POINT('Ctrl Pts',(-12.5575367130899,0.932336598817344,
-5.40844728025078));
#51512=CARTESIAN_POINT('Ctrl Pts',(-12.3188990479706,5.05394626734435,-2.13966834896028));
#51513=CARTESIAN_POINT('Ctrl Pts',(-12.0802613828514,4.53235632688813,3.09488281569163));
#51514=CARTESIAN_POINT('Ctrl Pts',(-11.8416237177322,-0.153234180957902,
5.48607991215335));
#51515=CARTESIAN_POINT('Ctrl Pts',(-11.602986052613,-4.69804422706777,2.83706432025457));
#51516=CARTESIAN_POINT('Ctrl Pts',(-11.3643483874937,-4.92663166925799,
-2.41844038839298));
#51517=CARTESIAN_POINT('Ctrl Pts',(-11.1257107223745,-0.628986929655938,
-5.45205731436018));
#51518=CARTESIAN_POINT('Ctrl Pts',(-10.8870730572553,4.24652542296462,-3.47671904945761));
#51519=CARTESIAN_POINT('Ctrl Pts',(-10.6484353921361,5.22063793070565,1.69277674642096));
#51520=CARTESIAN_POINT('Ctrl Pts',(-10.4097977270168,1.39840660805754,5.30707193047986));
#51521=CARTESIAN_POINT('Ctrl Pts',(-10.1711600618976,-3.70857937407062,
4.04561398837858));
#51522=CARTESIAN_POINT('Ctrl Pts',(-9.93252239677838,-5.40839136014118,
-0.93266093104433));
#51523=CARTESIAN_POINT('Ctrl Pts',(-9.69388473165915,-2.13936526993532,
-5.05407456994261));
#51524=CARTESIAN_POINT('Ctrl Pts',(-9.45524706653993,3.09515460658571,-4.53217072472762));
#51525=CARTESIAN_POINT('Ctrl Pts',(-9.21660940142069,5.48607071313765,0.153563170061505));
#51526=CARTESIAN_POINT('Ctrl Pts',(-8.97797173630149,2.83678258271826,4.69821435176505));
#51527=CARTESIAN_POINT('Ctrl Pts',(-8.73933407118223,-2.41873582441721,
4.92648663130547));
#51528=CARTESIAN_POINT('Ctrl Pts',(-8.50069640606304,-5.45209502366077,
0.628659979413207));
#51529=CARTESIAN_POINT('Ctrl Pts',(-8.26205874094379,-3.47646438746268,
-4.24673390730354));
#51530=CARTESIAN_POINT('Ctrl Pts',(-8.02342107582457,1.69308981472579,-5.22053640884249));
#51531=CARTESIAN_POINT('Ctrl Pts',(-7.78478341070535,5.30715578061822,-1.398088350914));
#51532=CARTESIAN_POINT('Ctrl Pts',(-7.54614574558612,4.04539158492623,3.70882197487425));
#51533=CARTESIAN_POINT('Ctrl Pts',(-7.30750808046689,-0.932985259924489,
5.40833542060147));
#51534=CARTESIAN_POINT('Ctrl Pts',(-7.06887041534766,-5.05420285435175,
2.13906218317974));
#51535=CARTESIAN_POINT('Ctrl Pts',(-6.83023275022844,-4.53198510629524,
-3.09542638627781));
#51536=CARTESIAN_POINT('Ctrl Pts',(-6.5915950851092,0.153892158663785,-5.48606149452997));
#51537=CARTESIAN_POINT('Ctrl Pts',(-6.35295741998999,4.69838445946899,-2.83650083471779));
#51538=CARTESIAN_POINT('Ctrl Pts',(-6.11431975487076,4.92634157582419,2.41903125123913));
#51539=CARTESIAN_POINT('Ctrl Pts',(-5.87568208975152,0.628333026549508,
5.45213271432227));
#51540=CARTESIAN_POINT('Ctrl Pts',(-5.63704442463231,-4.24694237567916,
3.47620971110884));
#51541=CARTESIAN_POINT('Ctrl Pts',(-5.39840675951308,-5.22043486953231,
-1.69340287337793));
#51542=CARTESIAN_POINT('Ctrl Pts',(-5.15976909439385,-1.39777008619599,
-5.30723961851162));
#51543=CARTESIAN_POINT('Ctrl Pts',(-4.92113142927462,3.70906455745249,-4.04516915379718));
#51544=CARTESIAN_POINT('Ctrl Pts',(-4.6824937641554,5.40827947099373,0.933309560251545));
#51545=CARTESIAN_POINT('Ctrl Pts',(-4.44385609903617,2.13875907072644,5.05433116894732));
#51546=CARTESIAN_POINT('Ctrl Pts',(-4.20521843391694,-3.09569812028096,
4.53179937874414));
#51547=CARTESIAN_POINT('Ctrl Pts',(-3.96658076879772,-5.48605232251892,
-0.154220968562498));
#51548=CARTESIAN_POINT('Ctrl Pts',(-3.72794310367849,-2.83621894921919,
-4.69855489219838));
#51549=CARTESIAN_POINT('Ctrl Pts',(-3.48930543855926,2.41932642504106,-4.92619584638074));
#51550=CARTESIAN_POINT('Ctrl Pts',(-3.25066777344004,5.45217085429907,-0.62800733095214));
#51551=CARTESIAN_POINT('Ctrl Pts',(-3.01203010832081,3.47595412225719,4.24715324617577));
#51552=CARTESIAN_POINT('Ctrl Pts',(-2.77339244320158,-1.69371419858668,
5.22032867177245));
#51553=CARTESIAN_POINT('Ctrl Pts',(-2.53475477808237,-5.30732675260943,
1.39746072132896));
#51554=CARTESIAN_POINT('Ctrl Pts',(-2.29611711296313,-4.04494034512231,
-3.70932421772263));
#51555=CARTESIAN_POINT('Ctrl Pts',(-2.05747944784391,0.933621644789192,
-5.40819069931389));
#51556=CARTESIAN_POINT('Ctrl Pts',(-1.81884178272468,5.05448290456958,-2.13851890831426));
#51557=CARTESIAN_POINT('Ctrl Pts',(-1.58020411760545,4.53156864812263,3.09609067750451));
#51558=CARTESIAN_POINT('Ctrl Pts',(-1.34156645248623,-0.154463433667277,
5.48581121207333));
#51559=CARTESIAN_POINT('Ctrl Pts',(-1.102928787367,-4.69889104257927,2.83638219731909));
#51560=CARTESIAN_POINT('Ctrl Pts',(-0.86429112224777,-4.92573186882932,
-2.42047617778675));
#51561=CARTESIAN_POINT('Ctrl Pts',(-0.625653457128544,-0.628293675082119,
-5.45056668002));
#51562=CARTESIAN_POINT('Ctrl Pts',(-0.387015792009324,4.24855040464988,
-3.47886977601648));
#51563=CARTESIAN_POINT('Ctrl Pts',(-0.14837812689009,5.21783889380097,1.70028828353193));
#51564=CARTESIAN_POINT('Ctrl Pts',(0.0504865940425981,2.03857497647958,
4.69488343076037));
#51565=CARTESIAN_POINT('Ctrl Pts',(0.209578370788749,-1.16492393898944,
4.68723465536585));
#51566=CARTESIAN_POINT('Ctrl Pts',(0.28912425916182,-2.56661341648691,3.94223984839548));
#51567=CARTESIAN_POINT('Ctrl Pts',(0.328897203348356,-3.13634117333406,
3.41972378108145));
#51568=CARTESIAN_POINT('Ctrl Pts',(-29.575,-2.16839587231048,4.42195480991686));
#51569=CARTESIAN_POINT('Ctrl Pts',(-29.5352270558135,-2.90509583874368,
4.06069893214025));
#51570=CARTESIAN_POINT('Ctrl Pts',(-29.4556811674404,-4.18324566372502,
2.96300845498348));
#51571=CARTESIAN_POINT('Ctrl Pts',(-29.2965893906942,-5.42884690065524,
-0.200773892264263));
#51572=CARTESIAN_POINT('Ctrl Pts',(-29.0977246697616,-3.69728939208772,
-4.50086156121024));
#51573=CARTESIAN_POINT('Ctrl Pts',(-28.8590870046423,1.79703321005912,-5.54425914695472));
#51574=CARTESIAN_POINT('Ctrl Pts',(-28.6204493395231,5.63083420855472,-1.48536937264729));
#51575=CARTESIAN_POINT('Ctrl Pts',(-28.3818116744038,4.2963238890735,3.93377908400849));
#51576=CARTESIAN_POINT('Ctrl Pts',(-28.1431740092847,-0.987877365397176,
5.74113309814008));
#51577=CARTESIAN_POINT('Ctrl Pts',(-27.9045363441654,-5.36316607295304,
2.27276501584044));
#51578=CARTESIAN_POINT('Ctrl Pts',(-27.6658986790462,-4.81185532881875,
-3.28303757700034));
#51579=CARTESIAN_POINT('Ctrl Pts',(-27.4272610139269,0.160598340608156,
-5.82294475413315));
#51580=CARTESIAN_POINT('Ctrl Pts',(-27.1886233488077,4.98531888222138,-3.01298466885832));
#51581=CARTESIAN_POINT('Ctrl Pts',(-26.9499856836885,5.22998712030967,2.56500009502694));
#51582=CARTESIAN_POINT('Ctrl Pts',(-26.7113480185693,0.669671402875337,
5.78649412698952));
#51583=CARTESIAN_POINT('Ctrl Pts',(-26.4727103534501,-4.50586342242951,
3.69175295772048));
#51584=CARTESIAN_POINT('Ctrl Pts',(-26.2340726883308,-5.54175122291158,
-1.79469096668193));
#51585=CARTESIAN_POINT('Ctrl Pts',(-25.9954350232117,-1.48627238816434,
-5.6323093127302));
#51586=CARTESIAN_POINT('Ctrl Pts',(-25.7567973580923,3.93468207655805,-4.29536664098428));
#51587=CARTESIAN_POINT('Ctrl Pts',(-25.5181596929732,5.74073771545223,0.987845900950795));
#51588=CARTESIAN_POINT('Ctrl Pts',(-25.2795220278539,2.27261851380574,5.36349812090215));
#51589=CARTESIAN_POINT('Ctrl Pts',(-25.0408843627347,-3.28341736958705,
4.8115564455539));
#51590=CARTESIAN_POINT('Ctrl Pts',(-24.8022466976155,-5.82288757406612,
-0.160894387632515));
#51591=CARTESIAN_POINT('Ctrl Pts',(-24.5636090324963,-3.01271047268094,
-4.98552724498736));
#51592=CARTESIAN_POINT('Ctrl Pts',(-24.324971367377,2.56532662769952,-5.22981886622255));
#51593=CARTESIAN_POINT('Ctrl Pts',(-24.0863337022578,5.78652755146292,-0.669331913732308));
#51594=CARTESIAN_POINT('Ctrl Pts',(-23.8476960371386,3.69148624672874,4.50608871785483));
#51595=CARTESIAN_POINT('Ctrl Pts',(-23.6090583720193,-1.79502511668494,
5.54164154832996));
#51596=CARTESIAN_POINT('Ctrl Pts',(-23.3704207069001,-5.63239748036626,
1.48593569020165));
#51597=CARTESIAN_POINT('Ctrl Pts',(-23.1317830417809,-4.29513117367219,
-3.93494020808196));
#51598=CARTESIAN_POINT('Ctrl Pts',(-22.8931453766617,0.988190418061122,
-5.74067817734282));
#51599=CARTESIAN_POINT('Ctrl Pts',(-22.6545077115424,5.36363426118309,-2.27229702170649));
#51600=CARTESIAN_POINT('Ctrl Pts',(-22.4158700464232,4.81135960693467,3.28370598157288));
#51601=CARTESIAN_POINT('Ctrl Pts',(-22.177232381304,-0.161243610930449,
5.82287787425445));
#51602=CARTESIAN_POINT('Ctrl Pts',(-21.9385947161848,-4.98570788329408,
3.01241151630967));
#51603=CARTESIAN_POINT('Ctrl Pts',(-21.6999570510655,-5.22966502916022,
-2.56564025607911));
#51604=CARTESIAN_POINT('Ctrl Pts',(-21.4613193859463,-0.668984900732974,
-5.78656767379734));
#51605=CARTESIAN_POINT('Ctrl Pts',(-21.2226817208271,4.50631007820199,-3.69121602185732));
#51606=CARTESIAN_POINT('Ctrl Pts',(-20.9840440557079,5.54153389565618,1.79535743632542));
#51607=CARTESIAN_POINT('Ctrl Pts',(-20.7454063905886,1.4855979230446,5.63248657805113));
#51608=CARTESIAN_POINT('Ctrl Pts',(-20.5067687254694,-3.93519777116089,
4.29489519578073));
#51609=CARTESIAN_POINT('Ctrl Pts',(-20.2681310603502,-5.74061890739093,
-0.988534673640199));
#51610=CARTESIAN_POINT('Ctrl Pts',(-20.0294933952309,-2.27197537096228,
-5.36377051658862));
#51611=CARTESIAN_POINT('Ctrl Pts',(-19.7908557301117,3.28399450334934,-4.81116268098024));
#51612=CARTESIAN_POINT('Ctrl Pts',(-19.5522180649925,5.82286819435154,0.161592797159601));
#51613=CARTESIAN_POINT('Ctrl Pts',(-19.3135803998733,3.01211252782197,4.98588852268307));
#51614=CARTESIAN_POINT('Ctrl Pts',(-19.074942734754,-2.56595386414308,5.22951116338557));
#51615=CARTESIAN_POINT('Ctrl Pts',(-18.8363050696348,-5.78660778110002,
0.668637890488963));
#51616=CARTESIAN_POINT('Ctrl Pts',(-18.5976674045156,-3.69094578070135,
-4.50653142503277));
#51617=CARTESIAN_POINT('Ctrl Pts',(-18.3590297393963,1.79568974794104,-5.54142622165309));
#51618=CARTESIAN_POINT('Ctrl Pts',(-18.1203920742771,5.63257565629784,-1.48526015127511));
#51619=CARTESIAN_POINT('Ctrl Pts',(-17.8817544091579,4.29465920201836,3.93545532046853));
#51620=CARTESIAN_POINT('Ctrl Pts',(-17.6431167440387,-0.988878925442489,
5.74055961659669));
#51621=CARTESIAN_POINT('Ctrl Pts',(-17.4044790789195,-5.36390675282074,
2.2716537121509));
#51622=CARTESIAN_POINT('Ctrl Pts',(-17.1658414138002,-4.81096573766385,
-3.28428301336982));
#51623=CARTESIAN_POINT('Ctrl Pts',(-16.927203748681,0.161941982776275,-5.82285849348062));
#51624=CARTESIAN_POINT('Ctrl Pts',(-16.6885660835618,4.98606914415835,-3.01181352851682));
#51625=CARTESIAN_POINT('Ctrl Pts',(-16.4499284184425,5.22935727879621,2.56626746298708));
#51626=CARTESIAN_POINT('Ctrl Pts',(-16.2112907533233,0.668290877844823,
5.78664786758917));
#51627=CARTESIAN_POINT('Ctrl Pts',(-15.9726530882041,-4.50675275565964,
3.69067552627418));
#51628=CARTESIAN_POINT('Ctrl Pts',(-15.7340154230849,-5.5413185277209,-1.79602205310015));
#51629=CARTESIAN_POINT('Ctrl Pts',(-15.4953777579656,-1.48492237416498,
-5.63266471428835));
#51630=CARTESIAN_POINT('Ctrl Pts',(-15.2567400928464,3.93571285562398,-4.29442319281195));
#51631=CARTESIAN_POINT('Ctrl Pts',(-15.0181024277272,5.74050030515826,0.989223173688781));
#51632=CARTESIAN_POINT('Ctrl Pts',(-14.779464762608,2.2713320451704,5.36404296976328));
#51633=CARTESIAN_POINT('Ctrl Pts',(-14.5408270974887,-3.28457151157951,
4.81076877704648));
#51634=CARTESIAN_POINT('Ctrl Pts',(-14.3021894323695,-5.82284877166972,
-0.16229116781057));
#51635=CARTESIAN_POINT('Ctrl Pts',(-14.0635517672503,-3.01151451838073,
-4.98624974770287));
#51636=CARTESIAN_POINT('Ctrl Pts',(-13.824914102131,2.56658105260234,-5.22920337540123));
#51637=CARTESIAN_POINT('Ctrl Pts',(-13.5862764370118,5.78668793326858,-0.667943862797434));
#51638=CARTESIAN_POINT('Ctrl Pts',(-13.3476387718926,3.69040525857474,4.50697407007948));
#51639=CARTESIAN_POINT('Ctrl Pts',(-13.1090011067734,-1.79635435180044,
5.54121081386123));
#51640=CARTESIAN_POINT('Ctrl Pts',(-12.8703634416541,-5.63275375202288,
1.48458459171485));
#51641=CARTESIAN_POINT('Ctrl Pts',(-12.6317257765349,-4.29418716816209,
-3.93597037662593));
#51642=CARTESIAN_POINT('Ctrl Pts',(-12.3930881114157,0.989567418377627,
-5.74044097307606));
#51643=CARTESIAN_POINT('Ctrl Pts',(-12.1544504462965,5.36417916741587,-2.27101037002181));
#51644=CARTESIAN_POINT('Ctrl Pts',(-11.9158127811772,4.81057179912879,3.28485999797732));
#51645=CARTESIAN_POINT('Ctrl Pts',(-11.677175116058,-0.162640352261234,
5.82283902891891));
#51646=CARTESIAN_POINT('Ctrl Pts',(-11.4385374509388,-4.98643033331604,
3.01121549741473));
#51647=CARTESIAN_POINT('Ctrl Pts',(-11.1998997858196,-5.22904945320118,
-2.56689463298775));
#51648=CARTESIAN_POINT('Ctrl Pts',(-10.9612621207004,-0.667596845348008,
-5.78672797813811));
#51649=CARTESIAN_POINT('Ctrl Pts',(-10.7226244555811,4.50719536829151,-3.69013497760401));
#51650=CARTESIAN_POINT('Ctrl Pts',(-10.4839867904619,5.54110308007444,1.79668664404075));
#51651=CARTESIAN_POINT('Ctrl Pts',(-10.2453491253427,1.48424680392591,5.63284276950108));
#51652=CARTESIAN_POINT('Ctrl Pts',(-10.0067114602234,-3.93622788347351,
4.29395112806967));
#51653=CARTESIAN_POINT('Ctrl Pts',(-9.7680737951042,-5.74038162035028,-0.989911659507881));
#51654=CARTESIAN_POINT('Ctrl Pts',(-9.52943612998498,-2.27068868670629,
-5.36431534577795));
#51655=CARTESIAN_POINT('Ctrl Pts',(-9.29079846486575,3.2851484725623,-4.81037480391155));
#51656=CARTESIAN_POINT('Ctrl Pts',(-9.05216079974653,5.82282926522816,0.162989536127165));
#51657=CARTESIAN_POINT('Ctrl Pts',(-8.81352313462729,3.01091646561997,4.98661090099698));
#51658=CARTESIAN_POINT('Ctrl Pts',(-8.57488546950808,-2.56720820414237,
5.22889551219701));
#51659=CARTESIAN_POINT('Ctrl Pts',(-8.33624780438884,-5.78676800219732,
0.667249825496974));
#51660=CARTESIAN_POINT('Ctrl Pts',(-8.09761013926962,-3.6898646833635,-4.50741665029341));
#51661=CARTESIAN_POINT('Ctrl Pts',(-7.85897247415039,1.79701892982099,-5.54099532636385));
#51662=CARTESIAN_POINT('Ctrl Pts',(-7.62033480903117,5.6329317667206,-1.48390901079377));
#51663=CARTESIAN_POINT('Ctrl Pts',(-7.38169714391194,4.29371507253944,3.93648537615507));
#51664=CARTESIAN_POINT('Ctrl Pts',(-7.14305947879271,-0.990255897085868,
5.74032224700168));
#51665=CARTESIAN_POINT('Ctrl Pts',(-6.90442181367349,-5.36445150483438,
2.27036699518559));
#51666=CARTESIAN_POINT('Ctrl Pts',(-6.66578414855427,-4.81017779142361,
-3.28543693525765));
#51667=CARTESIAN_POINT('Ctrl Pts',(-6.42714648343502,0.163338719461003,
-5.82281948074281));
#51668=CARTESIAN_POINT('Ctrl Pts',(-6.18850881831581,4.98679145064144,-3.0106174227187));
#51669=CARTESIAN_POINT('Ctrl Pts',(-5.94987115319658,5.2287415525881,2.56752176552981));
#51670=CARTESIAN_POINT('Ctrl Pts',(-5.71123348807735,0.666902802864079,
5.78680800647329));
#51671=CARTESIAN_POINT('Ctrl Pts',(-5.47259582295812,-4.50763791535213,
3.68959437388266));
#51672=CARTESIAN_POINT('Ctrl Pts',(-5.2339581578389,-5.54088755413527,-1.79735120535602));
#51673=CARTESIAN_POINT('Ctrl Pts',(-4.99532049271967,-1.48357120962223,
-5.63302075094351));
#51674=CARTESIAN_POINT('Ctrl Pts',(-4.75668282760044,3.93674284949249,-4.29347898763361));
#51675=CARTESIAN_POINT('Ctrl Pts',(-4.51804516248123,5.74026286296703,0.990600104358038));
#51676=CARTESIAN_POINT('Ctrl Pts',(-4.27940749736199,2.27004527638976,5.36458769593022));
#51677=CARTESIAN_POINT('Ctrl Pts',(-4.04076983224277,-3.28572534945949,
4.80998066311877));
#51678=CARTESIAN_POINT('Ctrl Pts',(-3.80213216712354,-5.82280974571438,
-0.16368771312168));
#51679=CARTESIAN_POINT('Ctrl Pts',(-3.56349450200431,-3.0103182338791,-4.98697234526281));
#51680=CARTESIAN_POINT('Ctrl Pts',(-3.32485683688509,2.56783505836581,-5.22858687764632));
#51681=CARTESIAN_POINT('Ctrl Pts',(-3.08621917176586,5.78684848764546,-0.666557114673928));
#51682=CARTESIAN_POINT('Ctrl Pts',(-2.84758150664664,3.68932309589099,4.50786172998432));
#51683=CARTESIAN_POINT('Ctrl Pts',(-2.60894384152741,-1.79768164104147,
5.54077483750139));
#51684=CARTESIAN_POINT('Ctrl Pts',(-2.37030617640819,-5.63311323370599,
1.48324285461269));
#51685=CARTESIAN_POINT('Ctrl Pts',(-2.13166851128895,-4.29323613370083,
-3.93701844882378));
#51686=CARTESIAN_POINT('Ctrl Pts',(-1.89303084616973,0.990931345983249,
-5.7401686421007));
#51687=CARTESIAN_POINT('Ctrl Pts',(-1.65439318105051,5.36474874573582,-2.26979037177858));
#51688=CARTESIAN_POINT('Ctrl Pts',(-1.41575551593128,4.80973576926203,3.28614200352924));
#51689=CARTESIAN_POINT('Ctrl Pts',(-1.17711785081205,-0.163945061774615,
5.82255383487542));
#51690=CARTESIAN_POINT('Ctrl Pts',(-0.938480185692826,-4.98732912999593,
3.0104915028476));
#51691=CARTESIAN_POINT('Ctrl Pts',(-0.699842520573593,-5.22809441916263,
-2.56905538786673));
#51692=CARTESIAN_POINT('Ctrl Pts',(-0.461204855454365,-0.666861035834833,
-5.78514584226827));
#51693=CARTESIAN_POINT('Ctrl Pts',(-0.222567190335147,4.50934465203849,
-3.6924177249843));
#51694=CARTESIAN_POINT('Ctrl Pts',(0.016070474784088,5.53813222627847,1.80465927151925));
#51695=CARTESIAN_POINT('Ctrl Pts',(0.214935195716776,2.16371145271264,4.98307551377353));
#51696=CARTESIAN_POINT('Ctrl Pts',(0.374026972462927,-1.23643196713973,
4.97495722373696));
#51697=CARTESIAN_POINT('Ctrl Pts',(0.453572860835998,-2.72416315711316,
4.18423143996577));
#51698=CARTESIAN_POINT('Ctrl Pts',(0.493345805022534,-3.32886324744157,
3.62964109518183));
#51699=CARTESIAN_POINT('',(0.,4.77615934004779,1.20163511869213));
#51700=CARTESIAN_POINT('Ctrl Pts',(1.27675647831893E-15,4.78202092340378,
1.20708649626074));
#51701=CARTESIAN_POINT('Ctrl Pts',(1.54554986213376E-15,4.74680432306751,
1.31141193121661));
#51702=CARTESIAN_POINT('Ctrl Pts',(-1.2200289887242E-15,4.70790283853999,
1.41429721113204));
#51703=CARTESIAN_POINT('Ctrl Pts',(-1.0547118733939E-15,4.66526667899838,
1.51554882908261));
#51704=CARTESIAN_POINT('Ctrl Pts',(-8.36120983837436E-16,4.60951044466766,
1.64795777485803));
#51705=CARTESIAN_POINT('Ctrl Pts',(1.7406482083505E-15,4.5473685300075,
1.77757428418243));
#51706=CARTESIAN_POINT('Ctrl Pts',(9.99200722162641E-16,4.47921304648044,
1.90412989878513));
#51707=CARTESIAN_POINT('Ctrl Pts',(5.41776053129587E-16,4.43716556493129,
1.98220644662206));
#51708=CARTESIAN_POINT('Ctrl Pts',(-6.14882986343895E-16,4.39282838373583,
2.05911740148693));
#51709=CARTESIAN_POINT('Ctrl Pts',(-5.55111512312578E-16,4.34628172346416,
2.13479307691151));
#51710=CARTESIAN_POINT('Ctrl Pts',(-5.12735502418862E-16,4.31328167171442,
2.18844464268728));
#51711=CARTESIAN_POINT('Ctrl Pts',(7.5446052363616E-15,4.27917094813153,
2.24147520753853));
#51712=CARTESIAN_POINT('Ctrl Pts',(7.32747196252603E-15,4.24397679643589,
2.29385817644388));
#51713=CARTESIAN_POINT('Ctrl Pts',(7.25033478916171E-15,4.23147398038747,
2.31246736554886));
#51714=CARTESIAN_POINT('Ctrl Pts',(1.1248375135418E-15,4.21883292816165,
2.33099695996549));
#51715=CARTESIAN_POINT('Ctrl Pts',(9.43689570931383E-16,4.20605981758978,
2.34943854375472));
#51716=CARTESIAN_POINT('Ctrl Pts',(-2.0749684309091E-16,4.12488731768033,
2.46663391680332));
#51717=CARTESIAN_POINT('Ctrl Pts',(1.20832359191774E-15,4.03848405238999,
2.58013740696103));
#51718=CARTESIAN_POINT('Ctrl Pts',(2.72004641033163E-15,3.94721695353052,
2.68968900864157));
#51719=CARTESIAN_POINT('Ctrl Pts',(4.18855970728122E-15,3.85855853902716,
2.79610930064906));
#51720=CARTESIAN_POINT('Ctrl Pts',(1.88596569557423E-15,3.7653095628778,
2.89880063696627));
#51721=CARTESIAN_POINT('Ctrl Pts',(-4.9960036108132E-16,3.66777702457831,
2.99748899318237));
#51722=CARTESIAN_POINT('Ctrl Pts',(-2.58697066065493E-15,3.58243605356626,
3.08384130487147));
#51723=CARTESIAN_POINT('Ctrl Pts',(-1.9993502333868E-15,3.49381479608703,
3.16712847527816));
#51724=CARTESIAN_POINT('Ctrl Pts',(-3.60822483003176E-15,3.40210641955682,
3.24714114973565));
#51725=CARTESIAN_POINT('Ctrl Pts',(-3.93090312754506E-15,3.38371325027676,
3.26318861150008));
#51726=CARTESIAN_POINT('Ctrl Pts',(-8.00198331154243E-15,3.36519389765555,
3.27910584403603));
#51727=CARTESIAN_POINT('Ctrl Pts',(-7.93809462606987E-15,3.34656787360052,
3.29487610387643));
#51728=CARTESIAN_POINT('Ctrl Pts',(-7.56940933970987E-15,3.23908184596226,
3.38588224560911));
#51729=CARTESIAN_POINT('Ctrl Pts',(9.69472795872832E-15,3.12792305846971,
3.4721065544235));
#51730=CARTESIAN_POINT('Ctrl Pts',(8.60422844084496E-15,3.01343370374636,
3.55329630674216));
#51731=CARTESIAN_POINT('Ctrl Pts',(7.5193745599244E-15,2.89953707311163,
3.63406573070746));
#51732=CARTESIAN_POINT('Ctrl Pts',(1.54891535256133E-14,2.78234353560187,
3.70985298607676));
#51733=CARTESIAN_POINT('Ctrl Pts',(1.29340982368831E-14,2.66216592270983,
3.78036399292217));
#51734=CARTESIAN_POINT('Ctrl Pts',(1.04428067996356E-14,2.54498745723108,
3.84911533006954));
#51735=CARTESIAN_POINT('Ctrl Pts',(9.06092894879522E-15,2.42497131537325,
3.91285066923259));
#51736=CARTESIAN_POINT('Ctrl Pts',(1.10467190950203E-14,2.30239503897639,
3.9712502394403));
#51737=CARTESIAN_POINT('Ctrl Pts',(1.25360617046891E-14,2.21046283167875,
4.01504991709609));
#51738=CARTESIAN_POINT('Ctrl Pts',(1.14694130650435E-14,2.11709024431302,
4.05584730347416));
#51739=CARTESIAN_POINT('Ctrl Pts',(1.04916075827077E-14,2.02239293435179,
4.09348836738669));
#51740=CARTESIAN_POINT('Ctrl Pts',(1.01019433215215E-14,1.98465520635888,
4.10848866921022));
#51741=CARTESIAN_POINT('Ctrl Pts',(1.58900622876451E-14,1.94670710034945,
4.12298752598548));
#51742=CARTESIAN_POINT('Ctrl Pts',(1.63757896132211E-14,1.90855596787325,
4.1369744095719));
#51743=CARTESIAN_POINT('Ctrl Pts',(1.66667902990066E-14,1.8856995109076,
4.14535399313934));
#51744=CARTESIAN_POINT('Ctrl Pts',(-3.74501732116749E-15,1.8627701834264,
4.15354980834729));
#51745=CARTESIAN_POINT('Ctrl Pts',(-4.38538094726937E-15,1.83976957424201,
4.16155951178909));
#51746=CARTESIAN_POINT('Ctrl Pts',(-4.90190327326717E-15,1.8212171023791,
4.16802020144052));
#51747=CARTESIAN_POINT('Ctrl Pts',(9.50430379515547E-15,1.80262497700585,
4.17435742449665));
#51748=CARTESIAN_POINT('Ctrl Pts',(9.38138455808257E-15,1.784001553863,
4.18056782352897));
#51749=CARTESIAN_POINT('Ctrl Pts',(8.54497039802425E-15,1.65727692396478,
4.22282699966724));
#51750=CARTESIAN_POINT('Ctrl Pts',(7.75693411885647E-15,1.52899676754921,
4.25925543233605));
#51751=CARTESIAN_POINT('Ctrl Pts',(7.66053886991358E-15,1.39943774817802,
4.28958765120325));
#51752=CARTESIAN_POINT('Ctrl Pts',(7.59729281300995E-15,1.31443255133079,
4.30948897685494));
#51753=CARTESIAN_POINT('Ctrl Pts',(1.2113674912629E-15,1.2288765362281,
4.32676501145738));
#51754=CARTESIAN_POINT('Ctrl Pts',(1.0547118733939E-15,1.14284625117365,
4.34132862407617));
#51755=CARTESIAN_POINT('Ctrl Pts',(8.68428161696615E-16,1.01006019941622,
4.36380727351629));
#51756=CARTESIAN_POINT('Ctrl Pts',(4.15203095003235E-15,0.876143569520156,
4.37982636972409));
#51757=CARTESIAN_POINT('Ctrl Pts',(4.94049245958195E-15,0.741565045486008,
4.38948206088079));
#51758=CARTESIAN_POINT('Ctrl Pts',(5.72761812915067E-15,0.607214529250332,
4.39912139301662));
#51759=CARTESIAN_POINT('Ctrl Pts',(1.10432148395374E-14,0.472203479324102,
4.40241856966672));
#51760=CARTESIAN_POINT('Ctrl Pts',(1.14075415780235E-14,0.337013667456073,
4.39942001130783));
#51761=CARTESIAN_POINT('Ctrl Pts',(1.15826238267446E-14,0.272046335208114,
4.39797901265212));
#51762=CARTESIAN_POINT('Ctrl Pts',(9.92588300807085E-15,0.207038030887552,
4.39508336506645));
#51763=CARTESIAN_POINT('Ctrl Pts',(1.02695629777827E-14,0.142044407157708,
4.39073446593813));
#51764=CARTESIAN_POINT('Ctrl Pts',(1.03617903745677E-14,0.124603202396043,
4.38956742776066));
#51765=CARTESIAN_POINT('Ctrl Pts',(4.4841957176862E-15,0.107164810159224,
4.38829579344102));
#51766=CARTESIAN_POINT('Ctrl Pts',(4.69069227904129E-15,0.0897419980454403,
4.38692068583962));
#51767=CARTESIAN_POINT('Ctrl Pts',(6.25118297356027E-15,-0.0419218708223804,
4.37652902313169));
#51768=CARTESIAN_POINT('Ctrl Pts',(-5.49571088697169E-16,-0.17288184694056,
4.36022055581769));
#51769=CARTESIAN_POINT('Ctrl Pts',(8.60422844084496E-16,-0.302702434116573,
4.33812072407467));
#51770=CARTESIAN_POINT('Ctrl Pts',(2.26456079903569E-15,-0.431983851255918,
4.31611267721224));
#51771=CARTESIAN_POINT('Ctrl Pts',(1.75511797657805E-14,-0.560136154997887,
4.28836093293126));
#51772=CARTESIAN_POINT('Ctrl Pts',(1.48214773787458E-14,-0.686713620784949,
4.25494071804226));
#51773=CARTESIAN_POINT('Ctrl Pts',(1.23397585715295E-14,-0.80179198203985,
4.22455660868837));
#51774=CARTESIAN_POINT('Ctrl Pts',(-2.35332166972068E-15,-0.915568901399882,
4.18948643033132));
#51775=CARTESIAN_POINT('Ctrl Pts',(-5.99520433297585E-15,-1.02768958167645,
4.14975498030284));
#51776=CARTESIAN_POINT('Ctrl Pts',(-8.67136215211543E-15,-1.11007901125274,
4.12055919326328));
#51777=CARTESIAN_POINT('Ctrl Pts',(6.0234625807556E-15,-1.19157368030025,
4.08884575090022));
#51778=CARTESIAN_POINT('Ctrl Pts',(4.84334794492725E-15,-1.27206424811892,
4.05464924064616));
#51779=CARTESIAN_POINT('Ctrl Pts',(4.19130181297638E-15,-1.31653752369003,
4.03575471840195));
#51780=CARTESIAN_POINT('Ctrl Pts',(7.59797375755575E-15,-1.36070412856013,
4.01610202232593));
#51781=CARTESIAN_POINT('Ctrl Pts',(7.70217223333702E-15,-1.40454455699869,
3.99569611765175));
#51782=CARTESIAN_POINT('Ctrl Pts',(7.75609059491098E-15,-1.42723014864851,
3.98513691380336));
#51783=CARTESIAN_POINT('Ctrl Pts',(-7.46205461605755E-15,-1.44982838930905,
3.97437601887541));
#51784=CARTESIAN_POINT('Ctrl Pts',(-8.10462807976364E-15,-1.47233648956831,
3.96341406098191));
#51785=CARTESIAN_POINT('Ctrl Pts',(-8.59111957832261E-15,-1.48937734177172,
3.95511477751635));
#51786=CARTESIAN_POINT('Ctrl Pts',(5.51713801836789E-15,-1.50635977342605,
3.94670349607368));
#51787=CARTESIAN_POINT('Ctrl Pts',(5.68989300120393E-15,-1.52327621904144,
3.93818410740871));
#51788=CARTESIAN_POINT('Ctrl Pts',(6.8760654734775E-15,-1.63942813424693,
3.87968817201454));
#51789=CARTESIAN_POINT('Ctrl Pts',(4.1445617132442E-15,-1.75256979369442,
3.81605162100472));
#51790=CARTESIAN_POINT('Ctrl Pts',(4.69069227904129E-15,-1.8623899266764,
3.74745962400277));
#51791=CARTESIAN_POINT('Ctrl Pts',(5.22545435247209E-15,-1.96992399580907,
3.68029546796622));
#51792=CARTESIAN_POINT('Ctrl Pts',(5.0249819177936E-15,-2.07427385910768,
3.60837941731036));
#51793=CARTESIAN_POINT('Ctrl Pts',(6.27276008913213E-15,-2.17511326369545,
3.53184659443599));
#51794=CARTESIAN_POINT('Ctrl Pts',(7.56032798375268E-15,-2.27916828152011,
3.45287325776349));
#51795=CARTESIAN_POINT('Ctrl Pts',(-5.02292661063484E-15,-2.37948625932775,
3.36898369722969));
#51796=CARTESIAN_POINT('Ctrl Pts',(-4.60395610524245E-15,-2.47566144275777,
3.28029126749575));
#51797=CARTESIAN_POINT('Ctrl Pts',(-4.21077948966132E-15,-2.56591560775799,
3.19705918098456));
#51798=CARTESIAN_POINT('Ctrl Pts',(5.23948052523968E-15,-2.65252139743486,
3.10959674386589));
#51799=CARTESIAN_POINT('Ctrl Pts',(5.31345800691696E-15,-2.73509733308257,
3.0179750570285));
#51800=CARTESIAN_POINT('Ctrl Pts',(5.31831121266542E-15,-2.74051463029901,
3.01196432393565));
#51801=CARTESIAN_POINT('Ctrl Pts',(2.3894388675905E-18,-2.74591456605251,
3.00593568341939));
#51802=CARTESIAN_POINT('Ctrl Pts',(-1.38777878078145E-17,-2.75129702511903,
2.99988915288068));
#51803=CARTESIAN_POINT('Ctrl Pts',(-0.808841525903593,-4.91703434725887,
-0.0013692803956027));
#51804=CARTESIAN_POINT('Ctrl Pts',(-0.772508524126926,-4.91859034973346,
-0.753815327274128));
#51805=CARTESIAN_POINT('Ctrl Pts',(-0.73617552235026,-4.75666071795644,
-1.50557039925234));
#51806=CARTESIAN_POINT('Ctrl Pts',(-0.699842520573593,-4.42776130708021,
-2.1751459818146));
#51807=CARTESIAN_POINT('Ctrl Pts',(-0.620296632200516,-3.70768329138669,
-3.64108553933391));
#51808=CARTESIAN_POINT('Ctrl Pts',(-0.540750743827439,-2.18727216361073,
-4.71311569080111));
#51809=CARTESIAN_POINT('Ctrl Pts',(-0.461204855454364,-0.564365651743867,
-4.90034274698736));
#51810=CARTESIAN_POINT('Ctrl Pts',(-0.381658967081291,1.05854086012297,
-5.08756980317361));
#51811=CARTESIAN_POINT('Ctrl Pts',(-0.302113078708221,2.78394275608069,
-4.38999376407897));
#51812=CARTESIAN_POINT('Ctrl Pts',(-0.222567190335146,3.81810829976624,
-3.12502624511441));
#51813=CARTESIAN_POINT('Ctrl Pts',(-0.148378126890099,4.78263047309757,
-1.94524489575994));
#51814=CARTESIAN_POINT('Ctrl Pts',(-0.0741890634450472,5.14588079318518,
-0.271918139693744));
#51815=CARTESIAN_POINT('Ctrl Pts',(1.31838984174237E-15,4.78202092340378,
1.20708649626074));
#51816=CARTESIAN_POINT('',(-29.575,-2.36230756092323,-3.31488661006752));
#51817=CARTESIAN_POINT('Ctrl Pts',(-29.575,-2.36826780557339,-3.31775809990771));
#51818=CARTESIAN_POINT('Ctrl Pts',(-29.575,-2.44830306796112,-3.27276844726465));
#51819=CARTESIAN_POINT('Ctrl Pts',(-29.575,-2.52655779909889,-3.22498344987375));
#51820=CARTESIAN_POINT('Ctrl Pts',(-29.575,-2.60286326628888,-3.1744359090982));
#51821=CARTESIAN_POINT('Ctrl Pts',(-29.575,-2.70499541343267,-3.106779828055));
#51822=CARTESIAN_POINT('Ctrl Pts',(-29.575,-2.80363682654566,-3.03417684171155));
#51823=CARTESIAN_POINT('Ctrl Pts',(-29.575,-2.89869614562238,-2.9570330604008));
#51824=CARTESIAN_POINT('Ctrl Pts',(-29.575,-2.96224887403662,-2.90545791942454));
#51825=CARTESIAN_POINT('Ctrl Pts',(-29.575,-3.02420016779924,-2.85185208063885));
#51826=CARTESIAN_POINT('Ctrl Pts',(-29.575,-3.08451737823507,-2.79632528183713));
#51827=CARTESIAN_POINT('Ctrl Pts',(-29.575,-3.11868159705198,-2.76487439591655));
#51828=CARTESIAN_POINT('Ctrl Pts',(-29.575,-3.15232148638354,-2.73280706845916));
#51829=CARTESIAN_POINT('Ctrl Pts',(-29.575,-3.18543039276807,-2.70014206823866));
#51830=CARTESIAN_POINT('Ctrl Pts',(-29.575,-3.20694675023592,-2.67891419035985));
#51831=CARTESIAN_POINT('Ctrl Pts',(-29.575,-3.22824271002023,-2.65742973362904));
#51832=CARTESIAN_POINT('Ctrl Pts',(-29.575,-3.24929376278556,-2.63571743596404));
#51833=CARTESIAN_POINT('Ctrl Pts',(-29.575,-3.33714135858251,-2.54511041643103));
#51834=CARTESIAN_POINT('Ctrl Pts',(-29.575,-3.42079165100367,-2.45047748262222));
#51835=CARTESIAN_POINT('Ctrl Pts',(-29.575,-3.50014704916176,-2.35224076529156));
#51836=CARTESIAN_POINT('Ctrl Pts',(-29.575,-3.58105807397336,-2.25207828538672));
#51837=CARTESIAN_POINT('Ctrl Pts',(-29.575,-3.65750467553342,-2.14816887047587));
#51838=CARTESIAN_POINT('Ctrl Pts',(-29.575,-3.72935582339607,-2.04091404902635));
#51839=CARTESIAN_POINT('Ctrl Pts',(-29.575,-3.76079070058598,-1.99399006464218));
#51840=CARTESIAN_POINT('Ctrl Pts',(-29.575,-3.79134558154171,-1.94642520728123));
#51841=CARTESIAN_POINT('Ctrl Pts',(-29.575,-3.82100749080666,-1.89825079032625));
#51842=CARTESIAN_POINT('Ctrl Pts',(-29.575,-3.83626358617193,-1.87347310347317));
#51843=CARTESIAN_POINT('Ctrl Pts',(-29.575,-3.85128343521349,-1.84853414389017));
#51844=CARTESIAN_POINT('Ctrl Pts',(-29.575,-3.86606513313638,-1.82343804723132));
#51845=CARTESIAN_POINT('Ctrl Pts',(-29.575,-3.87962032072916,-1.80042429740151));
#51846=CARTESIAN_POINT('Ctrl Pts',(-29.575,-3.8929775187076,-1.77727417891757));
#51847=CARTESIAN_POINT('Ctrl Pts',(-29.575,-3.90612065588015,-1.75401710046083));
#51848=CARTESIAN_POINT('Ctrl Pts',(-29.575,-3.97117453777595,-1.63890278526318));
#51849=CARTESIAN_POINT('Ctrl Pts',(-29.575,-4.03105238509688,-1.52106386401277));
#51850=CARTESIAN_POINT('Ctrl Pts',(-29.575,-4.08564840782879,-1.40094223444012));
#51851=CARTESIAN_POINT('Ctrl Pts',(-29.575,-4.14101887615531,-1.27911667732505));
#51852=CARTESIAN_POINT('Ctrl Pts',(-29.575,-4.19095714201348,-1.1549425736421));
#51853=CARTESIAN_POINT('Ctrl Pts',(-29.575,-4.23531866325731,-1.0288395166209));
#51854=CARTESIAN_POINT('Ctrl Pts',(-29.575,-4.27963521656908,-0.902864286453708));
#51855=CARTESIAN_POINT('Ctrl Pts',(-29.575,-4.31838678906507,-0.774963270506112));
#51856=CARTESIAN_POINT('Ctrl Pts',(-29.575,-4.35138804153719,-0.645524185385383));
#51857=CARTESIAN_POINT('Ctrl Pts',(-29.575,-4.37561871456528,-0.550485484921972));
#51858=CARTESIAN_POINT('Ctrl Pts',(-29.575,-4.39674856572066,-0.45461692513887));
#51859=CARTESIAN_POINT('Ctrl Pts',(-29.575,-4.41468782191536,-0.358064990641669));
#51860=CARTESIAN_POINT('Ctrl Pts',(-29.575,-4.42224607172046,-0.317385286189321));
#51861=CARTESIAN_POINT('Ctrl Pts',(-29.575,-4.42923776471172,-0.27658421805809));
#51862=CARTESIAN_POINT('Ctrl Pts',(-29.575,-4.43565536938885,-0.235672547990024));
#51863=CARTESIAN_POINT('Ctrl Pts',(-29.575,-4.43961660695444,-0.210420004011757));
#51864=CARTESIAN_POINT('Ctrl Pts',(-29.575,-4.44335980044231,-0.185119699039305));
#51865=CARTESIAN_POINT('Ctrl Pts',(-29.575,-4.44687885001345,-0.159806585076518));
#51866=CARTESIAN_POINT('Ctrl Pts',(-29.575,-4.46586121538066,-0.0232632462829367));
#51867=CARTESIAN_POINT('Ctrl Pts',(-29.575,-4.47835132040759,0.113799339019299));
#51868=CARTESIAN_POINT('Ctrl Pts',(-29.575,-4.48420367058679,0.25094774090325));
#51869=CARTESIAN_POINT('Ctrl Pts',(-29.575,-4.48802427633214,0.340482706542299));
#51870=CARTESIAN_POINT('Ctrl Pts',(-29.575,-4.4890151135886,0.430054946692756));
#51871=CARTESIAN_POINT('Ctrl Pts',(-29.575,-4.48712517877637,0.519549617577561));
#51872=CARTESIAN_POINT('Ctrl Pts',(-29.575,-4.48432359350001,0.652213956389896));
#51873=CARTESIAN_POINT('Ctrl Pts',(-29.575,-4.47519448741699,0.784707646574493));
#51874=CARTESIAN_POINT('Ctrl Pts',(-29.575,-4.45999947400341,0.916663774321655));
#51875=CARTESIAN_POINT('Ctrl Pts',(-29.575,-4.44456005012953,1.05074240482977));
#51876=CARTESIAN_POINT('Ctrl Pts',(-29.575,-4.42285792068252,1.1842667673282));
#51877=CARTESIAN_POINT('Ctrl Pts',(-29.575,-4.39511381888785,1.31685585528468));
#51878=CARTESIAN_POINT('Ctrl Pts',(-29.575,-4.38178896280792,1.38053535472801));
#51879=CARTESIAN_POINT('Ctrl Pts',(-29.575,-4.36706965006509,1.44399910643623));
#51880=CARTESIAN_POINT('Ctrl Pts',(-29.575,-4.35097613979996,1.50720443522242));
#51881=CARTESIAN_POINT('Ctrl Pts',(-29.575,-4.34482928679442,1.53134546218391));
#51882=CARTESIAN_POINT('Ctrl Pts',(-29.575,-4.33848058918165,1.55545340805442));
#51883=CARTESIAN_POINT('Ctrl Pts',(-29.575,-4.3319391871451,1.57949701586949));
#51884=CARTESIAN_POINT('Ctrl Pts',(-29.575,-4.29596876934752,1.71171005118469));
#51885=CARTESIAN_POINT('Ctrl Pts',(-29.575,-4.25413965605729,1.84212793058693));
#51886=CARTESIAN_POINT('Ctrl Pts',(-29.575,-4.20675605414909,1.97036806915586));
#51887=CARTESIAN_POINT('Ctrl Pts',(-29.575,-4.15824257123346,2.10166614530495));
#51888=CARTESIAN_POINT('Ctrl Pts',(-29.575,-4.10390647699439,2.23068214498256));
#51889=CARTESIAN_POINT('Ctrl Pts',(-29.575,-4.04401911667263,2.35700945357488));
#51890=CARTESIAN_POINT('Ctrl Pts',(-29.575,-3.98492825956341,2.48165660617797));
#51891=CARTESIAN_POINT('Ctrl Pts',(-29.575,-3.92043243319514,2.60368687307991));
#51892=CARTESIAN_POINT('Ctrl Pts',(-29.575,-3.85074314886284,2.72270204804338));
#51893=CARTESIAN_POINT('Ctrl Pts',(-29.575,-3.79985133012436,2.80961496111749));
#51894=CARTESIAN_POINT('Ctrl Pts',(-29.575,-3.74618885745191,2.89491983557514));
#51895=CARTESIAN_POINT('Ctrl Pts',(-29.575,-3.68984439893471,2.97851803505928));
#51896=CARTESIAN_POINT('Ctrl Pts',(-29.575,-3.66391228552828,3.01699347783834));
#51897=CARTESIAN_POINT('Ctrl Pts',(-29.575,-3.63741189415848,3.05510731852617));
#51898=CARTESIAN_POINT('Ctrl Pts',(-29.575,-3.61035102303907,3.09284943609328));
#51899=CARTESIAN_POINT('Ctrl Pts',(-29.575,-3.59584650743156,3.11307905586041));
#51900=CARTESIAN_POINT('Ctrl Pts',(-29.575,-3.58118096187307,3.13320187682416));
#51901=CARTESIAN_POINT('Ctrl Pts',(-29.575,-3.56635552732019,3.15321629747535));
#51902=CARTESIAN_POINT('Ctrl Pts',(-29.575,-3.5546900145129,3.16896480586503));
#51903=CARTESIAN_POINT('Ctrl Pts',(-29.575,-3.54292488679082,3.18464691960963));
#51904=CARTESIAN_POINT('Ctrl Pts',(-29.575,-3.53107100158975,3.20024854439494));
#51905=CARTESIAN_POINT('Ctrl Pts',(-29.575,-3.444915061959,3.31364365665938));
#51906=CARTESIAN_POINT('Ctrl Pts',(-29.575,-3.353952606715,3.42295435898676));
#51907=CARTESIAN_POINT('Ctrl Pts',(-29.575,-3.25851212336527,3.52794677560707));
#51908=CARTESIAN_POINT('Ctrl Pts',(-29.575,-3.1617890061929,3.63435019539871));
#51909=CARTESIAN_POINT('Ctrl Pts',(-29.575,-3.06046638882771,3.73631912635592));
#51910=CARTESIAN_POINT('Ctrl Pts',(-29.575,-2.95483635071748,3.83359158033952));
#51911=CARTESIAN_POINT('Ctrl Pts',(-29.575,-2.84930340889874,3.93077462041477));
#51912=CARTESIAN_POINT('Ctrl Pts',(-29.575,-2.73947053698142,4.02327043490703));
#51913=CARTESIAN_POINT('Ctrl Pts',(-29.575,-2.62558525501093,4.11078989098106));
#51914=CARTESIAN_POINT('Ctrl Pts',(-29.575,-2.51319651570498,4.19715927219268));
#51915=CARTESIAN_POINT('Ctrl Pts',(-29.575,-2.39686069001292,4.27868275896332));
#51916=CARTESIAN_POINT('Ctrl Pts',(-29.575,-2.27677987968084,4.3550468235479));
#51917=CARTESIAN_POINT('Ctrl Pts',(-29.575,-2.24098328939054,4.37781126963447));
#51918=CARTESIAN_POINT('Ctrl Pts',(-29.575,-2.20485367910692,4.40011694506889));
#51919=CARTESIAN_POINT('Ctrl Pts',(-29.575,-2.16839587231048,4.42195480991686));
#51920=CARTESIAN_POINT('Ctrl Pts',(-29.575,-2.36826780557337,-3.31775809990772));
#51921=CARTESIAN_POINT('Ctrl Pts',(-29.5008109365549,-1.33928601121754,
-4.04293436335451));
#51922=CARTESIAN_POINT('Ctrl Pts',(-29.3470759847368,1.55637121596689,-4.50701225231274));
#51923=CARTESIAN_POINT('Ctrl Pts',(-29.1137951445456,4.65387018191312,-1.22765401651987));
#51924=CARTESIAN_POINT('Ctrl Pts',(-28.8751574794264,3.55090078994383,3.25125842872222));
#51925=CARTESIAN_POINT('Ctrl Pts',(-28.6365198143072,-0.816478135197904,
4.74503193420896));
#51926=CARTESIAN_POINT('Ctrl Pts',(-28.4455297648071,-3.71062116286106,
2.45079400531014));
#51927=CARTESIAN_POINT('Ctrl Pts',(-28.3340856036801,-4.06733760858173,
0.547694664417248));
#51928=CARTESIAN_POINT('Ctrl Pts',(-28.3021873309261,-4.06480101368718,
0.00206955444756761));
#51929=CARTESIAN_POINT('Origin',(-29.575,-4.52129938221115E-16,0.));
#51930=CARTESIAN_POINT('',(-29.575,-4.925,-6.03138548580071E-16));
#51931=CARTESIAN_POINT('Origin',(-29.575,0.,0.));
#51932=CARTESIAN_POINT('Origin',(-29.575,0.,0.));
#51933=CARTESIAN_POINT('',(-29.575,2.36230756092324,-3.31488661006752));
#51934=CARTESIAN_POINT('Ctrl Pts',(-29.575,2.17494790042119,4.42655504786424));
#51935=CARTESIAN_POINT('Ctrl Pts',(-29.575,2.26967152441801,4.37041752782518));
#51936=CARTESIAN_POINT('Ctrl Pts',(-29.575,2.36222031470781,4.31097507135364));
#51937=CARTESIAN_POINT('Ctrl Pts',(-29.575,2.45239463893034,4.24821920794634));
#51938=CARTESIAN_POINT('Ctrl Pts',(-29.575,2.57031754301399,4.16615201503894));
#51939=CARTESIAN_POINT('Ctrl Pts',(-29.575,2.68418134028915,4.07841926504524));
#51940=CARTESIAN_POINT('Ctrl Pts',(-29.575,2.793800816624,3.98544075385194));
#51941=CARTESIAN_POINT('Ctrl Pts',(-29.575,2.86142888819741,3.928079073063));
#51942=CARTESIAN_POINT('Ctrl Pts',(-29.575,2.92744077307288,3.8687200679563));
#51943=CARTESIAN_POINT('Ctrl Pts',(-29.575,2.99178498903163,3.80745669486626));
#51944=CARTESIAN_POINT('Ctrl Pts',(-29.575,3.03740293232873,3.76402296833516));
#51945=CARTESIAN_POINT('Ctrl Pts',(-29.575,3.08218251964483,3.71963195357705));
#51946=CARTESIAN_POINT('Ctrl Pts',(-29.575,3.12610340234575,3.67431582845979));
#51947=CARTESIAN_POINT('Ctrl Pts',(-29.575,3.14170642099533,3.65821714596868));
#51948=CARTESIAN_POINT('Ctrl Pts',(-29.575,3.15720284290207,3.64199979656664));
#51949=CARTESIAN_POINT('Ctrl Pts',(-29.575,3.17258572052557,3.62567157287578));
#51950=CARTESIAN_POINT('Ctrl Pts',(-29.575,3.27034309847291,3.52190657040855));
#51951=CARTESIAN_POINT('Ctrl Pts',(-29.575,3.36340172212969,3.41379269192058));
#51952=CARTESIAN_POINT('Ctrl Pts',(-29.575,3.45158356813246,3.30174290977256));
#51953=CARTESIAN_POINT('Ctrl Pts',(-29.575,3.53724490642985,3.19289585417305));
#51954=CARTESIAN_POINT('Ctrl Pts',(-29.575,3.61830434560196,3.08033384565738));
#51955=CARTESIAN_POINT('Ctrl Pts',(-29.575,3.69455768842054,2.96441414844495));
#51956=CARTESIAN_POINT('Ctrl Pts',(-29.575,3.76127936338681,2.86298441338408));
#51957=CARTESIAN_POINT('Ctrl Pts',(-29.575,3.82432087679273,2.75898335344391));
#51958=CARTESIAN_POINT('Ctrl Pts',(-29.575,3.88351761773973,2.65264344251299));
#51959=CARTESIAN_POINT('Ctrl Pts',(-29.575,3.89539020296671,2.63131575393826));
#51960=CARTESIAN_POINT('Ctrl Pts',(-29.575,3.90710917047629,2.60989171569305));
#51961=CARTESIAN_POINT('Ctrl Pts',(-29.575,3.91866219954629,2.58839389445723));
#51962=CARTESIAN_POINT('Ctrl Pts',(-29.575,3.98533187012549,2.46433529032153));
#51963=CARTESIAN_POINT('Ctrl Pts',(-29.575,4.04656060379988,2.33767837925172));
#51964=CARTESIAN_POINT('Ctrl Pts',(-29.575,4.10217235556336,2.20881042226382));
#51965=CARTESIAN_POINT('Ctrl Pts',(-29.575,4.15749625211679,2.08060950617376));
#51966=CARTESIAN_POINT('Ctrl Pts',(-29.575,4.20726139736363,1.95021957273537));
#51967=CARTESIAN_POINT('Ctrl Pts',(-29.575,4.25124518841383,1.81800776290176));
#51968=CARTESIAN_POINT('Ctrl Pts',(-29.575,4.29413119192342,1.68909581590603));
#51969=CARTESIAN_POINT('Ctrl Pts',(-29.575,4.33152087503006,1.55845109390724));
#51970=CARTESIAN_POINT('Ctrl Pts',(-29.575,4.36315916984956,1.42641155759016));
#51971=CARTESIAN_POINT('Ctrl Pts',(-29.575,4.38688789096419,1.32738190535235));
#51972=CARTESIAN_POINT('Ctrl Pts',(-29.575,4.40738049178401,1.22756756386048));
#51973=CARTESIAN_POINT('Ctrl Pts',(-29.575,4.42451035861733,1.12711368795651));
#51974=CARTESIAN_POINT('Ctrl Pts',(-29.575,4.43133674032546,1.08708205737504));
#51975=CARTESIAN_POINT('Ctrl Pts',(-29.575,4.4376289049131,1.04694890359475));
#51976=CARTESIAN_POINT('Ctrl Pts',(-29.575,4.44337808320161,1.00672360633312));
#51977=CARTESIAN_POINT('Ctrl Pts',(-29.575,4.44682246179442,0.982624309733816));
#51978=CARTESIAN_POINT('Ctrl Pts',(-29.575,4.45007193773189,0.958491942467769));
#51979=CARTESIAN_POINT('Ctrl Pts',(-29.575,4.45312454919313,0.934328545878378));
#51980=CARTESIAN_POINT('Ctrl Pts',(-29.575,4.45558677843594,0.914838406879834));
#51981=CARTESIAN_POINT('Ctrl Pts',(-29.575,4.45791999829306,0.895335151707175));
#51982=CARTESIAN_POINT('Ctrl Pts',(-29.575,4.46012266207708,0.87582765091181));
#51983=CARTESIAN_POINT('Ctrl Pts',(-29.575,4.47511104469547,0.743085700928035));
#51984=CARTESIAN_POINT('Ctrl Pts',(-29.575,4.48407271847718,0.610034498076699));
#51985=CARTESIAN_POINT('Ctrl Pts',(-29.575,4.48680554393477,0.476999857930275));
#51986=CARTESIAN_POINT('Ctrl Pts',(-29.575,4.48859856927288,0.389714927249725));
#51987=CARTESIAN_POINT('Ctrl Pts',(-29.575,4.48770920842808,0.302437045899035));
#51988=CARTESIAN_POINT('Ctrl Pts',(-29.575,4.48406815367479,0.215259203818982));
#51989=CARTESIAN_POINT('Ctrl Pts',(-29.575,4.47844824112982,0.0807015326092455));
#51990=CARTESIAN_POINT('Ctrl Pts',(-29.575,4.46627498023888,-0.0536189903864601));
#51991=CARTESIAN_POINT('Ctrl Pts',(-29.575,4.44773981895834,-0.187263918132325));
#51992=CARTESIAN_POINT('Ctrl Pts',(-29.575,4.42923611011045,-0.320682062953368));
#51993=CARTESIAN_POINT('Ctrl Pts',(-29.575,4.40439160268717,-0.453427703408474));
#51994=CARTESIAN_POINT('Ctrl Pts',(-29.575,4.37335182340664,-0.58503925570624));
#51995=CARTESIAN_POINT('Ctrl Pts',(-29.575,4.35843537009352,-0.648286405680295));
#51996=CARTESIAN_POINT('Ctrl Pts',(-29.575,4.34208757622849,-0.711271201901602));
#51997=CARTESIAN_POINT('Ctrl Pts',(-29.575,4.32432137404194,-0.773939500968908));
#51998=CARTESIAN_POINT('Ctrl Pts',(-29.575,4.31955371135246,-0.790756899990894));
#51999=CARTESIAN_POINT('Ctrl Pts',(-29.575,4.31468432223976,-0.807549803851364));
#52000=CARTESIAN_POINT('Ctrl Pts',(-29.575,4.30971696019155,-0.824305954558689));
#52001=CARTESIAN_POINT('Ctrl Pts',(-29.575,4.27217870230904,-0.950931857858156));
#52002=CARTESIAN_POINT('Ctrl Pts',(-29.575,4.22899927473913,-1.07563909243635));
#52003=CARTESIAN_POINT('Ctrl Pts',(-29.575,4.18039187949891,-1.19802776435577));
#52004=CARTESIAN_POINT('Ctrl Pts',(-29.575,4.13198650007613,-1.3199077801853));
#52005=CARTESIAN_POINT('Ctrl Pts',(-29.575,4.07819767353095,-1.43948920797592));
#52006=CARTESIAN_POINT('Ctrl Pts',(-29.575,4.01919161106764,-1.55635171305596));
#52007=CARTESIAN_POINT('Ctrl Pts',(-29.575,3.96554454554038,-1.66260063403094));
#52008=CARTESIAN_POINT('Ctrl Pts',(-29.575,3.90758410693226,-1.7666021746683));
#52009=CARTESIAN_POINT('Ctrl Pts',(-29.575,3.84540829196954,-1.86801442537029));
#52010=CARTESIAN_POINT('Ctrl Pts',(-29.575,3.79972079463418,-1.9425333027907));
#52011=CARTESIAN_POINT('Ctrl Pts',(-29.575,3.7517566228007,-2.01565352617642));
#52012=CARTESIAN_POINT('Ctrl Pts',(-29.575,3.70157235710967,-2.08727533440549));
#52013=CARTESIAN_POINT('Ctrl Pts',(-29.575,3.67384420437395,-2.12684830434812));
#52014=CARTESIAN_POINT('Ctrl Pts',(-29.575,3.64543819285622,-2.16596367436737));
#52015=CARTESIAN_POINT('Ctrl Pts',(-29.575,3.61636323740365,-2.20460339725076));
#52016=CARTESIAN_POINT('Ctrl Pts',(-29.575,3.60131842230507,-2.22459749447954));
#52017=CARTESIAN_POINT('Ctrl Pts',(-29.575,3.58609448820911,-2.24446422067884));
#52018=CARTESIAN_POINT('Ctrl Pts',(-29.575,3.57069262976354,-2.26420097811176));
#52019=CARTESIAN_POINT('Ctrl Pts',(-29.575,3.55903139036739,-2.27914430810939));
#52020=CARTESIAN_POINT('Ctrl Pts',(-29.575,3.54727273939743,-2.29400720550239));
#52021=CARTESIAN_POINT('Ctrl Pts',(-29.575,3.53542205698418,-2.30878307744774));
#52022=CARTESIAN_POINT('Ctrl Pts',(-29.575,3.45405476451608,-2.41023484639433));
#52023=CARTESIAN_POINT('Ctrl Pts',(-29.575,3.36828498238971,-2.50767334973966));
#52024=CARTESIAN_POINT('Ctrl Pts',(-29.575,3.27835860536771,-2.60083261446428));
#52025=CARTESIAN_POINT('Ctrl Pts',(-29.575,3.19030403000318,-2.69205278554481));
#52026=CARTESIAN_POINT('Ctrl Pts',(-29.575,3.09826340014138,-2.77917034507256));
#52027=CARTESIAN_POINT('Ctrl Pts',(-29.575,3.00243676957963,-2.86189425854725));
#52028=CARTESIAN_POINT('Ctrl Pts',(-29.575,2.90355461728311,-2.94725590136843));
#52029=CARTESIAN_POINT('Ctrl Pts',(-29.575,2.80064068610558,-3.02794003035809));
#52030=CARTESIAN_POINT('Ctrl Pts',(-29.575,2.69389027200841,-3.10357332294541));
#52031=CARTESIAN_POINT('Ctrl Pts',(-29.575,2.59371175266095,-3.17455038967486));
#52032=CARTESIAN_POINT('Ctrl Pts',(-29.575,2.49015393838355,-3.24107925145737));
#52033=CARTESIAN_POINT('Ctrl Pts',(-29.575,2.38336574054609,-3.30280154424992));
#52034=CARTESIAN_POINT('Ctrl Pts',(-29.575,2.37636023875519,-3.30685063995014));
#52035=CARTESIAN_POINT('Ctrl Pts',(-29.575,2.36934083188486,-3.31087903158254));
#52036=CARTESIAN_POINT('Ctrl Pts',(-29.575,2.36230756092332,-3.31488661006746));
#52037=CARTESIAN_POINT('Origin',(-29.575,0.,0.));
#52038=CARTESIAN_POINT('Origin',(-32.3478126690739,0.,0.));
#52039=CARTESIAN_POINT('Ctrl Pts',(-29.575,2.36230756092324,-3.31488661006752));
#52040=CARTESIAN_POINT('Ctrl Pts',(-29.5352270558135,2.91456939066647,-2.92132494432319));
#52041=CARTESIAN_POINT('Ctrl Pts',(-29.4556811674404,3.80947864266608,-1.85446537575054));
#52042=CARTESIAN_POINT('Ctrl Pts',(-29.2965893906943,4.40029930288375,0.892938679230673));
#52043=CARTESIAN_POINT('Ctrl Pts',(-29.0977246697615,2.41062119233501,4.16711865021482));
#52044=CARTESIAN_POINT('Ctrl Pts',(-28.8590870046423,-2.21020820766824,
4.28001845847083));
#52045=CARTESIAN_POINT('Ctrl Pts',(-28.6924496710798,-4.01269863755865,
1.60905902128973));
#52046=CARTESIAN_POINT('Ctrl Pts',(-28.6053582258903,-4.07619291884947,
0.130177206130288));
#52047=CARTESIAN_POINT('Ctrl Pts',(-28.5978126690739,-4.07533558288693,
0.00197868943318465));
#52048=CARTESIAN_POINT('Ctrl Pts',(-30.0683458050225,2.85821514250009,-4.01076441581692));
#52049=CARTESIAN_POINT('Ctrl Pts',(-30.028572860836,3.52641057585851,-3.5345842895939));
#52050=CARTESIAN_POINT('Ctrl Pts',(-29.9490269724629,4.60918371579173,-2.24376415073622));
#52051=CARTESIAN_POINT('Ctrl Pts',(-29.7899351957168,5.32403244483542,1.08038889453645));
#52052=CARTESIAN_POINT('Ctrl Pts',(-29.5910704747841,2.91667101639856,5.0419013271853));
#52053=CARTESIAN_POINT('Ctrl Pts',(-29.3524328096649,-2.6741863217702,5.17850163566369));
#52054=CARTESIAN_POINT('Ctrl Pts',(-29.1137951445457,-5.7973743179944,0.550511209599409));
#52055=CARTESIAN_POINT('Ctrl Pts',(-28.8751574794264,-3.59989778886694,
-4.57971187869854));
#52056=CARTESIAN_POINT('Ctrl Pts',(-28.6365198143073,1.9077811732274,-5.50426057988267));
#52057=CARTESIAN_POINT('Ctrl Pts',(-28.3978821491879,5.66123134949523,-1.37093968550409));
#52058=CARTESIAN_POINT('Ctrl Pts',(-28.1592444840688,4.21433244584917,4.02140449350459));
#52059=CARTESIAN_POINT('Ctrl Pts',(-27.9206068189495,-1.10479606405923,
5.71943238413845));
#52060=CARTESIAN_POINT('Ctrl Pts',(-27.6819691538303,-5.40870633854705,
2.16272545229035));
#52061=CARTESIAN_POINT('Ctrl Pts',(-27.4433314887111,-4.74359941984978,
-3.380866692594));
#52062=CARTESIAN_POINT('Ctrl Pts',(-27.2046938235918,0.279640350988314,
-5.8184000833979));
#52063=CARTESIAN_POINT('Ctrl Pts',(-26.9660561584726,5.04593690996907,-2.91039003941573));
#52064=CARTESIAN_POINT('Ctrl Pts',(-26.7274184933533,5.17640786355619,2.67146555315453));
#52065=CARTESIAN_POINT('Ctrl Pts',(-26.4887808282342,0.551162248122564,
5.79897734693768));
#52066=CARTESIAN_POINT('Ctrl Pts',(-26.2501431631149,-4.58044707277724,
3.59880626920218));
#52067=CARTESIAN_POINT('Ctrl Pts',(-26.0115054979957,-5.50387573699426,
-1.90768582721621));
#52068=CARTESIAN_POINT('Ctrl Pts',(-25.7728678328765,-1.37074105079164,
-5.66153515210527));
#52069=CARTESIAN_POINT('Ctrl Pts',(-25.5342301677573,4.02173058771444,-4.21397584735458));
#52070=CARTESIAN_POINT('Ctrl Pts',(-25.295592502638,5.71932789822544,1.10507891249598));
#52071=CARTESIAN_POINT('Ctrl Pts',(-25.0569548375188,2.16242101025971,5.40886734761332));
#52072=CARTESIAN_POINT('Ctrl Pts',(-24.8183171723995,-3.38116152304108,
4.74338034983671));
#52073=CARTESIAN_POINT('Ctrl Pts',(-24.5796795072803,-5.81837790032782,
-0.27998076825629));
#52074=CARTESIAN_POINT('Ctrl Pts',(-24.3410418421611,-2.91009025392015,
-5.04611585917912));
#52075=CARTESIAN_POINT('Ctrl Pts',(-24.1024041770419,2.67177743350171,-5.17624534512243));
#52076=CARTESIAN_POINT('Ctrl Pts',(-23.8637665119226,5.79900962484977,-0.550815695476877));
#52077=CARTESIAN_POINT('Ctrl Pts',(-23.6251288468035,3.59853198023136,4.58066350376895));
#52078=CARTESIAN_POINT('Ctrl Pts',(-23.3864911816842,-1.90801608760284,
5.50376100088902));
#52079=CARTESIAN_POINT('Ctrl Pts',(-23.147853516565,-5.66161723459444,1.37040170709392));
#52080=CARTESIAN_POINT('Ctrl Pts',(-22.9092158514458,-4.21373472077718,
-4.02198337277209));
#52081=CARTESIAN_POINT('Ctrl Pts',(-22.6705781863265,1.10542191660648,-5.71926157245085));
#52082=CARTESIAN_POINT('Ctrl Pts',(-22.4319405212073,5.40899699874395,-2.16209667128711));
#52083=CARTESIAN_POINT('Ctrl Pts',(-22.1933028560881,4.74317758767807,3.38144598062146));
#52084=CARTESIAN_POINT('Ctrl Pts',(-21.9546651909688,-0.280329688527433,
5.81836109345686));
#52085=CARTESIAN_POINT('Ctrl Pts',(-21.7160275258496,-5.04629036031444,
2.90978764647796));
#52086=CARTESIAN_POINT('Ctrl Pts',(-21.4773898607304,-5.17608511572218,
-2.67208783967747));
#52087=CARTESIAN_POINT('Ctrl Pts',(-21.2387521956112,-0.55046793874511,
-5.79904264483125));
#52088=CARTESIAN_POINT('Ctrl Pts',(-21.0001145304919,4.58087929208444,-3.59825728089574));
#52089=CARTESIAN_POINT('Ctrl Pts',(-20.7614768653727,5.50364657119464,1.90834613410097));
#52090=CARTESIAN_POINT('Ctrl Pts',(-20.5228392002535,1.37006218854147,5.66169940456846));
#52091=CARTESIAN_POINT('Ctrl Pts',(-20.2842015351343,-4.02223605484748,
4.21349352286768));
#52092=CARTESIAN_POINT('Ctrl Pts',(-20.045563870015,-5.71919527222015,-1.10576488747686));
#52093=CARTESIAN_POINT('Ctrl Pts',(-19.8069262048958,-2.16177230051888,
-5.40912664566764));
#52094=CARTESIAN_POINT('Ctrl Pts',(-19.5682885397766,3.38173041352887,-4.74297480052089));
#52095=CARTESIAN_POINT('Ctrl Pts',(-19.3296508746573,5.81834427218029,0.28067860365368));
#52096=CARTESIAN_POINT('Ctrl Pts',(-19.0910132095381,2.90948502517622,5.04646484545742));
#52097=CARTESIAN_POINT('Ctrl Pts',(-18.8523755444189,-2.67239823447518,
5.17592486658531));
#52098=CARTESIAN_POINT('Ctrl Pts',(-18.6137378792997,-5.79907564487983,
0.550120180618539));
#52099=CARTESIAN_POINT('Ctrl Pts',(-18.3751002141804,-3.59798256814023,
-4.58109506423096));
#52100=CARTESIAN_POINT('Ctrl Pts',(-18.1364625490612,1.90867617348636,-5.50353212154956));
#52101=CARTESIAN_POINT('Ctrl Pts',(-17.897824883942,5.66178155431231,-1.3697226651447));
#52102=CARTESIAN_POINT('Ctrl Pts',(-17.6591872188228,4.2132523097379,4.02248872250135));
#52103=CARTESIAN_POINT('Ctrl Pts',(-17.4205495537035,-1.10610785433544,
5.71912895139983));
#52104=CARTESIAN_POINT('Ctrl Pts',(-17.1819118885843,-5.40925627315763,
2.16144792198822));
#52105=CARTESIAN_POINT('Ctrl Pts',(-16.9432742234651,-4.74277199629759,
-3.38201483428115));
#52106=CARTESIAN_POINT('Ctrl Pts',(-16.7046365583458,0.281027517765593,
-5.81832742997681));
#52107=CARTESIAN_POINT('Ctrl Pts',(-16.4659988932266,5.04663931245511,-2.90918239341314));
#52108=CARTESIAN_POINT('Ctrl Pts',(-16.2273612281074,5.17576459883361,2.67270861966342));
#52109=CARTESIAN_POINT('Ctrl Pts',(-15.9887235629882,0.549772420514306,
5.79910862407352));
#52110=CARTESIAN_POINT('Ctrl Pts',(-15.750085897869,-4.5813108199035,3.597707842446));
#52111=CARTESIAN_POINT('Ctrl Pts',(-15.5114482327497,-5.50341765211267,
-1.90900620600798));
#52112=CARTESIAN_POINT('Ctrl Pts',(-15.2728105676305,-1.36938313682227,
-5.66186368369541));
#52113=CARTESIAN_POINT('Ctrl Pts',(-15.0341729025113,4.02274137568974,-4.21301108145661));
#52114=CARTESIAN_POINT('Ctrl Pts',(-14.7955352373921,5.71906261001256,1.10645081721627));
#52115=CARTESIAN_POINT('Ctrl Pts',(-14.5568975722728,2.16112353568466,5.40938588119503));
#52116=CARTESIAN_POINT('Ctrl Pts',(-14.3182599071536,-3.38229924287111,
4.74256917501852));
#52117=CARTESIAN_POINT('Ctrl Pts',(-14.0796222420344,-5.81831056684969,
-0.281376430866862));
#52118=CARTESIAN_POINT('Ctrl Pts',(-13.8409845769151,-2.90887975118817,
-5.04681376130423));
#52119=CARTESIAN_POINT('Ctrl Pts',(-13.6023469117959,2.67301899524012,-5.17560431246901));
#52120=CARTESIAN_POINT('Ctrl Pts',(-13.3637092466767,5.79914158241269,-0.549424658433007));
#52121=CARTESIAN_POINT('Ctrl Pts',(-13.1250715815575,3.5974331038138,4.5815265591009));
#52122=CARTESIAN_POINT('Ctrl Pts',(-12.8864339164382,-1.90933623166449,
5.50330316288458));
#52123=CARTESIAN_POINT('Ctrl Pts',(-12.647796251319,-5.66194579271754,1.3690436035753));
#52124=CARTESIAN_POINT('Ctrl Pts',(-12.4091585861998,-4.21276983802462,
-4.0229940144117));
#52125=CARTESIAN_POINT('Ctrl Pts',(-12.1705209210806,1.10679377611814,-5.7189962480586));
#52126=CARTESIAN_POINT('Ctrl Pts',(-11.9318832559613,5.4095154697794,-2.16079914160935));
#52127=CARTESIAN_POINT('Ctrl Pts',(-11.6932455908421,4.74236633668439,3.38258363929778));
#52128=CARTESIAN_POINT('Ctrl Pts',(-11.4546079257229,-0.281725342956251,
5.81829368279896));
#52129=CARTESIAN_POINT('Ctrl Pts',(-11.2159702606036,-5.04698819200419,
2.9085770985024));
#52130=CARTESIAN_POINT('Ctrl Pts',(-10.9773325954844,-5.17544400749208,
-2.67332936120422));
#52131=CARTESIAN_POINT('Ctrl Pts',(-10.7386949303652,-0.549076894375944,
-5.79917451989717));
#52132=CARTESIAN_POINT('Ctrl Pts',(-10.5000572652459,4.58174228182235,-3.5971583522447));
#52133=CARTESIAN_POINT('Ctrl Pts',(-10.2614196001268,5.50318865386573,1.9096662504547));
#52134=CARTESIAN_POINT('Ctrl Pts',(-10.0227819350075,1.36870406540507,5.66202788137834));
#52135=CARTESIAN_POINT('Ctrl Pts',(-9.78414426988828,-4.02324663866633,
4.21252857944289));
#52136=CARTESIAN_POINT('Ctrl Pts',(-9.54550660476906,-5.71892986553813,
-1.10713673103989));
#52137=CARTESIAN_POINT('Ctrl Pts',(-9.30686893964983,-2.16047473976357,
-5.40964503891006));
#52138=CARTESIAN_POINT('Ctrl Pts',(-9.0682312745306,3.38286802356034,-4.74216348129631));
#52139=CARTESIAN_POINT('Ctrl Pts',(-8.82959360941138,5.81827677782428,0.282074254033242));
#52140=CARTESIAN_POINT('Ctrl Pts',(-8.59095594429215,2.90827443535771,5.04716260455295));
#52141=CARTESIAN_POINT('Ctrl Pts',(-8.35231827917293,-2.67363971755611,
5.1752836839061));
#52142=CARTESIAN_POINT('Ctrl Pts',(-8.1136806140537,-5.79920743652394,0.548729128339138));
#52143=CARTESIAN_POINT('Ctrl Pts',(-7.87504294893448,-3.59688358774524,
-4.58195798805725));
#52144=CARTESIAN_POINT('Ctrl Pts',(-7.63640528381524,1.90999626238828,-5.50307412507543));
#52145=CARTESIAN_POINT('Ctrl Pts',(-7.39776761869603,5.66210994965676,-1.36836452227643));
#52146=CARTESIAN_POINT('Ctrl Pts',(-7.15912995357678,4.21228730575213,4.0234992483829));
#52147=CARTESIAN_POINT('Ctrl Pts',(-6.92049228845757,-1.10747968205672,
5.7188634625854));
#52148=CARTESIAN_POINT('Ctrl Pts',(-6.68185462333833,-5.40977458843978,
2.16015032989127));
#52149=CARTESIAN_POINT('Ctrl Pts',(-6.44321695821912,-4.74196060913677,
-3.38315239516401));
#52150=CARTESIAN_POINT('Ctrl Pts',(-6.20457929309988,0.282423164637435,
-5.81825985287354));
#52151=CARTESIAN_POINT('Ctrl Pts',(-5.96594162798066,5.04733699791161,-2.90797175993565));
#52152=CARTESIAN_POINT('Ctrl Pts',(-5.72730396286144,5.17512334370478,2.6739500608018));
#52153=CARTESIAN_POINT('Ctrl Pts',(-5.4886662977422,0.548381356497653,5.79924033899806));
#52154=CARTESIAN_POINT('Ctrl Pts',(-5.25002863262299,-4.58217367045971,
3.59660879744466));
#52155=CARTESIAN_POINT('Ctrl Pts',(-5.01139096750376,-5.5029595906143,-1.91032624275442));
#52156=CARTESIAN_POINT('Ctrl Pts',(-4.77275330238452,-1.3680249471228,-5.66219204498688));
#52157=CARTESIAN_POINT('Ctrl Pts',(-4.53411563726531,4.02375179159935,-4.21204592589478));
#52158=CARTESIAN_POINT('Ctrl Pts',(-4.29547797214607,5.71879713894916,1.10782245436525));
#52159=CARTESIAN_POINT('Ctrl Pts',(-4.05684030702685,2.1598257205091,5.40990445393106));
#52160=CARTESIAN_POINT('Ctrl Pts',(-3.81820264190762,-3.38343638652024,
4.74175707603558));
#52161=CARTESIAN_POINT('Ctrl Pts',(-3.57956497678839,-5.8182436135944,-0.282770838170588));
#52162=CARTESIAN_POINT('Ctrl Pts',(-3.34092731166917,-2.90766771762518,
-5.04751374594047));
#52163=CARTESIAN_POINT('Ctrl Pts',(-3.10228964654994,2.67425779052882,-5.17495842985376));
#52164=CARTESIAN_POINT('Ctrl Pts',(-2.86365198143071,5.79927821925697,-0.54804232686631));
#52165=CARTESIAN_POINT('Ctrl Pts',(-2.62501431631149,3.59632439845965,4.58240612234822));
#52166=CARTESIAN_POINT('Ctrl Pts',(-2.38637665119227,-1.91063779555211,
5.5028128128105));
#52167=CARTESIAN_POINT('Ctrl Pts',(-2.14773898607303,-5.66230948168428,
1.36774722574033));
#52168=CARTESIAN_POINT('Ctrl Pts',(-1.90910132095381,-4.21173664772448,
-4.02412306903384));
#52169=CARTESIAN_POINT('Ctrl Pts',(-1.67046365583459,1.10803490710056,-5.71850283364837));
#52170=CARTESIAN_POINT('Ctrl Pts',(-1.43182599071535,5.41028448303652,-2.15993873727599));
#52171=CARTESIAN_POINT('Ctrl Pts',(-1.19318832559614,4.74107307396736,3.3845606937213));
#52172=CARTESIAN_POINT('Ctrl Pts',(-0.954550660476906,-0.282194523950606,
5.81661222925236));
#52173=CARTESIAN_POINT('Ctrl Pts',(-0.715912995357673,-5.049479635978,2.91048227618002));
#52174=CARTESIAN_POINT('Ctrl Pts',(-0.477275330238451,-5.17121721536142,
-2.68071843402506));
#52175=CARTESIAN_POINT('Ctrl Pts',(-0.278410609305759,-1.32510607804596,
-5.26845855246328));
#52176=CARTESIAN_POINT('Ctrl Pts',(-0.119318832559609,2.02851289583626,
-4.70788567421457));
#52177=CARTESIAN_POINT('Ctrl Pts',(-0.0397729441865337,3.3679595299544,
-3.68587930545211));
#52178=CARTESIAN_POINT('Ctrl Pts',(4.44089209850063E-15,3.87448963569911,
-3.0403873211912));
#52179=CARTESIAN_POINT('Ctrl Pts',(-29.9038972033484,2.6929126153078,-3.77880514723378));
#52180=CARTESIAN_POINT('Ctrl Pts',(-29.8641242591618,3.32246351412783,-3.330164507837));
#52181=CARTESIAN_POINT('Ctrl Pts',(-29.7845783707887,4.34261535808318,-2.11399789240766));
#52182=CARTESIAN_POINT('Ctrl Pts',(-29.6254865940426,5.0161213975182,1.01790548943452));
#52183=CARTESIAN_POINT('Ctrl Pts',(-29.4266218731099,2.74798774171071,4.75030710152848));
#52184=CARTESIAN_POINT('Ctrl Pts',(-29.1879842079907,-2.51952695040288,
4.87900724326607));
#52185=CARTESIAN_POINT('Ctrl Pts',(-28.9493465428715,-5.46208793188772,
0.518672845565351));
#52186=CARTESIAN_POINT('Ctrl Pts',(-28.7107088777522,-3.39170065447864,
-4.31484800050243));
#52187=CARTESIAN_POINT('Ctrl Pts',(-28.472071212633,1.79744621468105,-5.18592618627794));
#52188=CARTESIAN_POINT('Ctrl Pts',(-28.2334335475138,5.33381868024693,-1.29165251384495));
#52189=CARTESIAN_POINT('Ctrl Pts',(-27.9947958823946,3.97059998730579,3.78882986476014));
#52190=CARTESIAN_POINT('Ctrl Pts',(-27.7561582172753,-1.04090109033753,
5.38865370581382));
#52191=CARTESIAN_POINT('Ctrl Pts',(-27.5175205521561,-5.09589824607407,
2.03764600058257));
#52192=CARTESIAN_POINT('Ctrl Pts',(-27.2788828870369,-4.4692572402043,-3.18533704191237));
#52193=CARTESIAN_POINT('Ctrl Pts',(-27.0402452219176,0.26346758077383,-5.48189768940374));
#52194=CARTESIAN_POINT('Ctrl Pts',(-26.8016075567985,4.75410928969372,-2.74207001987724));
#52195=CARTESIAN_POINT('Ctrl Pts',(-26.5629698916792,4.87703456275017,2.51696353520732));
#52196=CARTESIAN_POINT('Ctrl Pts',(-26.32433222656,0.519286231809787,5.46359825096759));
#52197=CARTESIAN_POINT('Ctrl Pts',(-26.0856945614407,-4.31554067523491,
3.39067226195794));
#52198=CARTESIAN_POINT('Ctrl Pts',(-25.8470568963215,-5.18556360046217,
-1.79735638292817));
#52199=CARTESIAN_POINT('Ctrl Pts',(-25.6084192312023,-1.29146536700809,
-5.33410491268233));
#52200=CARTESIAN_POINT('Ctrl Pts',(-25.3697815660831,3.78913709957896,-3.97026401239249));
#52201=CARTESIAN_POINT('Ctrl Pts',(-25.1311439009638,5.38855526275784,1.04116758046706));
#52202=CARTESIAN_POINT('Ctrl Pts',(-24.8925062358446,2.03735916570693,5.09604994331312));
#52203=CARTESIAN_POINT('Ctrl Pts',(-24.6538685707254,-3.18561482108248,
4.46905083992566));
#52204=CARTESIAN_POINT('Ctrl Pts',(-24.4152309056062,-5.48187678927333,
-0.263788310288471));
#52205=CARTESIAN_POINT('Ctrl Pts',(-24.1765932404869,-2.74178757222978,
-4.75427788952306));
#52206=CARTESIAN_POINT('Ctrl Pts',(-23.9379555753677,2.51725737821055,-4.87688144343666));
#52207=CARTESIAN_POINT('Ctrl Pts',(-23.6993179102484,5.46362866211312,-0.518959721751974));
#52208=CARTESIAN_POINT('Ctrl Pts',(-23.4606802451293,3.39041383626465,4.31574458911784));
#52209=CARTESIAN_POINT('Ctrl Pts',(-23.22204258001,-1.79766754297636,5.1854555000254));
#52210=CARTESIAN_POINT('Ctrl Pts',(-22.9834049148908,-5.33418224799811,
1.29114564897465));
#52211=CARTESIAN_POINT('Ctrl Pts',(-22.7447672497716,-3.97003683117282,
-3.78937526502026));
#52212=CARTESIAN_POINT('Ctrl Pts',(-22.5061295846523,1.04149074721631,-5.38849277288));
#52213=CARTESIAN_POINT('Ctrl Pts',(-22.2674919195332,5.09617209617701,-2.03705358461264));
#52214=CARTESIAN_POINT('Ctrl Pts',(-22.0288542544139,4.46885980435008,3.18588282729214));
#52215=CARTESIAN_POINT('Ctrl Pts',(-21.7902165892947,-0.264117051042074,
5.48186095441396));
#52216=CARTESIAN_POINT('Ctrl Pts',(-21.5515789241754,-4.75444229852842,
2.74150246584068));
#52217=CARTESIAN_POINT('Ctrl Pts',(-21.3129412590562,-4.87673048077228,
-2.51754983229987));
#52218=CARTESIAN_POINT('Ctrl Pts',(-21.074303593937,-0.518632077245404,
-5.46365977241106));
#52219=CARTESIAN_POINT('Ctrl Pts',(-20.8356659288178,4.31594789749319,-3.39015502393968));
#52220=CARTESIAN_POINT('Ctrl Pts',(-20.5970282636985,5.1853476882785,1.79797850150613));
#52221=CARTESIAN_POINT('Ctrl Pts',(-20.3583905985793,1.29082576619906,5.3342596657391));
#52222=CARTESIAN_POINT('Ctrl Pts',(-20.1197529334601,-3.78961333343518,
3.96980958274648));
#52223=CARTESIAN_POINT('Ctrl Pts',(-19.8811152683408,-5.38843030706872,
-1.04181388264786));
#52224=CARTESIAN_POINT('Ctrl Pts',(-19.6424776032216,-2.0367479735616,-5.09629424507725));
#52225=CARTESIAN_POINT('Ctrl Pts',(-19.4038399381024,3.18615081025577,-4.46866874522171));
#52226=CARTESIAN_POINT('Ctrl Pts',(-19.1652022729832,5.48184510598211,0.264445786948331));
#52227=CARTESIAN_POINT('Ctrl Pts',(-18.9265646078639,2.74121734639358,4.75460669246635));
#52228=CARTESIAN_POINT('Ctrl Pts',(-18.6879269427447,-2.51784227566918,
4.87657949951273));
#52229=CARTESIAN_POINT('Ctrl Pts',(-18.4492892776255,-5.46369086392892,
0.518304431424697));
#52230=CARTESIAN_POINT('Ctrl Pts',(-18.2106516125063,-3.38989619897094,
-4.31615119063469));
#52231=CARTESIAN_POINT('Ctrl Pts',(-17.972013947387,1.7982894533345,-5.18523985773471));
#52232=CARTESIAN_POINT('Ctrl Pts',(-17.7333762822678,5.33433706441994,-1.29050587885931));
#52233=CARTESIAN_POINT('Ctrl Pts',(-17.4947386171486,3.96958231998011,3.78985138826264));
#52234=CARTESIAN_POINT('Ctrl Pts',(-17.2561009520293,-1.04213701429963,
5.38836782185863));
#52235=CARTESIAN_POINT('Ctrl Pts',(-17.0174632869101,-5.09641637566774,
2.03644235519705));
#52236=CARTESIAN_POINT('Ctrl Pts',(-16.7788256217909,-4.46847767001423,
-3.18641878176725));
#52237=CARTESIAN_POINT('Ctrl Pts',(-16.5401879566717,0.264774521898913,
-5.48182923783365));
#52238=CARTESIAN_POINT('Ctrl Pts',(-16.3015502915525,4.7547710693084,-2.74093221709016));
#52239=CARTESIAN_POINT('Ctrl Pts',(-16.0629126264332,4.87642850071492,2.51813470998477));
#52240=CARTESIAN_POINT('Ctrl Pts',(-15.824274961314,0.517976783740707,5.46372193579801));
#52241=CARTESIAN_POINT('Ctrl Pts',(-15.5856372961948,-4.31635446825496,
3.38963736181178));
#52242=CARTESIAN_POINT('Ctrl Pts',(-15.3469996310756,-5.18513200854378,
-1.79860039869607));
#52243=CARTESIAN_POINT('Ctrl Pts',(-15.1083619659563,-1.29018598687877,
-5.33441444391757));
#52244=CARTESIAN_POINT('Ctrl Pts',(-14.8697243008371,3.7900894294612,-3.9693550429385));
#52245=CARTESIAN_POINT('Ctrl Pts',(-14.6310866357179,5.38830531727106,1.0424601422037));
#52246=CARTESIAN_POINT('Ctrl Pts',(-14.3924489705986,2.03613672950916,5.09653848793067));
#52247=CARTESIAN_POINT('Ctrl Pts',(-14.1538113054794,-3.18668674181981,
4.46828657873739));
#52248=CARTESIAN_POINT('Ctrl Pts',(-13.9151736403602,-5.48181334997165,
-0.265103255897302));
#52249=CARTESIAN_POINT('Ctrl Pts',(-13.6765359752409,-2.74064707792992,
-4.75493542905149));
#52250=CARTESIAN_POINT('Ctrl Pts',(-13.4378983101217,2.51842713524471,-4.87627748438068));
#52251=CARTESIAN_POINT('Ctrl Pts',(-13.1992606450025,5.46375298801868,-0.517649134193991));
#52252=CARTESIAN_POINT('Ctrl Pts',(-12.9606229798833,3.38937851246291,4.31655773035292));
#52253=CARTESIAN_POINT('Ctrl Pts',(-12.721985314764,-1.79891133758957,5.18502414070623));
#52254=CARTESIAN_POINT('Ctrl Pts',(-12.4833476496448,-5.33449180423179,
1.28986609025851));
#52255=CARTESIAN_POINT('Ctrl Pts',(-12.2447099845256,-3.96912775162243,
-3.79032745703001));
#52256=CARTESIAN_POINT('Ctrl Pts',(-12.0060723194064,1.04278326635893,-5.38824279330623));
#52257=CARTESIAN_POINT('Ctrl Pts',(-11.7674346542871,5.0966605818656,-2.03583109649899));
#52258=CARTESIAN_POINT('Ctrl Pts',(-11.5287969891679,4.46809547139186,3.18695469041253));
#52259=CARTESIAN_POINT('Ctrl Pts',(-11.2901593240487,-0.265431988942334,
5.48179744239614));
#52260=CARTESIAN_POINT('Ctrl Pts',(-11.0515216589295,-4.75509977169506,
2.74036192891386));
#52261=CARTESIAN_POINT('Ctrl Pts',(-10.8128839938102,-4.87612645051055,
-2.51871955144797));
#52262=CARTESIAN_POINT('Ctrl Pts',(-10.574246328691,-0.517321482785775,
-5.46378402059077));
#52263=CARTESIAN_POINT('Ctrl Pts',(-10.3356086635718,4.3167609769278,-3.38911965092534));
#52264=CARTESIAN_POINT('Ctrl Pts',(-10.0969709984526,5.18491625422252,1.79922227001388));
#52265=CARTESIAN_POINT('Ctrl Pts',(-9.85833333333333,1.28954618899972,5.33456914536226));
#52266=CARTESIAN_POINT('Ctrl Pts',(-9.61969566821411,-3.79056547096819,
3.96890044603278));
#52267=CARTESIAN_POINT('Ctrl Pts',(-9.38105800309488,-5.38818024996436,
-1.04310638676421));
#52268=CARTESIAN_POINT('Ctrl Pts',(-9.14242033797565,-2.03552545616774,
-5.09678265747193));
#52269=CARTESIAN_POINT('Ctrl Pts',(-8.90378267285643,3.18722262754464,-4.46790434797868));
#52270=CARTESIAN_POINT('Ctrl Pts',(-8.6651450077372,5.48178151510679,0.265760721033513));
#52271=CARTESIAN_POINT('Ctrl Pts',(-8.42650734261798,2.74007677004376,4.7552640972372));
#52272=CARTESIAN_POINT('Ctrl Pts',(-8.18786967749874,-2.51901195859494,
4.87597539910758));
#52273=CARTESIAN_POINT('Ctrl Pts',(-7.94923201237954,-5.46381503351144,
0.516993829512319));
#52274=CARTESIAN_POINT('Ctrl Pts',(-7.71059434726029,-3.38886077720523,
-4.31696420796962));
#52275=CARTESIAN_POINT('Ctrl Pts',(-7.47195668214107,1.7995331959781,-5.18480834911082));
#52276=CARTESIAN_POINT('Ctrl Pts',(-7.23331901702184,5.33464646728914,-1.28922628306928));
#52277=CARTESIAN_POINT('Ctrl Pts',(-6.99468135190262,3.96867312620793,3.79080347120911));
#52278=CARTESIAN_POINT('Ctrl Pts',(-6.75604368678338,-1.04342950349043,
5.38811768737191));
#52279=CARTESIAN_POINT('Ctrl Pts',(-6.51740602166417,-5.09690471461091,
2.03521980827418));
#52280=CARTESIAN_POINT('Ctrl Pts',(-6.27876835654494,-4.467713208764,-3.18749055274999));
#52281=CARTESIAN_POINT('Ctrl Pts',(-6.04013069142571,0.266089452679246,
-5.48176556899668));
#52282=CARTESIAN_POINT('Ctrl Pts',(-5.80149302630648,4.75542840469908,-2.73979159960635));
#52283=CARTESIAN_POINT('Ctrl Pts',(-5.56285536118726,4.87582433205023,2.5193043533937));
#52284=CARTESIAN_POINT('Ctrl Pts',(-5.32421769606802,0.516666170769886,
5.46384603309797));
#52285=CARTESIAN_POINT('Ctrl Pts',(-5.08558003094881,-4.31716741655734,
3.38860187917618));
#52286=CARTESIAN_POINT('Ctrl Pts',(-4.84694236582958,-5.18470043865627,
-1.79984409220056));
#52287=CARTESIAN_POINT('Ctrl Pts',(-4.60830470071034,-1.28890634696599,
-5.3347238147032));
#52288=CARTESIAN_POINT('Ctrl Pts',(-4.36966703559113,3.79104140879587,-3.96844570635655));
#52289=CARTESIAN_POINT('Ctrl Pts',(-4.13102937047189,5.38805519950874,1.04375245184379));
#52290=CARTESIAN_POINT('Ctrl Pts',(-3.89239170535267,2.03491397240924,5.09702706943807));
#52291=CARTESIAN_POINT('Ctrl Pts',(-3.65375404023344,-3.18775811969919,
4.46752144683269));
#52292=CARTESIAN_POINT('Ctrl Pts',(-3.41511637511422,-5.48175026890294,
-0.266417018798925));
#52293=CARTESIAN_POINT('Ctrl Pts',(-3.17647870999499,-2.7395051413334,-4.75559493065073));
#52294=CARTESIAN_POINT('Ctrl Pts',(-2.93784104487577,2.51959428582449,-4.87566895585645));
#52295=CARTESIAN_POINT('Ctrl Pts',(-2.69920337975653,5.4638817225832,-0.516346748639057));
#52296=CARTESIAN_POINT('Ctrl Pts',(-2.46056571463731,3.38833392817308,4.31738642478165));
#52297=CARTESIAN_POINT('Ctrl Pts',(-2.22192804951809,-1.80013762659788,
5.18456214962629));
#52298=CARTESIAN_POINT('Ctrl Pts',(-1.98329038439885,-5.33483445954559,
1.28864468737176));
#52299=CARTESIAN_POINT('Ctrl Pts',(-1.74465271927964,-3.96815431503542,
-3.79139121370463));
#52300=CARTESIAN_POINT('Ctrl Pts',(-1.50601505416041,1.0439526175495,-5.38777791511351));
#52301=CARTESIAN_POINT('Ctrl Pts',(-1.26737738904118,5.09738511987209,-2.03502045294416));
#52302=CARTESIAN_POINT('Ctrl Pts',(-1.02873972392196,4.46687700346276,3.18881740351592));
#52303=CARTESIAN_POINT('Ctrl Pts',(-0.790102058802729,-0.265874035238907,
5.48021323433553));
#52304=CARTESIAN_POINT('Ctrl Pts',(-0.551464393683494,-4.75744712505124,
2.74215692220397));
#52305=CARTESIAN_POINT('Ctrl Pts',(-0.312826728564273,-4.87214411143407,
-2.52568128330601));
#52306=CARTESIAN_POINT('Ctrl Pts',(-0.113962007631581,-1.24846965546114,
-4.96376157560509));
#52307=CARTESIAN_POINT('Ctrl Pts',(0.0451297691145686,1.91119551719046,
-4.43560896973968));
#52308=CARTESIAN_POINT('Ctrl Pts',(0.124675657487644,3.17317635443185,-3.47270950061224));
#52309=CARTESIAN_POINT('Ctrl Pts',(0.164448601674182,3.65041170719118,-2.86454901554259));
#52310=CARTESIAN_POINT('Ctrl Pts',(-29.7394486016742,2.52761008811552,-3.54684587865065));
#52311=CARTESIAN_POINT('Ctrl Pts',(-29.6996756574876,3.11851645239715,-3.12574472608009));
#52312=CARTESIAN_POINT('Ctrl Pts',(-29.6201297691146,4.07604700037463,-1.9842316340791));
#52313=CARTESIAN_POINT('Ctrl Pts',(-29.4610379923684,4.70821035020098,0.955422084332599));
#52314=CARTESIAN_POINT('Ctrl Pts',(-29.2621732714357,2.57930446702286,4.45871287587165));
#52315=CARTESIAN_POINT('Ctrl Pts',(-29.0235356063165,-2.36486757903556,
4.57951285086845));
#52316=CARTESIAN_POINT('Ctrl Pts',(-28.7848979411973,-5.12680154578104,
0.486834481531294));
#52317=CARTESIAN_POINT('Ctrl Pts',(-28.546260276078,-3.18350352009034,-4.04998412230631));
#52318=CARTESIAN_POINT('Ctrl Pts',(-28.3076226109588,1.6871112561347,-4.86759179267321));
#52319=CARTESIAN_POINT('Ctrl Pts',(-28.0689849458396,5.00640601099863,-1.21236534218581));
#52320=CARTESIAN_POINT('Ctrl Pts',(-27.8303472807204,3.72686752876241,3.55625523601567));
#52321=CARTESIAN_POINT('Ctrl Pts',(-27.5917096156011,-0.977006116615824,
5.05787502748919));
#52322=CARTESIAN_POINT('Ctrl Pts',(-27.3530719504819,-4.7830901536011,1.91256654887478));
#52323=CARTESIAN_POINT('Ctrl Pts',(-27.1144342853627,-4.19491506055882,
-2.98980739123073));
#52324=CARTESIAN_POINT('Ctrl Pts',(-26.8757966202435,0.247294810559338,
-5.1453952954096));
#52325=CARTESIAN_POINT('Ctrl Pts',(-26.6371589551242,4.46228166941837,-2.57375000033875));
#52326=CARTESIAN_POINT('Ctrl Pts',(-26.398521290005,4.57766126194414,2.3624615172601));
#52327=CARTESIAN_POINT('Ctrl Pts',(-26.1598836248858,0.487410215497018,
5.12821915499749));
#52328=CARTESIAN_POINT('Ctrl Pts',(-25.9212459597666,-4.05063427769259,
3.1825382547137));
#52329=CARTESIAN_POINT('Ctrl Pts',(-25.6826082946473,-4.86725146393007,
-1.68702693864012));
#52330=CARTESIAN_POINT('Ctrl Pts',(-25.4439706295281,-1.21218968322454,
-5.0066746732594));
#52331=CARTESIAN_POINT('Ctrl Pts',(-25.2053329644089,3.55654361144349,-3.7265521774304));
#52332=CARTESIAN_POINT('Ctrl Pts',(-24.9666952992897,5.05778262729025,0.977256248438136));
#52333=CARTESIAN_POINT('Ctrl Pts',(-24.7280576341704,1.91229732115414,4.78323253901292));
#52334=CARTESIAN_POINT('Ctrl Pts',(-24.4894199690512,-2.99006811912389,
4.19472133001462));
#52335=CARTESIAN_POINT('Ctrl Pts',(-24.250782303932,-5.14537567821884,-0.247595852320659));
#52336=CARTESIAN_POINT('Ctrl Pts',(-24.0121446388127,-2.57348489053941,
-4.46243991986699));
#52337=CARTESIAN_POINT('Ctrl Pts',(-23.7735069736935,2.3627373229194,-4.57751754175089));
#52338=CARTESIAN_POINT('Ctrl Pts',(-23.5348693085743,5.12824769937646,-0.487103748027066));
#52339=CARTESIAN_POINT('Ctrl Pts',(-23.2962316434551,3.18229569229794,4.05082567446672));
#52340=CARTESIAN_POINT('Ctrl Pts',(-23.0575939783358,-1.68731899834989,
4.8671499991618));
#52341=CARTESIAN_POINT('Ctrl Pts',(-22.8189563132166,-5.00674726140177,
1.21188959085538));
#52342=CARTESIAN_POINT('Ctrl Pts',(-22.5803186480974,-3.72633894156846,
-3.55676715726841));
#52343=CARTESIAN_POINT('Ctrl Pts',(-22.3416809829781,0.97755957782614,-5.05772397330915));
#52344=CARTESIAN_POINT('Ctrl Pts',(-22.1030433178589,4.78334719361007,-1.91201049793817));
#52345=CARTESIAN_POINT('Ctrl Pts',(-21.8644056527397,4.19454202102207,2.99031967396282));
#52346=CARTESIAN_POINT('Ctrl Pts',(-21.6257679876205,-0.247904413556711,
5.14536081537106));
#52347=CARTESIAN_POINT('Ctrl Pts',(-21.3871303225013,-4.4625942367424,2.57321728520339));
#52348=CARTESIAN_POINT('Ctrl Pts',(-21.148492657382,-4.57737584582237,-2.36301182492228));
#52349=CARTESIAN_POINT('Ctrl Pts',(-20.9098549922628,-0.486796215745698,
-5.12827689999088));
#52350=CARTESIAN_POINT('Ctrl Pts',(-20.6712173271436,4.05101650290193,-3.18205276698362));
#52351=CARTESIAN_POINT('Ctrl Pts',(-20.4325796620244,4.86704880536236,1.68761086891128));
#52352=CARTESIAN_POINT('Ctrl Pts',(-20.1939419969051,1.21158934385664,5.00681992690976));
#52353=CARTESIAN_POINT('Ctrl Pts',(-19.9553043317859,-3.55699061202287,
3.72612564262527));
#52354=CARTESIAN_POINT('Ctrl Pts',(-19.7166666666667,-5.05766534191731,
-0.977862877818859));
#52355=CARTESIAN_POINT('Ctrl Pts',(-19.4780290015474,-1.91172364660431,
-4.78346184448688));
#52356=CARTESIAN_POINT('Ctrl Pts',(-19.2393913364282,2.99057120698267,-4.19436268992253));
#52357=CARTESIAN_POINT('Ctrl Pts',(-19.000753671309,5.14534593978394,0.248212970242977));
#52358=CARTESIAN_POINT('Ctrl Pts',(-18.7621160061898,2.57294966761094,4.46274853947527));
#52359=CARTESIAN_POINT('Ctrl Pts',(-18.5234783410705,-2.36328631686318,
4.57723413244015));
#52360=CARTESIAN_POINT('Ctrl Pts',(-18.2848406759513,-5.12830608297801,
0.486488682230852));
#52361=CARTESIAN_POINT('Ctrl Pts',(-18.0462030108321,-3.18180982980166,
-4.0512073170384));
#52362=CARTESIAN_POINT('Ctrl Pts',(-17.8075653457129,1.68790273318265,-4.86694759391988));
#52363=CARTESIAN_POINT('Ctrl Pts',(-17.5689276805936,5.00689257452757,-1.21128909257392));
#52364=CARTESIAN_POINT('Ctrl Pts',(-17.3302900154744,3.72591233022232,3.55721405402392));
#52365=CARTESIAN_POINT('Ctrl Pts',(-17.0916523503552,-0.978166174263816,
5.05760669231743));
#52366=CARTESIAN_POINT('Ctrl Pts',(-16.8530146852359,-4.78357647817786,
1.91143678840589));
#52367=CARTESIAN_POINT('Ctrl Pts',(-16.6143770201167,-4.19418334373088,
-2.99082272925335));
#52368=CARTESIAN_POINT('Ctrl Pts',(-16.3757393549975,0.248521526032233,
-5.14533104569049));
#52369=CARTESIAN_POINT('Ctrl Pts',(-16.1371016898783,4.46290282616169,-2.57268204076719));
#52370=CARTESIAN_POINT('Ctrl Pts',(-15.8984640247591,4.57709240259623,2.36356080030613));
#52371=CARTESIAN_POINT('Ctrl Pts',(-15.6598263596398,0.486181146967108,
5.12833524752249));
#52372=CARTESIAN_POINT('Ctrl Pts',(-15.4211886945206,-4.05139811660642,
3.18156688117757));
#52373=CARTESIAN_POINT('Ctrl Pts',(-15.1825510294014,-4.86684636497488,
-1.68819459138417));
#52374=CARTESIAN_POINT('Ctrl Pts',(-14.9439133642821,-1.21098883693528,
-5.00696520413972));
#52375=CARTESIAN_POINT('Ctrl Pts',(-14.7052756991629,3.55743748323268,-3.7256990044204));
#52376=CARTESIAN_POINT('Ctrl Pts',(-14.4666380340437,5.05754802452954,0.978469467191119));
#52377=CARTESIAN_POINT('Ctrl Pts',(-14.2280003689245,1.91114992333367,4.7836910946663));
#52378=CARTESIAN_POINT('Ctrl Pts',(-13.9893627038052,-2.99107424076851,
4.19400398245627));
#52379=CARTESIAN_POINT('Ctrl Pts',(-13.750725038686,-5.1453161330936,-0.248830080927746));
#52380=CARTESIAN_POINT('Ctrl Pts',(-13.5120873735668,-2.57241440467166,
-4.46305709679875));
#52381=CARTESIAN_POINT('Ctrl Pts',(-13.2734497084476,2.3638352752493,-4.57695065629236));
#52382=CARTESIAN_POINT('Ctrl Pts',(-13.0348120433283,5.12836439362466,-0.485873609954974));
#52383=CARTESIAN_POINT('Ctrl Pts',(-12.7961743782091,3.18132392111204,4.05158890160494));
#52384=CARTESIAN_POINT('Ctrl Pts',(-12.5575367130899,-1.68848644351467,
4.86674511852789));
#52385=CARTESIAN_POINT('Ctrl Pts',(-12.3188990479707,-5.00703781574603,
1.21068857694173));
#52386=CARTESIAN_POINT('Ctrl Pts',(-12.0802613828514,-3.72548566522024,
-3.55766089964832));
#52387=CARTESIAN_POINT('Ctrl Pts',(-11.8416237177322,0.978772756599708,
-5.05748933855386));
#52388=CARTESIAN_POINT('Ctrl Pts',(-11.602986052613,4.78380569395181,-1.91086305138862));
#52389=CARTESIAN_POINT('Ctrl Pts',(-11.3643483874938,4.19382460609933,2.99132574152728));
#52390=CARTESIAN_POINT('Ctrl Pts',(-11.1257107223745,-0.249138634928415,
5.14530120199331));
#52391=CARTESIAN_POINT('Ctrl Pts',(-10.8870730572553,-4.46321135138594,
2.57214675932532));
#52392=CARTESIAN_POINT('Ctrl Pts',(-10.6484353921361,-4.57680889352901,
-2.36410974169172));
#52393=CARTESIAN_POINT('Ctrl Pts',(-10.4097977270168,-0.485566071195607,
-5.12839352128436));
#52394=CARTESIAN_POINT('Ctrl Pts',(-10.1711600618976,4.05177967203326,-3.18108094960599));
#52395=CARTESIAN_POINT('Ctrl Pts',(-9.93252239677838,4.86664385457931,1.68877828957306));
#52396=CARTESIAN_POINT('Ctrl Pts',(-9.69388473165916,1.21038831259436,5.00711040934616));
#52397=CARTESIAN_POINT('Ctrl Pts',(-9.45524706653992,-3.55788430327004,
3.72527231262268));
#52398=CARTESIAN_POINT('Ctrl Pts',(-9.21660940142071,-5.0574306343906,-0.979076042488542));
#52399=CARTESIAN_POINT('Ctrl Pts',(-8.97797173630147,-1.91057617257191,
-4.78392027603378));
#52400=CARTESIAN_POINT('Ctrl Pts',(-8.73933407118225,2.99157723152894,-4.19364521466106));
#52401=CARTESIAN_POINT('Ctrl Pts',(-8.50069640606303,5.14528625238931,0.249447188033793));
#52402=CARTESIAN_POINT('Ctrl Pts',(-8.26205874094379,2.57187910472981,4.46336558992145));
#52403=CARTESIAN_POINT('Ctrl Pts',(-8.02342107582458,-2.36438419963377,
4.57666711430907));
#52404=CARTESIAN_POINT('Ctrl Pts',(-7.78478341070534,-5.12842263049894,
0.485258530685497));
#52405=CARTESIAN_POINT('Ctrl Pts',(-7.54614574558613,-3.18083796666522,
-4.051970427882));
#52406=CARTESIAN_POINT('Ctrl Pts',(-7.30750808046688,1.68907012956793,-4.86654257314621));
#52407=CARTESIAN_POINT('Ctrl Pts',(-7.06887041534768,5.00718298492152,-1.21008804386212));
#52408=CARTESIAN_POINT('Ctrl Pts',(-6.83023275022843,3.72505894666373,3.55810769403531));
#52409=CARTESIAN_POINT('Ctrl Pts',(-6.59159508510922,-0.979379324924138,
5.05737191215842));
#52410=CARTESIAN_POINT('Ctrl Pts',(-6.35295741998998,-4.78403484078203,
1.91028928665709));
#52411=CARTESIAN_POINT('Ctrl Pts',(-6.11431975487076,-4.19346580839123,
-2.99182871033596));
#52412=CARTESIAN_POINT('Ctrl Pts',(-5.87568208975153,0.24975574072106,-5.14527128511983));
#52413=CARTESIAN_POINT('Ctrl Pts',(-5.63704442463231,4.46351981148654,-2.57161143927705));
#52414=CARTESIAN_POINT('Ctrl Pts',(-5.39840675951308,4.57652532039568,2.3646586459856));
#52415=CARTESIAN_POINT('Ctrl Pts',(-5.15976909439384,0.48495098504212,5.12845172719788));
#52416=CARTESIAN_POINT('Ctrl Pts',(-4.92113142927463,-4.05216116265496,
3.18059496090769));
#52417=CARTESIAN_POINT('Ctrl Pts',(-4.68249376415541,-4.86644128669823,
-1.68936194164671));
#52418=CARTESIAN_POINT('Ctrl Pts',(-4.44385609903616,-1.20978774680917,
-5.00725558441954));
#52419=CARTESIAN_POINT('Ctrl Pts',(-4.20521843391696,3.55833102599239,-3.72484548681831));
#52420=CARTESIAN_POINT('Ctrl Pts',(-3.96658076879771,5.05731326006834,0.97968244932232));
#52421=CARTESIAN_POINT('Ctrl Pts',(-3.7279431036785,1.91000222430937,4.78414968494508));
#52422=CARTESIAN_POINT('Ctrl Pts',(-3.48930543855926,-2.99207985287812,
4.1932858176298));
#52423=CARTESIAN_POINT('Ctrl Pts',(-3.25066777344004,-5.14525692421147,
-0.250063199427267));
#52424=CARTESIAN_POINT('Ctrl Pts',(-3.01203010832081,-2.57134256504161,
-4.46367611536099));
#52425=CARTESIAN_POINT('Ctrl Pts',(-2.77339244320159,2.36493078112016,-4.57637948185914));
#52426=CARTESIAN_POINT('Ctrl Pts',(-2.53475477808235,5.12848522590942,-0.484651170411792));
#52427=CARTESIAN_POINT('Ctrl Pts',(-2.29611711296313,3.1803434578865,4.05236672721506));
#52428=CARTESIAN_POINT('Ctrl Pts',(-2.0574794478439,-1.68963745764365,4.86631148644208));
#52429=CARTESIAN_POINT('Ctrl Pts',(-1.81884178272468,-5.00735943740691,
1.20954214900319));
#52430=CARTESIAN_POINT('Ctrl Pts',(-1.58020411760546,-3.72457198234636,
-3.55865935837542));
#52431=CARTESIAN_POINT('Ctrl Pts',(-1.34156645248623,0.979870327998434,
-5.05705299657864));
#52432=CARTESIAN_POINT('Ctrl Pts',(-1.102928787367,4.78448575670765,-1.91010216861234));
#52433=CARTESIAN_POINT('Ctrl Pts',(-0.86429112224778,4.19268093295817,2.99307411331055));
#52434=CARTESIAN_POINT('Ctrl Pts',(-0.62565345712855,-0.24955354652721,
5.14381423941869));
#52435=CARTESIAN_POINT('Ctrl Pts',(-0.387015792009318,-4.46541461412448,
2.57383156822791));
#52436=CARTESIAN_POINT('Ctrl Pts',(-0.148378126890095,-4.57307100750672,
-2.37064413258696));
#52437=CARTESIAN_POINT('Ctrl Pts',(0.050486594042596,-1.17183323287632,
-4.6590645987469));
#52438=CARTESIAN_POINT('Ctrl Pts',(0.209578370788747,1.79387813854466,-4.16333226526479));
#52439=CARTESIAN_POINT('Ctrl Pts',(0.289124259161822,2.9783931789093,-3.25953969577237));
#52440=CARTESIAN_POINT('Ctrl Pts',(0.32889720334836,3.42633377868325,-2.68871070989398));
#52441=CARTESIAN_POINT('Ctrl Pts',(-29.575,2.36230756092324,-3.31488661006752));
#52442=CARTESIAN_POINT('Ctrl Pts',(-29.5352270558135,2.91456939066647,-2.92132494432319));
#52443=CARTESIAN_POINT('Ctrl Pts',(-29.4556811674404,3.80947864266608,-1.85446537575054));
#52444=CARTESIAN_POINT('Ctrl Pts',(-29.2965893906943,4.40029930288375,0.892938679230673));
#52445=CARTESIAN_POINT('Ctrl Pts',(-29.0977246697615,2.41062119233501,4.16711865021482));
#52446=CARTESIAN_POINT('Ctrl Pts',(-28.8590870046423,-2.21020820766824,
4.28001845847083));
#52447=CARTESIAN_POINT('Ctrl Pts',(-28.6204493395231,-4.79151515967436,
0.454996117497237));
#52448=CARTESIAN_POINT('Ctrl Pts',(-28.3818116744039,-2.97530638570203,
-3.7851202441102));
#52449=CARTESIAN_POINT('Ctrl Pts',(-28.1431740092847,1.57677629758835,-4.54925739906848));
#52450=CARTESIAN_POINT('Ctrl Pts',(-27.9045363441654,4.67899334175034,-1.13307817052668));
#52451=CARTESIAN_POINT('Ctrl Pts',(-27.6658986790463,3.48313507021902,3.32368060727122));
#52452=CARTESIAN_POINT('Ctrl Pts',(-27.4272610139269,-0.913111142894123,
4.72709634916456));
#52453=CARTESIAN_POINT('Ctrl Pts',(-27.1886233488078,-4.47028206112812,
1.78748709716699));
#52454=CARTESIAN_POINT('Ctrl Pts',(-26.9499856836885,-3.92057288091334,
-2.79427774054909));
#52455=CARTESIAN_POINT('Ctrl Pts',(-26.7113480185693,0.231122040344854,
-4.80889290141546));
#52456=CARTESIAN_POINT('Ctrl Pts',(-26.4727103534501,4.17045404914302,-2.40542998080026));
#52457=CARTESIAN_POINT('Ctrl Pts',(-26.2340726883308,4.27828796113812,2.20795949931288));
#52458=CARTESIAN_POINT('Ctrl Pts',(-25.9954350232116,0.45553419918425,4.79284005902739));
#52459=CARTESIAN_POINT('Ctrl Pts',(-25.7567973580924,-3.78572788015027,
2.97440424746946));
#52460=CARTESIAN_POINT('Ctrl Pts',(-25.5181596929732,-4.54893932739796,
-1.57669749435209));
#52461=CARTESIAN_POINT('Ctrl Pts',(-25.2795220278539,-1.132913999441,-4.67924443383647));
#52462=CARTESIAN_POINT('Ctrl Pts',(-25.0408843627347,3.32395012330801,-3.48284034246832));
#52463=CARTESIAN_POINT('Ctrl Pts',(-24.8022466976155,4.72700999182265,0.913344916409211));
#52464=CARTESIAN_POINT('Ctrl Pts',(-24.5636090324962,1.78723547660136,4.47041513471273));
#52465=CARTESIAN_POINT('Ctrl Pts',(-24.324971367377,-2.7945214171653,3.92039182010356));
#52466=CARTESIAN_POINT('Ctrl Pts',(-24.0863337022578,-4.80887456716434,
-0.231403394352836));
#52467=CARTESIAN_POINT('Ctrl Pts',(-23.8476960371386,-2.40518220884904,
-4.17060195021093));
#52468=CARTESIAN_POINT('Ctrl Pts',(-23.6090583720194,2.20821726762825,-4.27815364006511));
#52469=CARTESIAN_POINT('Ctrl Pts',(-23.3704207069001,4.7928667366398,-0.455247774302161));
#52470=CARTESIAN_POINT('Ctrl Pts',(-23.1317830417809,2.97417754833123,3.7859067598156));
#52471=CARTESIAN_POINT('Ctrl Pts',(-22.8931453766616,-1.57697045372341,
4.54884449829819));
#52472=CARTESIAN_POINT('Ctrl Pts',(-22.6545077115425,-4.67931227480544,
1.13263353273611));
#52473=CARTESIAN_POINT('Ctrl Pts',(-22.4158700464232,-3.48264105196409,
-3.32415904951658));
#52474=CARTESIAN_POINT('Ctrl Pts',(-22.177232381304,0.913628408435968,-4.7269551737383));
#52475=CARTESIAN_POINT('Ctrl Pts',(-21.9385947161847,4.47052229104313,-1.7869674112637));
#52476=CARTESIAN_POINT('Ctrl Pts',(-21.6999570510656,3.92022423769407,2.79475652063351));
#52477=CARTESIAN_POINT('Ctrl Pts',(-21.4613193859463,-0.231691776071347,
4.80886067632815));
#52478=CARTESIAN_POINT('Ctrl Pts',(-21.2226817208271,-4.17074617495639,
2.40493210456611));
#52479=CARTESIAN_POINT('Ctrl Pts',(-20.9840440557078,-4.27802121087247,
-2.20847381754468));
#52480=CARTESIAN_POINT('Ctrl Pts',(-20.7454063905886,-0.454960354245989,
-4.79289402757069));
#52481=CARTESIAN_POINT('Ctrl Pts',(-20.5067687254694,3.78608510831067,-2.97395051002756));
#52482=CARTESIAN_POINT('Ctrl Pts',(-20.2681310603502,4.54874992244621,1.57724323631644));
#52483=CARTESIAN_POINT('Ctrl Pts',(-20.0294933952309,1.13235292151423,4.67938018808041));
#52484=CARTESIAN_POINT('Ctrl Pts',(-19.7908557301117,-3.32436789061056,
3.48244170250407));
#52485=CARTESIAN_POINT('Ctrl Pts',(-19.5522180649925,-4.7269003767659,-0.91391187298986));
#52486=CARTESIAN_POINT('Ctrl Pts',(-19.3135803998733,-1.78669931964703,
-4.4706294438965));
#52487=CARTESIAN_POINT('Ctrl Pts',(-19.074942734754,2.79499160370957,-3.92005663462335));
#52488=CARTESIAN_POINT('Ctrl Pts',(-18.8363050696348,4.80884677358576,0.231980153537627));
#52489=CARTESIAN_POINT('Ctrl Pts',(-18.5976674045156,2.4046819888283,4.1708903864842));
#52490=CARTESIAN_POINT('Ctrl Pts',(-18.3590297393964,-2.20873035805718,
4.27788876536757));
#52491=CARTESIAN_POINT('Ctrl Pts',(-18.1203920742771,-4.79292130202709,
0.454672933037013));
#52492=CARTESIAN_POINT('Ctrl Pts',(-17.8817544091579,-2.97372346063237,
-3.78626344344212));
#52493=CARTESIAN_POINT('Ctrl Pts',(-17.6431167440387,1.5775160130308,-4.54865533010503));
#52494=CARTESIAN_POINT('Ctrl Pts',(-17.4044790789195,4.6794480846352,-1.13207230628853));
#52495=CARTESIAN_POINT('Ctrl Pts',(-17.1658414138002,3.48224234046452,3.3245767197852));
#52496=CARTESIAN_POINT('Ctrl Pts',(-16.927203748681,-0.914195334228,4.72684556277623));
#52497=CARTESIAN_POINT('Ctrl Pts',(-16.6885660835618,-4.47073658068798,
1.78643122161473));
#52498=CARTESIAN_POINT('Ctrl Pts',(-16.4499284184426,-3.91988901744752,
-2.79522667673945));
#52499=CARTESIAN_POINT('Ctrl Pts',(-16.2112907533233,0.232268530165553,
-4.80883285354733));
#52500=CARTESIAN_POINT('Ctrl Pts',(-15.9726530882041,4.17103458301497,-2.40443186444421));
#52501=CARTESIAN_POINT('Ctrl Pts',(-15.7340154230849,4.27775630447756,2.20898689062749));
#52502=CARTESIAN_POINT('Ctrl Pts',(-15.4953777579657,0.454385510193501,
4.79294855924697));
#52503=CARTESIAN_POINT('Ctrl Pts',(-15.2567400928464,-3.78644176495787,
2.97349640054336));
#52504=CARTESIAN_POINT('Ctrl Pts',(-15.0181024277272,-4.54856072140599,
-1.57778878407227));
#52505=CARTESIAN_POINT('Ctrl Pts',(-14.7794647626079,-1.13179168699179,
-4.67951596436188));
#52506=CARTESIAN_POINT('Ctrl Pts',(-14.5408270974888,3.32478553700414,-3.48204296590229));
#52507=CARTESIAN_POINT('Ctrl Pts',(-14.3021894323695,4.72679073178803,0.914478792178541));
#52508=CARTESIAN_POINT('Ctrl Pts',(-14.0635517672503,1.78616311715816,4.47084370140194));
#52509=CARTESIAN_POINT('Ctrl Pts',(-13.8249141021311,-2.79546173971721,
3.91972138617514));
#52510=CARTESIAN_POINT('Ctrl Pts',(-13.5862764370118,-4.80881891621556,
-0.232556905958181));
#52511=CARTESIAN_POINT('Ctrl Pts',(-13.3476387718926,-2.40418173141341,
-4.17117876454601));
#52512=CARTESIAN_POINT('Ctrl Pts',(-13.1090011067734,2.20924341525388,-4.27762382820403));
#52513=CARTESIAN_POINT('Ctrl Pts',(-12.8703634416541,4.79297579923065,-0.454098085715957));
#52514=CARTESIAN_POINT('Ctrl Pts',(-12.6317257765349,2.97326932976115,3.78662007285696));
#52515=CARTESIAN_POINT('Ctrl Pts',(-12.3930881114157,-1.57806154943975,
4.54846609634954));
#52516=CARTESIAN_POINT('Ctrl Pts',(-12.1544504462965,-4.67958382726028,
1.13151106362493));
#52517=CARTESIAN_POINT('Ctrl Pts',(-11.9158127811773,-3.48184357881804,
-3.32499434226663));
#52518=CARTESIAN_POINT('Ctrl Pts',(-11.677175116058,0.914762246840484,-4.7267358838015));
#52519=CARTESIAN_POINT('Ctrl Pts',(-11.4385374509388,4.47095080603802,-1.78589500627826));
#52520=CARTESIAN_POINT('Ctrl Pts',(-11.1998997858196,3.91955374080681,2.79569679264203));
#52521=CARTESIAN_POINT('Ctrl Pts',(-10.9612621207003,-0.232845280914501,
4.80880496159049));
#52522=CARTESIAN_POINT('Ctrl Pts',(-10.7226244555811,-4.17132293107681,
2.40393158973677));
#52523=CARTESIAN_POINT('Ctrl Pts',(-10.4839867904619,-4.27749133654748,
-2.20949993193547));
#52524=CARTESIAN_POINT('Ctrl Pts',(-10.2453491253427,-0.453810659605433,
-4.79300302197796));
#52525=CARTESIAN_POINT('Ctrl Pts',(-10.0067114602234,3.78679836713871,-2.97304224828663));
#52526=CARTESIAN_POINT('Ctrl Pts',(-9.76807379510421,4.54837145493611,1.57833430913225));
#52527=CARTESIAN_POINT('Ctrl Pts',(-9.52943612998497,1.131230436189,4.67965167333008));
#52528=CARTESIAN_POINT('Ctrl Pts',(-9.29079846486575,-3.3252031355719,3.48164417921258));
#52529=CARTESIAN_POINT('Ctrl Pts',(-9.05216079974653,-4.72668101881683,
-0.915045698212859));
#52530=CARTESIAN_POINT('Ctrl Pts',(-8.8135231346273,-1.78562688897607,-4.47105789459565));
#52531=CARTESIAN_POINT('Ctrl Pts',(-8.57488546950807,2.79593183551325,-3.91938608134342));
#52532=CARTESIAN_POINT('Ctrl Pts',(-8.33624780438884,4.80879098967182,0.233133655034067));
#52533=CARTESIAN_POINT('Ctrl Pts',(-8.09761013926962,2.40368143941586,4.17146708260569));
#52534=CARTESIAN_POINT('Ctrl Pts',(-7.85897247415039,-2.20975644067261,
4.27735882951057));
#52535=CARTESIAN_POINT('Ctrl Pts',(-7.62033480903117,-4.79303022748644,
0.453523231858677));
#52536=CARTESIAN_POINT('Ctrl Pts',(-7.38169714391193,-2.97281515612521,
-3.78697664779438));
#52537=CARTESIAN_POINT('Ctrl Pts',(-7.14305947879272,1.57860706315775,-4.5482767971816));
#52538=CARTESIAN_POINT('Ctrl Pts',(-6.90442181367349,4.6797195025539,-1.13094980465497));
#52539=CARTESIAN_POINT('Ctrl Pts',(-6.66578414855425,3.48144476711953,3.32541191686152));
#52540=CARTESIAN_POINT('Ctrl Pts',(-6.42714648343504,-0.91532914635784,
4.72662613694493));
#52541=CARTESIAN_POINT('Ctrl Pts',(-6.1885088183158,-4.47116496695316,1.78535876503999));
#52542=CARTESIAN_POINT('Ctrl Pts',(-5.94987115319659,-3.91921840801846,
-2.79616686792193));
#52543=CARTESIAN_POINT('Ctrl Pts',(-5.71123348807733,0.233422028762872,
-4.80877700124299));
#52544=CARTESIAN_POINT('Ctrl Pts',(-5.47259582295814,4.171611218274,-2.40343127894775));
#52545=CARTESIAN_POINT('Ctrl Pts',(-5.23395815783889,4.27722630874114,2.21001293857749));
#52546=CARTESIAN_POINT('Ctrl Pts',(-4.99532049271968,0.453235799314355,
4.7930574212978));
#52547=CARTESIAN_POINT('Ctrl Pts',(-4.75668282760044,-3.7871549087526,2.97258804263921));
#52548=CARTESIAN_POINT('Ctrl Pts',(-4.51804516248123,-4.54818213474018,
-1.57887979109285));
#52549=CARTESIAN_POINT('Ctrl Pts',(-4.27940749736198,-1.13066914665236,
-4.67978735413588));
#52550=CARTESIAN_POINT('Ctrl Pts',(-4.04076983224278,3.32562064318893,-3.48124526728007));
#52551=CARTESIAN_POINT('Ctrl Pts',(-3.80213216712354,4.72657132062792,0.915612446800854));
#52552=CARTESIAN_POINT('Ctrl Pts',(-3.56349450200431,1.78509047620951,4.4712723004521));
#52553=CARTESIAN_POINT('Ctrl Pts',(-3.32485683688509,-2.79640158605707,
3.91905018842691));
#52554=CARTESIAN_POINT('Ctrl Pts',(-3.08621917176585,-4.80876357952,-0.233709380055606));
#52555=CARTESIAN_POINT('Ctrl Pts',(-2.84758150664664,-2.40317998874982,
-4.17175730007125));
#52556=CARTESIAN_POINT('Ctrl Pts',(-2.60894384152741,2.21026727641583,-4.27709000786183));
#52557=CARTESIAN_POINT('Ctrl Pts',(-2.37030617640818,4.79308872923565,-0.452955592184536));
#52558=CARTESIAN_POINT('Ctrl Pts',(-2.13166851128895,2.97235298759993,3.78734702964848));
#52559=CARTESIAN_POINT('Ctrl Pts',(-1.89303084616973,-1.57913728868941,
4.54806082325786));
#52560=CARTESIAN_POINT('Ctrl Pts',(-1.6543931810505,-4.67988441526822,1.13043961063463));
#52561=CARTESIAN_POINT('Ctrl Pts',(-1.41575551593128,-3.4809896496573,-3.32592750304621));
#52562=CARTESIAN_POINT('Ctrl Pts',(-1.17711785081205,0.915788038447374,
-4.72632807804377));
#52563=CARTESIAN_POINT('Ctrl Pts',(-0.938480185692821,4.47158639354322,
-1.78518388428051));
#52564=CARTESIAN_POINT('Ctrl Pts',(-0.699842520573601,3.91848486245357,
2.79733082310517));
#52565=CARTESIAN_POINT('Ctrl Pts',(-0.461204855454373,-0.233233057815519,
4.80741524450186));
#52566=CARTESIAN_POINT('Ctrl Pts',(-0.222567190335139,-4.17338210319771,
2.40550621425186));
#52567=CARTESIAN_POINT('Ctrl Pts',(0.0160704747840829,-4.27399790357938,
-2.21560698186791));
#52568=CARTESIAN_POINT('Ctrl Pts',(0.214935195716774,-1.0951968102915,-4.35436762188871));
#52569=CARTESIAN_POINT('Ctrl Pts',(0.374026972462925,1.67656075989886,-3.8910555607899));
#52570=CARTESIAN_POINT('Ctrl Pts',(0.453572860836,2.78361000338674,-3.0463698909325));
#52571=CARTESIAN_POINT('Ctrl Pts',(0.493345805022538,3.20225585017532,-2.51287240424537));
#52572=CARTESIAN_POINT('',(4.44089209850063E-15,3.87448963569911,-3.0403873211912));
#52573=CARTESIAN_POINT('Ctrl Pts',(1.88737914186277E-15,-3.73764785372982,
-1.62671566533137));
#52574=CARTESIAN_POINT('Ctrl Pts',(2.39994637830129E-15,-3.71028158849173,
-1.71435575517499));
#52575=CARTESIAN_POINT('Ctrl Pts',(-1.76827187884598E-15,-3.67981086869404,
-1.80083539107987));
#52576=CARTESIAN_POINT('Ctrl Pts',(-3.27515792264421E-15,-3.64623269726973,
-1.88598270617316));
#52577=CARTESIAN_POINT('Ctrl Pts',(-5.28932042256129E-15,-3.60128953503947,
-1.99994929319637));
#52578=CARTESIAN_POINT('Ctrl Pts',(4.56536624768121E-15,-3.55078180752455,
-2.11152991672815));
#52579=CARTESIAN_POINT('Ctrl Pts',(6.43929354282591E-15,-3.49508775615109,
-2.22055078808827));
#52580=CARTESIAN_POINT('Ctrl Pts',(7.69212451415013E-15,-3.45785299647819,
-2.29343767356915));
#52581=CARTESIAN_POINT('Ctrl Pts',(-5.3505723180461E-15,-3.41829895641058,
-2.36518031524366));
#52582=CARTESIAN_POINT('Ctrl Pts',(-5.38458166943201E-15,-3.3765261879658,
-2.43572396492932));
#52583=CARTESIAN_POINT('Ctrl Pts',(-5.40384490325929E-15,-3.35286567774219,
-2.47568058755071));
#52584=CARTESIAN_POINT('Ctrl Pts',(-3.07309964203322E-15,-3.3284931802157,
-2.51525250052437));
#52585=CARTESIAN_POINT('Ctrl Pts',(-2.55351295663786E-15,-3.30342567080822,
-2.55442929399667));
#52586=CARTESIAN_POINT('Ctrl Pts',(-2.21585161566373E-15,-3.28713516706875,
-2.57988893141763));
#52587=CARTESIAN_POINT('Ctrl Pts',(-1.73369067459434E-14,-3.27054786797816,
-2.60518633230089));
#52588=CARTESIAN_POINT('Ctrl Pts',(-1.69309011255336E-14,-3.25368678771015,
-2.63029154815235));
#52589=CARTESIAN_POINT('Ctrl Pts',(-1.52366107287811E-14,-3.18332429778173,
-2.73505740356734));
#52590=CARTESIAN_POINT('Ctrl Pts',(-7.85431309872848E-15,-3.10815120519487,
-2.83655470454748));
#52591=CARTESIAN_POINT('Ctrl Pts',(-5.77315972805081E-15,-3.02856012624411,
-2.93460023723518));
#52592=CARTESIAN_POINT('Ctrl Pts',(-3.65120770442108E-15,-2.94740875440291,
-3.03456784146166));
#52593=CARTESIAN_POINT('Ctrl Pts',(-1.10974998716751E-14,-2.86166412082263,
-3.13094761193651));
#52594=CARTESIAN_POINT('Ctrl Pts',(-1.03805852802452E-14,-2.77169173795742,
-3.2235279094873));
#52595=CARTESIAN_POINT('Ctrl Pts',(-1.00669351464947E-14,-2.73232882045389,
-3.26403178966576));
#52596=CARTESIAN_POINT('Ctrl Pts',(1.1368289068979E-15,-2.69215607320333,
-3.30380815052698));
#52597=CARTESIAN_POINT('Ctrl Pts',(1.60982338570648E-15,-2.65120142765904,
-3.34283779060884));
#52598=CARTESIAN_POINT('Ctrl Pts',(1.85310027956541E-15,-2.63013708250599,
-3.36291204101334));
#52599=CARTESIAN_POINT('Ctrl Pts',(-2.39183766274509E-15,-2.60886587002882,
-3.38278873840918));
#52600=CARTESIAN_POINT('Ctrl Pts',(-1.77635683940025E-15,-2.58739143950339,
-3.40246515988401));
#52601=CARTESIAN_POINT('Ctrl Pts',(-1.21194577917492E-15,-2.56769885828742,
-3.42050892255673));
#52602=CARTESIAN_POINT('Ctrl Pts',(3.20395462986166E-15,-2.54783172387995,
-3.43838737529476));
#52603=CARTESIAN_POINT('Ctrl Pts',(2.72004641033163E-15,-2.52781546097606,
-3.45607868380752));
#52604=CARTESIAN_POINT('Ctrl Pts',(3.24874263539825E-16,-2.42874213786364,
-3.54364431646243));
#52605=CARTESIAN_POINT('Ctrl Pts',(-1.42112367967504E-14,-2.32592759453929,
-3.6267135247425));
#52606=CARTESIAN_POINT('Ctrl Pts',(-1.0991207943789E-14,-2.21978207787836,
-3.70509096548934));
#52607=CARTESIAN_POINT('Ctrl Pts',(-7.72550104896222E-15,-2.11213082335754,
-3.78458023727349));
#52608=CARTESIAN_POINT('Ctrl Pts',(3.10559049872635E-15,-2.00105292688667,
-3.85924433374753));
#52609=CARTESIAN_POINT('Ctrl Pts',(2.60902410786912E-15,-1.88692876195011,
-3.9288546438315));
#52610=CARTESIAN_POINT('Ctrl Pts',(2.11296027189519E-15,-1.77292009749333,
-3.99839450411882));
#52611=CARTESIAN_POINT('Ctrl Pts',(-1.19023239270618E-14,-1.65587069894074,
-4.06289140983169));
#52612=CARTESIAN_POINT('Ctrl Pts',(-1.44884104713583E-14,-1.53612127914559,
-4.12208347067618));
#52613=CARTESIAN_POINT('Ctrl Pts',(-1.63872008747819E-14,-1.44819728850264,
-4.16554424245053));
#52614=CARTESIAN_POINT('Ctrl Pts',(1.48322560200536E-15,-1.358816881025,
-4.20614452293028));
#52615=CARTESIAN_POINT('Ctrl Pts',(1.77635683940025E-15,-1.26810467560363,
-4.24376604966189));
#52616=CARTESIAN_POINT('Ctrl Pts',(1.89986052924058E-15,-1.22988530266112,
-4.25961696139028));
#52617=CARTESIAN_POINT('Ctrl Pts',(-6.83825980710587E-15,-1.19142942418558,
-4.27493893402116));
#52618=CARTESIAN_POINT('Ctrl Pts',(-6.77236045021345E-15,-1.15274600094195,
-4.28972236344086));
#52619=CARTESIAN_POINT('Ctrl Pts',(-6.73168489219131E-15,-1.1288691393026,
-4.29884725129232));
#52620=CARTESIAN_POINT('Ctrl Pts',(-6.80830697204428E-15,-1.10490022885304,
-4.30776879683175));
#52621=CARTESIAN_POINT('Ctrl Pts',(-6.55031584528842E-15,-1.08087218884353,
-4.31647376695309));
#52622=CARTESIAN_POINT('Ctrl Pts',(-5.15864969987438E-15,-0.951259165936978,
-4.36343046801116));
#52623=CARTESIAN_POINT('Ctrl Pts',(-9.14651306628698E-15,-0.819788429412977,
-4.4041447952911));
#52624=CARTESIAN_POINT('Ctrl Pts',(-7.49400541621981E-15,-0.686853690194028,
-4.43838432887677));
#52625=CARTESIAN_POINT('Ctrl Pts',(-6.41519723636329E-15,-0.600069774821131,
-4.46073695696003));
#52626=CARTESIAN_POINT('Ctrl Pts',(3.08265417366316E-15,-0.512661063187981,
-4.48032944741841));
#52627=CARTESIAN_POINT('Ctrl Pts',(2.72004641033163E-15,-0.424729285070971,
-4.49708803736938));
#52628=CARTESIAN_POINT('Ctrl Pts',(2.21027954554588E-15,-0.294380989358742,
-4.52193063336172));
#52629=CARTESIAN_POINT('Ctrl Pts',(-6.11319286711368E-15,-0.162884046650897,
-4.54054853308582));
#52630=CARTESIAN_POINT('Ctrl Pts',(-6.85562717706034E-15,-0.0306517464005833,
-4.55312130983207));
#52631=CARTESIAN_POINT('Ctrl Pts',(-7.61000109133581E-15,0.103707073763108,
-4.5658962781765));
#52632=CARTESIAN_POINT('Ctrl Pts',(-1.63497112532693E-15,0.238825822812114,
-4.57243019189283));
#52633=CARTESIAN_POINT('Ctrl Pts',(-2.63677968348475E-15,0.374285930049112,
-4.57285970409636));
#52634=CARTESIAN_POINT('Ctrl Pts',(-3.1179292879162E-15,0.439344844232451,
-4.57306599064198));
#52635=CARTESIAN_POINT('Ctrl Pts',(-1.01815445406519E-14,0.504482649963796,
-4.57186341188294));
#52636=CARTESIAN_POINT('Ctrl Pts',(-1.13242748511766E-14,0.56965339169973,
-4.56926290729125));
#52637=CARTESIAN_POINT('Ctrl Pts',(-1.17607086462203E-14,0.594543528838534,
-4.56826971749176));
#52638=CARTESIAN_POINT('Ctrl Pts',(-1.64394877692331E-14,0.619443271976647,
-4.56707223758195));
#52639=CARTESIAN_POINT('Ctrl Pts',(-1.64868119156836E-14,0.644320150574942,
-4.56567290865878));
#52640=CARTESIAN_POINT('Ctrl Pts',(-1.6747057075368E-14,0.78112319360564,
-4.55797771273081));
#52641=CARTESIAN_POINT('Ctrl Pts',(-4.80959600169574E-15,0.917388398723616,
-4.5441785389719));
#52642=CARTESIAN_POINT('Ctrl Pts',(-3.30291349825984E-15,1.05267829205595,
-4.52449336420144));
#52643=CARTESIAN_POINT('Ctrl Pts',(-1.76031124497757E-15,1.19119353586137,
-4.50433888912928));
#52644=CARTESIAN_POINT('Ctrl Pts',(-9.24810924555582E-15,1.32868716814533,
-4.47801451299053));
#52645=CARTESIAN_POINT('Ctrl Pts',(-6.0507154842071E-15,1.46470504959221,
-4.44570106748648));
#52646=CARTESIAN_POINT('Ctrl Pts',(-2.89585376704057E-15,1.59891360789184,
-4.41381745859138));
#52647=CARTESIAN_POINT('Ctrl Pts',(-2.10645447082242E-15,1.73168624049081,
-4.37610283665406));
#52648=CARTESIAN_POINT('Ctrl Pts',(-1.09634523681734E-15,1.862589475375,
-4.33268125614708));
#52649=CARTESIAN_POINT('Ctrl Pts',(-3.74816430711647E-16,1.9581841340492,
-4.30097179402927));
#52650=CARTESIAN_POINT('Ctrl Pts',(3.02205267408009E-15,2.05278195326171,
-4.26621781290806));
#52651=CARTESIAN_POINT('Ctrl Pts',(4.16333634234434E-15,2.14626801492587,
-4.22848555519344));
#52652=CARTESIAN_POINT('Ctrl Pts',(4.68860356446466E-15,2.18929427148484,
-4.21111956745068));
#52653=CARTESIAN_POINT('Ctrl Pts',(1.11734467368341E-15,2.23208498079157,
-4.19312252578931));
#52654=CARTESIAN_POINT('Ctrl Pts',(1.17961196366423E-15,2.27462862144891,
-4.17449995562647));
#52655=CARTESIAN_POINT('Ctrl Pts',(1.21298692846241E-15,2.29743180607061,
-4.16451834852861));
#52656=CARTESIAN_POINT('Ctrl Pts',(2.69478357067603E-15,2.32016400623282,
-4.15435702299221));
#52657=CARTESIAN_POINT('Ctrl Pts',(2.692290834716E-15,2.34282341818224,
-4.14401676235655));
#52658=CARTESIAN_POINT('Ctrl Pts',(2.69032939972027E-15,2.36065321014296,
-4.13588042164457));
#52659=CARTESIAN_POINT('Ctrl Pts',(-1.13007804132127E-14,2.37843876952637,
-4.12763283650539));
#52660=CARTESIAN_POINT('Ctrl Pts',(-1.09495745803656E-14,2.39616405253862,
-4.11928169694977));
#52661=CARTESIAN_POINT('Ctrl Pts',(-8.39698482786046E-15,2.52499270954159,
-4.05858500214088));
#52662=CARTESIAN_POINT('Ctrl Pts',(1.60026416366889E-15,2.6508256133944,
-3.99233766103874));
#52663=CARTESIAN_POINT('Ctrl Pts',(1.87350135405495E-15,2.77336570632561,
-3.92081240446126));
#52664=CARTESIAN_POINT('Ctrl Pts',(2.15041244287694E-15,2.89755345144912,
-3.84832543206502));
#52665=CARTESIAN_POINT('Ctrl Pts',(-2.86602714926484E-15,3.01835993446049,
-3.77041749676129));
#52666=CARTESIAN_POINT('Ctrl Pts',(-2.33146835171283E-15,3.13546816361818,
-3.68731987875136));
#52667=CARTESIAN_POINT('Ctrl Pts',(-1.79739883395837E-15,3.25246920402336,
-3.60429831970052));
#52668=CARTESIAN_POINT('Ctrl Pts',(-1.49727946848197E-15,3.3657794534396,
-3.51609628762174));
#52669=CARTESIAN_POINT('Ctrl Pts',(-1.44675937896466E-15,3.47506462955744,
-3.42289583527326));
#52670=CARTESIAN_POINT('Ctrl Pts',(-1.39690296057887E-15,3.5829141507272,
-3.33091973644948));
#52671=CARTESIAN_POINT('Ctrl Pts',(7.97356274507999E-15,3.68684428184482,
-3.23407532274603));
#52672=CARTESIAN_POINT('Ctrl Pts',(8.63198401646059E-15,3.786506317757,
-3.13249514891036));
#52673=CARTESIAN_POINT('Ctrl Pts',(8.82826822414374E-15,3.81621690671488,
-3.10221273732326));
#52674=CARTESIAN_POINT('Ctrl Pts',(4.28211893531462E-15,3.84554796150488,
-3.07150918131398));
#52675=CARTESIAN_POINT('Ctrl Pts',(4.44089209850063E-15,3.87448963569911,
-3.0403873211912));
#52676=CARTESIAN_POINT('Ctrl Pts',(4.44089209850063E-15,3.87448963569911,
-3.0403873211912));
#52677=CARTESIAN_POINT('Ctrl Pts',(-0.039772944186534,3.3679595299544,-3.68587930545212));
#52678=CARTESIAN_POINT('Ctrl Pts',(-0.0795458883730713,2.69823621289534,
-4.19688248983334));
#52679=CARTESIAN_POINT('Ctrl Pts',(-0.11931883255961,1.94417218263051,-4.52245569180505));
#52680=CARTESIAN_POINT('Ctrl Pts',(-0.159091776746148,1.19010815236569,
-4.84802889377675));
#52681=CARTESIAN_POINT('Ctrl Pts',(-0.198864720932685,0.351703408895132,
-4.98817211333893));
#52682=CARTESIAN_POINT('Ctrl Pts',(-0.238637665119224,-0.463640495906287,
-4.90908491848449));
#52683=CARTESIAN_POINT('Ctrl Pts',(-0.318183553492298,-2.09432830550906,
-4.75091052877563));
#52684=CARTESIAN_POINT('Ctrl Pts',(-0.397729441865374,-3.63277276043523,
-3.71581448140035));
#52685=CARTESIAN_POINT('Ctrl Pts',(-0.477275330238448,-4.38170539133441,
-2.26639967267857));
#52686=CARTESIAN_POINT('Ctrl Pts',(-0.515236378191096,-4.7391125194254,
-1.57470703862169));
#52687=CARTESIAN_POINT('Ctrl Pts',(-0.553197426143743,-4.91671556355819,
-0.788657102896253));
#52688=CARTESIAN_POINT('Ctrl Pts',(-0.591158474096391,-4.91617236260859,
-0.00191614214703012));
#52689=CARTESIAN_POINT('Origin',(0.5,7.95374963839832,-1.25014666726696));
#52690=CARTESIAN_POINT('',(9.,7.8971245663519,-1.27883680879202));
#52691=CARTESIAN_POINT('',(0.499999999999999,7.8971245663519,-1.27883680879202));
#52692=CARTESIAN_POINT('',(4.75,7.8971245663519,-1.27883680879202));
#52693=CARTESIAN_POINT('',(9.,7.73074086114583,-1.3631381946854));
#52694=CARTESIAN_POINT('',(9.,7.95374963839832,-1.25014666726696));
#52695=CARTESIAN_POINT('',(0.5,7.73074086114583,-1.3631381946854));
#52696=CARTESIAN_POINT('',(0.5,7.73074086114583,-1.3631381946854));
#52697=CARTESIAN_POINT('',(0.5,7.95374963839832,-1.25014666726696));
#52698=CARTESIAN_POINT('Origin',(0.5,7.82922163644705,-1.3805030124521));
#52699=CARTESIAN_POINT('',(0.499999999999999,7.85825762906118,-1.49926216363308));
#52700=CARTESIAN_POINT('Origin',(0.5,0.,0.));
#52701=CARTESIAN_POINT('',(0.5,7.73074086114583,-1.3631381946854));
#52702=CARTESIAN_POINT('Origin',(0.5,7.73074086114583,-1.3631381946854));
#52703=CARTESIAN_POINT('',(9.,7.85825762906118,-1.49926216363308));
#52704=CARTESIAN_POINT('',(4.75,7.85825762906118,-1.49926216363308));
#52705=CARTESIAN_POINT('',(9.,7.73074086114583,-1.3631381946854));
#52706=CARTESIAN_POINT('Origin',(9.,7.82922163644705,-1.3805030124521));
#52707=CARTESIAN_POINT('Origin',(9.,0.,0.));
#52708=CARTESIAN_POINT('Origin',(0.5,7.61582861882541,-2.61230826065375));
#52709=CARTESIAN_POINT('',(9.,7.55508181806639,-2.63072969389153));
#52710=CARTESIAN_POINT('',(0.499999999999999,7.55508181806639,-2.63072969389153));
#52711=CARTESIAN_POINT('',(4.75,7.55508181806639,-2.63072969389153));
#52712=CARTESIAN_POINT('',(9.,7.37658707316938,-2.6848581251065));
#52713=CARTESIAN_POINT('',(9.,7.61582861882541,-2.61230826065375));
#52714=CARTESIAN_POINT('',(0.5,7.37658707316938,-2.6848581251065));
#52715=CARTESIAN_POINT('',(0.5,7.37658707316938,-2.6848581251065));
#52716=CARTESIAN_POINT('',(0.5,7.61582861882541,-2.61230826065375));
#52717=CARTESIAN_POINT('Origin',(0.5,7.47055633524797,-2.71906013943907));
#52718=CARTESIAN_POINT('',(0.499999999999999,7.47852889570692,-2.84105711946744));
#52719=CARTESIAN_POINT('Origin',(0.5,0.,0.));
#52720=CARTESIAN_POINT('',(0.5,7.37658707316938,-2.6848581251065));
#52721=CARTESIAN_POINT('Origin',(0.5,7.37658707316938,-2.6848581251065));
#52722=CARTESIAN_POINT('',(9.,7.47852889570692,-2.84105711946744));
#52723=CARTESIAN_POINT('',(4.75,7.47852889570692,-2.84105711946744));
#52724=CARTESIAN_POINT('',(9.,7.37658707316938,-2.6848581251065));
#52725=CARTESIAN_POINT('Origin',(9.,7.47055633524797,-2.71906013943907));
#52726=CARTESIAN_POINT('Origin',(9.,0.,0.));
#52727=CARTESIAN_POINT('Origin',(0.5,7.04650450046473,-3.89509618943234));
#52728=CARTESIAN_POINT('',(9.,6.98348173179481,-3.9026891884556));
#52729=CARTESIAN_POINT('',(0.499999999999999,6.98348173179481,-3.9026891884556));
#52730=CARTESIAN_POINT('',(4.75,6.98348173179481,-3.9026891884556));
#52731=CARTESIAN_POINT('',(9.,6.79829941970784,-3.925));
#52732=CARTESIAN_POINT('',(9.,7.04650450046473,-3.89509618943234));
#52733=CARTESIAN_POINT('',(0.5,6.79829941970784,-3.925));
#52734=CARTESIAN_POINT('',(0.5,6.79829941970784,-3.925));
#52735=CARTESIAN_POINT('',(0.5,7.04650450046473,-3.89509618943234));
#52736=CARTESIAN_POINT('Origin',(0.5,6.88490196008629,-3.975));
#52737=CARTESIAN_POINT('',(0.499999999999999,6.87156884617482,-4.09652799237106));
#52738=CARTESIAN_POINT('Origin',(0.5,0.,0.));
#52739=CARTESIAN_POINT('',(0.5,6.79829941970784,-3.925));
#52740=CARTESIAN_POINT('Origin',(0.5,6.79829941970784,-3.925));
#52741=CARTESIAN_POINT('',(9.,6.87156884617482,-4.09652799237106));
#52742=CARTESIAN_POINT('',(4.75,6.87156884617482,-4.09652799237106));
#52743=CARTESIAN_POINT('',(9.,6.79829941970784,-3.925));
#52744=CARTESIAN_POINT('Origin',(9.,6.88490196008629,-3.975));
#52745=CARTESIAN_POINT('Origin',(9.,0.,0.));
#52746=CARTESIAN_POINT('Origin',(0.5,6.26307590856075,-5.0595335915088));
#52747=CARTESIAN_POINT('',(9.,6.1996920869149,-5.05606744688446));
#52748=CARTESIAN_POINT('',(0.499999999999999,6.1996920869149,-5.05606744688446));
#52749=CARTESIAN_POINT('',(4.75,6.1996920869149,-5.05606744688446));
#52750=CARTESIAN_POINT('',(9.,6.01344887848397,-5.04588273603934));
#52751=CARTESIAN_POINT('',(9.,6.26307590856075,-5.0595335915088));
#52752=CARTESIAN_POINT('',(0.5,6.01344887848397,-5.04588273603934));
#52753=CARTESIAN_POINT('',(0.5,6.01344887848397,-5.04588273603934));
#52754=CARTESIAN_POINT('',(0.5,6.26307590856075,-5.0595335915088));
#52755=CARTESIAN_POINT('Origin',(0.5,6.09005332279587,-5.11016149700799));
#52756=CARTESIAN_POINT('',(0.499999999999999,6.05581965443331,-5.22752793516966));
#52757=CARTESIAN_POINT('Origin',(0.5,0.,0.));
#52758=CARTESIAN_POINT('',(0.5,6.01344887848397,-5.04588273603934));
#52759=CARTESIAN_POINT('Origin',(0.5,6.01344887848397,-5.04588273603934));
#52760=CARTESIAN_POINT('',(9.,6.05581965443331,-5.22752793516966));
#52761=CARTESIAN_POINT('',(4.75,6.05581965443331,-5.22752793516966));
#52762=CARTESIAN_POINT('',(9.,6.01344887848397,-5.04588273603934));
#52763=CARTESIAN_POINT('Origin',(9.,6.09005332279587,-5.11016149700799));
#52764=CARTESIAN_POINT('Origin',(9.,0.,0.));
#52765=CARTESIAN_POINT('Origin',(0.5,5.28934692444449,-6.07023962565479));
#52766=CARTESIAN_POINT('',(9.,5.22752793516966,-6.05581965443332));
#52767=CARTESIAN_POINT('',(0.499999999999999,5.22752793516966,-6.05581965443332));
#52768=CARTESIAN_POINT('',(4.75,5.22752793516966,-6.05581965443332));
#52769=CARTESIAN_POINT('',(9.,5.04588273603933,-6.01344887848398));
#52770=CARTESIAN_POINT('',(9.,5.28934692444449,-6.07023962565479));
#52771=CARTESIAN_POINT('',(0.5,5.04588273603933,-6.01344887848398));
#52772=CARTESIAN_POINT('',(0.5,5.04588273603933,-6.01344887848398));
#52773=CARTESIAN_POINT('',(0.5,5.28934692444449,-6.07023962565479));
#52774=CARTESIAN_POINT('Origin',(0.5,5.11016149700799,-6.09005332279588));
#52775=CARTESIAN_POINT('',(0.499999999999999,5.05606744688446,-6.19969208691491));
#52776=CARTESIAN_POINT('Origin',(0.5,0.,0.));
#52777=CARTESIAN_POINT('',(0.5,5.04588273603933,-6.01344887848398));
#52778=CARTESIAN_POINT('Origin',(0.5,5.04588273603933,-6.01344887848398));
#52779=CARTESIAN_POINT('',(9.,5.05606744688446,-6.19969208691491));
#52780=CARTESIAN_POINT('',(4.75,5.05606744688446,-6.19969208691491));
#52781=CARTESIAN_POINT('',(9.,5.04588273603933,-6.01344887848398));
#52782=CARTESIAN_POINT('Origin',(9.,5.11016149700799,-6.09005332279588));
#52783=CARTESIAN_POINT('Origin',(9.,0.,0.));
#52784=CARTESIAN_POINT('Origin',(0.5,4.15490381056767,-6.89650450046473));
#52785=CARTESIAN_POINT('',(9.,4.09652799237105,-6.87156884617482));
#52786=CARTESIAN_POINT('',(0.499999999999999,4.09652799237105,-6.87156884617482));
#52787=CARTESIAN_POINT('',(4.75,4.09652799237105,-6.87156884617482));
#52788=CARTESIAN_POINT('',(9.,3.925,-6.79829941970784));
#52789=CARTESIAN_POINT('',(9.,4.15490381056767,-6.89650450046473));
#52790=CARTESIAN_POINT('',(0.5,3.925,-6.79829941970784));
#52791=CARTESIAN_POINT('',(0.5,3.925,-6.79829941970784));
#52792=CARTESIAN_POINT('',(0.5,4.15490381056767,-6.89650450046473));
#52793=CARTESIAN_POINT('Origin',(0.5,3.975,-6.88490196008629));
#52794=CARTESIAN_POINT('',(0.499999999999999,3.9026891884556,-6.98348173179481));
#52795=CARTESIAN_POINT('Origin',(0.5,0.,0.));
#52796=CARTESIAN_POINT('',(0.5,3.925,-6.79829941970784));
#52797=CARTESIAN_POINT('Origin',(0.5,3.925,-6.79829941970784));
#52798=CARTESIAN_POINT('',(9.,3.9026891884556,-6.98348173179481));
#52799=CARTESIAN_POINT('',(4.75,3.9026891884556,-6.98348173179481));
#52800=CARTESIAN_POINT('',(9.,3.925,-6.79829941970784));
#52801=CARTESIAN_POINT('Origin',(9.,3.975,-6.88490196008629));
#52802=CARTESIAN_POINT('Origin',(9.,0.,0.));
#52803=CARTESIAN_POINT('Origin',(0.5,2.89421604688952,-7.51322257582772));
#52804=CARTESIAN_POINT('',(9.,2.84105711946744,-7.47852889570692));
#52805=CARTESIAN_POINT('',(0.499999999999999,2.84105711946744,-7.47852889570692));
#52806=CARTESIAN_POINT('',(4.75,2.84105711946744,-7.47852889570692));
#52807=CARTESIAN_POINT('',(9.,2.6848581251065,-7.37658707316938));
#52808=CARTESIAN_POINT('',(9.,2.89421604688952,-7.51322257582772));
#52809=CARTESIAN_POINT('',(0.5,2.6848581251065,-7.37658707316938));
#52810=CARTESIAN_POINT('',(0.5,2.6848581251065,-7.37658707316938));
#52811=CARTESIAN_POINT('',(0.5,2.89421604688952,-7.51322257582772));
#52812=CARTESIAN_POINT('Origin',(0.5,2.71906013943906,-7.47055633524797));
#52813=CARTESIAN_POINT('',(0.499999999999999,2.63072969389152,-7.5550818180664));
#52814=CARTESIAN_POINT('Origin',(0.5,0.,0.));
#52815=CARTESIAN_POINT('',(0.5,2.6848581251065,-7.37658707316938));
#52816=CARTESIAN_POINT('Origin',(0.5,2.6848581251065,-7.37658707316938));
#52817=CARTESIAN_POINT('',(9.,2.63072969389152,-7.5550818180664));
#52818=CARTESIAN_POINT('',(4.75,2.63072969389152,-7.5550818180664));
#52819=CARTESIAN_POINT('',(9.,2.6848581251065,-7.37658707316938));
#52820=CARTESIAN_POINT('Origin',(9.,2.71906013943906,-7.47055633524797));
#52821=CARTESIAN_POINT('Origin',(9.,0.,0.));
#52822=CARTESIAN_POINT('Origin',(0.5,1.54558899317062,-7.90165518509824));
#52823=CARTESIAN_POINT('',(9.,1.49926216363307,-7.85825762906118));
#52824=CARTESIAN_POINT('',(0.499999999999999,1.49926216363307,-7.85825762906118));
#52825=CARTESIAN_POINT('',(4.75,1.49926216363307,-7.85825762906118));
#52826=CARTESIAN_POINT('',(9.,1.3631381946854,-7.73074086114583));
#52827=CARTESIAN_POINT('',(9.,1.54558899317062,-7.90165518509824));
#52828=CARTESIAN_POINT('',(0.5,1.3631381946854,-7.73074086114583));
#52829=CARTESIAN_POINT('',(0.5,1.3631381946854,-7.73074086114583));
#52830=CARTESIAN_POINT('',(0.5,1.54558899317062,-7.90165518509824));
#52831=CARTESIAN_POINT('Origin',(0.5,1.38050301245209,-7.82922163644705));
#52832=CARTESIAN_POINT('',(0.499999999999999,1.27883680879201,-7.8971245663519));
#52833=CARTESIAN_POINT('Origin',(0.5,0.,0.));
#52834=CARTESIAN_POINT('',(0.5,1.3631381946854,-7.73074086114583));
#52835=CARTESIAN_POINT('Origin',(0.5,1.3631381946854,-7.73074086114583));
#52836=CARTESIAN_POINT('',(9.,1.27883680879201,-7.8971245663519));
#52837=CARTESIAN_POINT('',(4.75,1.27883680879201,-7.8971245663519));
#52838=CARTESIAN_POINT('',(9.,1.3631381946854,-7.73074086114583));
#52839=CARTESIAN_POINT('Origin',(9.,1.38050301245209,-7.82922163644705));
#52840=CARTESIAN_POINT('Origin',(9.,0.,0.));
#52841=CARTESIAN_POINT('Origin',(0.5,0.149999999999999,-8.05));
#52842=CARTESIAN_POINT('',(9.,0.111912885619984,-7.99921718082665));
#52843=CARTESIAN_POINT('',(0.499999999999999,0.111912885619984,-7.99921718082665));
#52844=CARTESIAN_POINT('',(4.75,0.111912885619984,-7.99921718082665));
#52845=CARTESIAN_POINT('',(9.,-1.44202160599601E-15,-7.85));
#52846=CARTESIAN_POINT('',(9.,0.149999999999999,-8.05));
#52847=CARTESIAN_POINT('',(0.5,-1.44202160599601E-15,-7.85));
#52848=CARTESIAN_POINT('',(0.5,-1.44202160599601E-15,-7.85));
#52849=CARTESIAN_POINT('',(0.5,0.149999999999999,-8.05));
#52850=CARTESIAN_POINT('Origin',(0.5,-1.46039130798322E-15,-7.95));
#52851=CARTESIAN_POINT('',(0.499999999999999,-0.111912885619986,-7.99921718082665));
#52852=CARTESIAN_POINT('Origin',(0.5,0.,0.));
#52853=CARTESIAN_POINT('',(0.5,-1.44202160599601E-15,-7.85));
#52854=CARTESIAN_POINT('Origin',(0.5,-1.44202160599601E-15,-7.85));
#52855=CARTESIAN_POINT('',(9.,-0.111912885619986,-7.99921718082665));
#52856=CARTESIAN_POINT('',(4.75,-0.111912885619986,-7.99921718082665));
#52857=CARTESIAN_POINT('',(9.,-1.44202160599601E-15,-7.85));
#52858=CARTESIAN_POINT('Origin',(9.,-1.46039130798322E-15,-7.95));
#52859=CARTESIAN_POINT('Origin',(9.,0.,0.));
#52860=CARTESIAN_POINT('Origin',(0.5,-1.25014666726696,-7.95374963839832));
#52861=CARTESIAN_POINT('',(9.,-1.27883680879202,-7.8971245663519));
#52862=CARTESIAN_POINT('',(0.499999999999999,-1.27883680879202,-7.8971245663519));
#52863=CARTESIAN_POINT('',(4.75,-1.27883680879202,-7.8971245663519));
#52864=CARTESIAN_POINT('',(9.,-1.3631381946854,-7.73074086114583));
#52865=CARTESIAN_POINT('',(9.,-1.25014666726696,-7.95374963839832));
#52866=CARTESIAN_POINT('',(0.5,-1.3631381946854,-7.73074086114583));
#52867=CARTESIAN_POINT('',(0.5,-1.3631381946854,-7.73074086114583));
#52868=CARTESIAN_POINT('',(0.5,-1.25014666726696,-7.95374963839832));
#52869=CARTESIAN_POINT('Origin',(0.5,-1.3805030124521,-7.82922163644705));
#52870=CARTESIAN_POINT('',(0.499999999999999,-1.49926216363308,-7.85825762906118));
#52871=CARTESIAN_POINT('Origin',(0.5,0.,0.));
#52872=CARTESIAN_POINT('',(0.5,-1.3631381946854,-7.73074086114583));
#52873=CARTESIAN_POINT('Origin',(0.5,-1.3631381946854,-7.73074086114583));
#52874=CARTESIAN_POINT('',(9.,-1.49926216363308,-7.85825762906118));
#52875=CARTESIAN_POINT('',(4.75,-1.49926216363308,-7.85825762906118));
#52876=CARTESIAN_POINT('',(9.,-1.3631381946854,-7.73074086114583));
#52877=CARTESIAN_POINT('Origin',(9.,-1.3805030124521,-7.82922163644705));
#52878=CARTESIAN_POINT('Origin',(9.,0.,0.));
#52879=CARTESIAN_POINT('Origin',(0.5,-2.61230826065375,-7.61582861882541));
#52880=CARTESIAN_POINT('',(9.,-2.63072969389153,-7.55508181806639));
#52881=CARTESIAN_POINT('',(0.499999999999999,-2.63072969389153,-7.55508181806639));
#52882=CARTESIAN_POINT('',(4.75,-2.63072969389153,-7.55508181806639));
#52883=CARTESIAN_POINT('',(9.,-2.6848581251065,-7.37658707316938));
#52884=CARTESIAN_POINT('',(9.,-2.61230826065375,-7.61582861882541));
#52885=CARTESIAN_POINT('',(0.5,-2.6848581251065,-7.37658707316938));
#52886=CARTESIAN_POINT('',(0.5,-2.6848581251065,-7.37658707316938));
#52887=CARTESIAN_POINT('',(0.5,-2.61230826065375,-7.61582861882541));
#52888=CARTESIAN_POINT('Origin',(0.5,-2.71906013943907,-7.47055633524797));
#52889=CARTESIAN_POINT('',(0.499999999999999,-2.84105711946745,-7.47852889570692));
#52890=CARTESIAN_POINT('Origin',(0.5,0.,0.));
#52891=CARTESIAN_POINT('',(0.5,-2.6848581251065,-7.37658707316938));
#52892=CARTESIAN_POINT('Origin',(0.5,-2.6848581251065,-7.37658707316938));
#52893=CARTESIAN_POINT('',(9.,-2.84105711946745,-7.47852889570692));
#52894=CARTESIAN_POINT('',(4.75,-2.84105711946744,-7.47852889570692));
#52895=CARTESIAN_POINT('',(9.,-2.6848581251065,-7.37658707316938));
#52896=CARTESIAN_POINT('Origin',(9.,-2.71906013943907,-7.47055633524797));
#52897=CARTESIAN_POINT('Origin',(9.,0.,0.));
#52898=CARTESIAN_POINT('Origin',(0.5,-3.89509618943234,-7.04650450046473));
#52899=CARTESIAN_POINT('',(9.,-3.9026891884556,-6.98348173179481));
#52900=CARTESIAN_POINT('',(0.499999999999999,-3.9026891884556,-6.98348173179481));
#52901=CARTESIAN_POINT('',(4.75,-3.9026891884556,-6.98348173179481));
#52902=CARTESIAN_POINT('',(9.,-3.925,-6.79829941970784));
#52903=CARTESIAN_POINT('',(9.,-3.89509618943234,-7.04650450046473));
#52904=CARTESIAN_POINT('',(0.5,-3.925,-6.79829941970784));
#52905=CARTESIAN_POINT('',(0.5,-3.925,-6.79829941970784));
#52906=CARTESIAN_POINT('',(0.5,-3.89509618943234,-7.04650450046473));
#52907=CARTESIAN_POINT('Origin',(0.5,-3.975,-6.88490196008629));
#52908=CARTESIAN_POINT('',(0.499999999999999,-4.09652799237106,-6.87156884617482));
#52909=CARTESIAN_POINT('Origin',(0.5,0.,0.));
#52910=CARTESIAN_POINT('',(0.5,-3.925,-6.79829941970784));
#52911=CARTESIAN_POINT('Origin',(0.5,-3.925,-6.79829941970784));
#52912=CARTESIAN_POINT('',(9.,-4.09652799237106,-6.87156884617482));
#52913=CARTESIAN_POINT('',(4.75,-4.09652799237106,-6.87156884617482));
#52914=CARTESIAN_POINT('',(9.,-3.925,-6.79829941970784));
#52915=CARTESIAN_POINT('Origin',(9.,-3.975,-6.88490196008629));
#52916=CARTESIAN_POINT('Origin',(9.,0.,0.));
#52917=CARTESIAN_POINT('Origin',(0.5,-5.0595335915088,-6.26307590856075));
#52918=CARTESIAN_POINT('',(9.,-5.05606744688446,-6.1996920869149));
#52919=CARTESIAN_POINT('',(0.499999999999999,-5.05606744688446,-6.1996920869149));
#52920=CARTESIAN_POINT('',(4.75,-5.05606744688446,-6.1996920869149));
#52921=CARTESIAN_POINT('',(9.,-5.04588273603933,-6.01344887848398));
#52922=CARTESIAN_POINT('',(9.,-5.0595335915088,-6.26307590856075));
#52923=CARTESIAN_POINT('',(0.5,-5.04588273603933,-6.01344887848398));
#52924=CARTESIAN_POINT('',(0.5,-5.04588273603933,-6.01344887848398));
#52925=CARTESIAN_POINT('',(0.5,-5.0595335915088,-6.26307590856075));
#52926=CARTESIAN_POINT('Origin',(0.5,-5.11016149700799,-6.09005332279587));
#52927=CARTESIAN_POINT('',(0.499999999999999,-5.22752793516966,-6.05581965443332));
#52928=CARTESIAN_POINT('Origin',(0.5,0.,0.));
#52929=CARTESIAN_POINT('',(0.5,-5.04588273603933,-6.01344887848398));
#52930=CARTESIAN_POINT('Origin',(0.5,-5.04588273603933,-6.01344887848398));
#52931=CARTESIAN_POINT('',(9.,-5.22752793516966,-6.05581965443332));
#52932=CARTESIAN_POINT('',(4.75,-5.22752793516966,-6.05581965443332));
#52933=CARTESIAN_POINT('',(9.,-5.04588273603933,-6.01344887848398));
#52934=CARTESIAN_POINT('Origin',(9.,-5.11016149700799,-6.09005332279587));
#52935=CARTESIAN_POINT('Origin',(9.,0.,0.));
#52936=CARTESIAN_POINT('Origin',(0.5,-6.07023962565479,-5.28934692444449));
#52937=CARTESIAN_POINT('',(9.,-6.05581965443332,-5.22752793516966));
#52938=CARTESIAN_POINT('',(0.499999999999999,-6.05581965443332,-5.22752793516966));
#52939=CARTESIAN_POINT('',(4.75,-6.05581965443332,-5.22752793516966));
#52940=CARTESIAN_POINT('',(9.,-6.01344887848398,-5.04588273603933));
#52941=CARTESIAN_POINT('',(9.,-6.07023962565479,-5.28934692444449));
#52942=CARTESIAN_POINT('',(0.5,-6.01344887848398,-5.04588273603933));
#52943=CARTESIAN_POINT('',(0.5,-6.01344887848398,-5.04588273603933));
#52944=CARTESIAN_POINT('',(0.5,-6.07023962565479,-5.28934692444449));
#52945=CARTESIAN_POINT('Origin',(0.5,-6.09005332279588,-5.11016149700799));
#52946=CARTESIAN_POINT('',(0.499999999999999,-6.1996920869149,-5.05606744688446));
#52947=CARTESIAN_POINT('Origin',(0.5,0.,0.));
#52948=CARTESIAN_POINT('',(0.5,-6.01344887848398,-5.04588273603933));
#52949=CARTESIAN_POINT('Origin',(0.5,-6.01344887848398,-5.04588273603933));
#52950=CARTESIAN_POINT('',(9.,-6.1996920869149,-5.05606744688446));
#52951=CARTESIAN_POINT('',(4.75,-6.1996920869149,-5.05606744688446));
#52952=CARTESIAN_POINT('',(9.,-6.01344887848398,-5.04588273603933));
#52953=CARTESIAN_POINT('Origin',(9.,-6.09005332279588,-5.11016149700799));
#52954=CARTESIAN_POINT('Origin',(9.,0.,0.));
#52955=CARTESIAN_POINT('Origin',(0.5,-6.89650450046473,-4.15490381056766));
#52956=CARTESIAN_POINT('',(9.,-6.87156884617482,-4.09652799237105));
#52957=CARTESIAN_POINT('',(0.499999999999999,-6.87156884617482,-4.09652799237105));
#52958=CARTESIAN_POINT('',(4.75,-6.87156884617482,-4.09652799237105));
#52959=CARTESIAN_POINT('',(9.,-6.79829941970784,-3.925));
#52960=CARTESIAN_POINT('',(9.,-6.89650450046473,-4.15490381056766));
#52961=CARTESIAN_POINT('',(0.5,-6.79829941970784,-3.925));
#52962=CARTESIAN_POINT('',(0.5,-6.79829941970784,-3.925));
#52963=CARTESIAN_POINT('',(0.5,-6.89650450046473,-4.15490381056766));
#52964=CARTESIAN_POINT('Origin',(0.5,-6.88490196008629,-3.975));
#52965=CARTESIAN_POINT('',(0.499999999999999,-6.98348173179481,-3.90268918845559));
#52966=CARTESIAN_POINT('Origin',(0.5,0.,0.));
#52967=CARTESIAN_POINT('',(0.5,-6.79829941970784,-3.925));
#52968=CARTESIAN_POINT('Origin',(0.5,-6.79829941970784,-3.925));
#52969=CARTESIAN_POINT('',(9.,-6.98348173179481,-3.90268918845559));
#52970=CARTESIAN_POINT('',(4.75,-6.98348173179481,-3.90268918845559));
#52971=CARTESIAN_POINT('',(9.,-6.79829941970784,-3.925));
#52972=CARTESIAN_POINT('Origin',(9.,-6.88490196008629,-3.975));
#52973=CARTESIAN_POINT('Origin',(9.,0.,0.));
#52974=CARTESIAN_POINT('Origin',(0.5,-7.51322257582771,-2.89421604688952));
#52975=CARTESIAN_POINT('',(9.,-7.47852889570692,-2.84105711946744));
#52976=CARTESIAN_POINT('',(0.499999999999999,-7.47852889570692,-2.84105711946744));
#52977=CARTESIAN_POINT('',(4.75,-7.47852889570692,-2.84105711946744));
#52978=CARTESIAN_POINT('',(9.,-7.37658707316938,-2.6848581251065));
#52979=CARTESIAN_POINT('',(9.,-7.51322257582771,-2.89421604688952));
#52980=CARTESIAN_POINT('',(0.5,-7.37658707316938,-2.6848581251065));
#52981=CARTESIAN_POINT('',(0.5,-7.37658707316938,-2.6848581251065));
#52982=CARTESIAN_POINT('',(0.5,-7.51322257582771,-2.89421604688952));
#52983=CARTESIAN_POINT('Origin',(0.5,-7.47055633524797,-2.71906013943907));
#52984=CARTESIAN_POINT('',(0.499999999999999,-7.55508181806639,-2.63072969389152));
#52985=CARTESIAN_POINT('Origin',(0.5,0.,0.));
#52986=CARTESIAN_POINT('',(0.5,-7.37658707316938,-2.6848581251065));
#52987=CARTESIAN_POINT('Origin',(0.5,-7.37658707316938,-2.6848581251065));
#52988=CARTESIAN_POINT('',(9.,-7.55508181806639,-2.63072969389152));
#52989=CARTESIAN_POINT('',(4.75,-7.55508181806639,-2.63072969389152));
#52990=CARTESIAN_POINT('',(9.,-7.37658707316938,-2.6848581251065));
#52991=CARTESIAN_POINT('Origin',(9.,-7.47055633524797,-2.71906013943907));
#52992=CARTESIAN_POINT('Origin',(9.,0.,0.));
#52993=CARTESIAN_POINT('Origin',(0.5,-7.90165518509824,-1.54558899317062));
#52994=CARTESIAN_POINT('',(9.,-7.85825762906118,-1.49926216363307));
#52995=CARTESIAN_POINT('',(0.499999999999999,-7.85825762906118,-1.49926216363307));
#52996=CARTESIAN_POINT('',(4.75,-7.85825762906118,-1.49926216363307));
#52997=CARTESIAN_POINT('',(9.,-7.73074086114583,-1.3631381946854));
#52998=CARTESIAN_POINT('',(9.,-7.90165518509824,-1.54558899317062));
#52999=CARTESIAN_POINT('',(0.5,-7.73074086114583,-1.3631381946854));
#53000=CARTESIAN_POINT('',(0.5,-7.73074086114583,-1.3631381946854));
#53001=CARTESIAN_POINT('',(0.5,-7.90165518509824,-1.54558899317062));
#53002=CARTESIAN_POINT('Origin',(0.5,-7.82922163644705,-1.38050301245209));
#53003=CARTESIAN_POINT('',(0.499999999999999,-7.8971245663519,-1.27883680879201));
#53004=CARTESIAN_POINT('Origin',(0.5,0.,0.));
#53005=CARTESIAN_POINT('',(0.5,-7.73074086114583,-1.3631381946854));
#53006=CARTESIAN_POINT('Origin',(0.5,-7.73074086114583,-1.3631381946854));
#53007=CARTESIAN_POINT('',(9.,-7.8971245663519,-1.27883680879201));
#53008=CARTESIAN_POINT('',(4.75,-7.8971245663519,-1.27883680879201));
#53009=CARTESIAN_POINT('',(9.,-7.73074086114583,-1.3631381946854));
#53010=CARTESIAN_POINT('Origin',(9.,-7.82922163644705,-1.38050301245209));
#53011=CARTESIAN_POINT('Origin',(9.,0.,0.));
#53012=CARTESIAN_POINT('Origin',(0.5,-8.05,-0.149999999999999));
#53013=CARTESIAN_POINT('',(9.,-7.99921718082665,-0.111912885619986));
#53014=CARTESIAN_POINT('',(0.499999999999999,-7.99921718082665,-0.111912885619986));
#53015=CARTESIAN_POINT('',(4.75,-7.99921718082665,-0.111912885619986));
#53016=CARTESIAN_POINT('',(9.,-7.85,9.61347737330672E-16));
#53017=CARTESIAN_POINT('',(9.,-8.05,-0.149999999999999));
#53018=CARTESIAN_POINT('',(0.5,-7.85,9.61347737330672E-16));
#53019=CARTESIAN_POINT('',(0.5,-7.85,9.61347737330672E-16));
#53020=CARTESIAN_POINT('',(0.5,-8.05,-0.149999999999999));
#53021=CARTESIAN_POINT('Origin',(0.5,-7.95,9.73594205322146E-16));
#53022=CARTESIAN_POINT('',(0.5,-8.,-9.79717439317883E-16));
#53023=CARTESIAN_POINT('Origin',(0.5,0.,0.));
#53024=CARTESIAN_POINT('',(0.499999999999999,-7.99921718082665,0.111912885619986));
#53025=CARTESIAN_POINT('',(0.5,-7.85,9.61347737330672E-16));
#53026=CARTESIAN_POINT('Origin',(0.5,0.,0.));
#53027=CARTESIAN_POINT('Origin',(0.5,-7.85,9.61347737330672E-16));
#53028=CARTESIAN_POINT('',(9.,-7.99921718082665,0.111912885619986));
#53029=CARTESIAN_POINT('',(4.75,-7.99921718082665,0.111912885619986));
#53030=CARTESIAN_POINT('',(9.,-7.85,9.61347737330672E-16));
#53031=CARTESIAN_POINT('Origin',(9.,-7.95,9.73594205322146E-16));
#53032=CARTESIAN_POINT('',(9.,-8.,-9.79717439317883E-16));
#53033=CARTESIAN_POINT('Origin',(9.,0.,0.));
#53034=CARTESIAN_POINT('Origin',(9.,0.,0.));
#53035=CARTESIAN_POINT('Origin',(0.5,-7.95374963839832,1.25014666726696));
#53036=CARTESIAN_POINT('',(9.,-7.8971245663519,1.27883680879202));
#53037=CARTESIAN_POINT('',(0.499999999999999,-7.8971245663519,1.27883680879202));
#53038=CARTESIAN_POINT('',(4.75,-7.8971245663519,1.27883680879202));
#53039=CARTESIAN_POINT('',(9.,-7.73074086114583,1.36313819468541));
#53040=CARTESIAN_POINT('',(9.,-7.95374963839832,1.25014666726696));
#53041=CARTESIAN_POINT('',(0.5,-7.73074086114583,1.36313819468541));
#53042=CARTESIAN_POINT('',(0.5,-7.73074086114583,1.36313819468541));
#53043=CARTESIAN_POINT('',(0.5,-7.95374963839832,1.25014666726696));
#53044=CARTESIAN_POINT('Origin',(0.5,-7.82922163644705,1.3805030124521));
#53045=CARTESIAN_POINT('',(0.499999999999999,-7.85825762906118,1.49926216363308));
#53046=CARTESIAN_POINT('Origin',(0.5,0.,0.));
#53047=CARTESIAN_POINT('',(0.5,-7.73074086114583,1.36313819468541));
#53048=CARTESIAN_POINT('Origin',(0.5,-7.73074086114583,1.36313819468541));
#53049=CARTESIAN_POINT('',(9.,-7.85825762906118,1.49926216363308));
#53050=CARTESIAN_POINT('',(4.75,-7.85825762906118,1.49926216363308));
#53051=CARTESIAN_POINT('',(9.,-7.73074086114583,1.36313819468541));
#53052=CARTESIAN_POINT('Origin',(9.,-7.82922163644705,1.3805030124521));
#53053=CARTESIAN_POINT('Origin',(9.,0.,0.));
#53054=CARTESIAN_POINT('Origin',(0.5,-7.61582861882541,2.61230826065375));
#53055=CARTESIAN_POINT('',(9.,-7.55508181806639,2.63072969389153));
#53056=CARTESIAN_POINT('',(0.499999999999999,-7.55508181806639,2.63072969389153));
#53057=CARTESIAN_POINT('',(4.75,-7.55508181806639,2.63072969389153));
#53058=CARTESIAN_POINT('',(9.,-7.37658707316938,2.6848581251065));
#53059=CARTESIAN_POINT('',(9.,-7.61582861882541,2.61230826065375));
#53060=CARTESIAN_POINT('',(0.5,-7.37658707316938,2.6848581251065));
#53061=CARTESIAN_POINT('',(0.5,-7.37658707316938,2.6848581251065));
#53062=CARTESIAN_POINT('',(0.5,-7.61582861882541,2.61230826065375));
#53063=CARTESIAN_POINT('Origin',(0.5,-7.47055633524797,2.71906013943907));
#53064=CARTESIAN_POINT('',(0.499999999999999,-7.47852889570692,2.84105711946744));
#53065=CARTESIAN_POINT('Origin',(0.5,0.,0.));
#53066=CARTESIAN_POINT('',(0.5,-7.37658707316938,2.6848581251065));
#53067=CARTESIAN_POINT('Origin',(0.5,-7.37658707316938,2.6848581251065));
#53068=CARTESIAN_POINT('',(9.,-7.47852889570692,2.84105711946744));
#53069=CARTESIAN_POINT('',(4.75,-7.47852889570692,2.84105711946744));
#53070=CARTESIAN_POINT('',(9.,-7.37658707316938,2.6848581251065));
#53071=CARTESIAN_POINT('Origin',(9.,-7.47055633524797,2.71906013943907));
#53072=CARTESIAN_POINT('Origin',(9.,0.,0.));
#53073=CARTESIAN_POINT('Origin',(0.5,-7.04650450046473,3.89509618943233));
#53074=CARTESIAN_POINT('',(9.,-6.98348173179481,3.90268918845559));
#53075=CARTESIAN_POINT('',(0.499999999999999,-6.98348173179481,3.90268918845559));
#53076=CARTESIAN_POINT('',(4.75,-6.98348173179481,3.90268918845559));
#53077=CARTESIAN_POINT('',(9.,-6.79829941970784,3.925));
#53078=CARTESIAN_POINT('',(9.,-7.04650450046473,3.89509618943233));
#53079=CARTESIAN_POINT('',(0.5,-6.79829941970784,3.925));
#53080=CARTESIAN_POINT('',(0.5,-6.79829941970784,3.925));
#53081=CARTESIAN_POINT('',(0.5,-7.04650450046473,3.89509618943233));
#53082=CARTESIAN_POINT('Origin',(0.5,-6.88490196008629,3.975));
#53083=CARTESIAN_POINT('',(0.499999999999999,-6.87156884617482,4.09652799237105));
#53084=CARTESIAN_POINT('Origin',(0.5,0.,0.));
#53085=CARTESIAN_POINT('',(0.5,-6.79829941970784,3.925));
#53086=CARTESIAN_POINT('Origin',(0.5,-6.79829941970784,3.925));
#53087=CARTESIAN_POINT('',(9.,-6.87156884617482,4.09652799237105));
#53088=CARTESIAN_POINT('',(4.75,-6.87156884617482,4.09652799237105));
#53089=CARTESIAN_POINT('',(9.,-6.79829941970784,3.925));
#53090=CARTESIAN_POINT('Origin',(9.,-6.88490196008629,3.975));
#53091=CARTESIAN_POINT('Origin',(9.,0.,0.));
#53092=CARTESIAN_POINT('Origin',(0.5,-6.26307590856075,5.0595335915088));
#53093=CARTESIAN_POINT('',(9.,-6.1996920869149,5.05606744688446));
#53094=CARTESIAN_POINT('',(0.499999999999999,-6.1996920869149,5.05606744688446));
#53095=CARTESIAN_POINT('',(4.75,-6.1996920869149,5.05606744688446));
#53096=CARTESIAN_POINT('',(9.,-6.01344887848398,5.04588273603933));
#53097=CARTESIAN_POINT('',(9.,-6.26307590856075,5.0595335915088));
#53098=CARTESIAN_POINT('',(0.5,-6.01344887848398,5.04588273603933));
#53099=CARTESIAN_POINT('',(0.5,-6.01344887848398,5.04588273603933));
#53100=CARTESIAN_POINT('',(0.5,-6.26307590856075,5.0595335915088));
#53101=CARTESIAN_POINT('Origin',(0.5,-6.09005332279587,5.11016149700799));
#53102=CARTESIAN_POINT('',(0.499999999999999,-6.05581965443332,5.22752793516966));
#53103=CARTESIAN_POINT('Origin',(0.5,0.,0.));
#53104=CARTESIAN_POINT('',(0.5,-6.01344887848398,5.04588273603933));
#53105=CARTESIAN_POINT('Origin',(0.5,-6.01344887848398,5.04588273603933));
#53106=CARTESIAN_POINT('',(9.,-6.05581965443332,5.22752793516966));
#53107=CARTESIAN_POINT('',(4.75,-6.05581965443332,5.22752793516966));
#53108=CARTESIAN_POINT('',(9.,-6.01344887848398,5.04588273603933));
#53109=CARTESIAN_POINT('Origin',(9.,-6.09005332279587,5.11016149700799));
#53110=CARTESIAN_POINT('Origin',(9.,0.,0.));
#53111=CARTESIAN_POINT('Origin',(0.5,-5.28934692444449,6.07023962565479));
#53112=CARTESIAN_POINT('',(9.,-5.22752793516966,6.05581965443332));
#53113=CARTESIAN_POINT('',(0.499999999999999,-5.22752793516966,6.05581965443332));
#53114=CARTESIAN_POINT('',(4.75,-5.22752793516966,6.05581965443332));
#53115=CARTESIAN_POINT('',(9.,-5.04588273603933,6.01344887848398));
#53116=CARTESIAN_POINT('',(9.,-5.28934692444449,6.07023962565479));
#53117=CARTESIAN_POINT('',(0.5,-5.04588273603933,6.01344887848398));
#53118=CARTESIAN_POINT('',(0.5,-5.04588273603933,6.01344887848398));
#53119=CARTESIAN_POINT('',(0.5,-5.28934692444449,6.07023962565479));
#53120=CARTESIAN_POINT('Origin',(0.5,-5.11016149700799,6.09005332279587));
#53121=CARTESIAN_POINT('',(0.499999999999999,-5.05606744688446,6.1996920869149));
#53122=CARTESIAN_POINT('Origin',(0.5,0.,0.));
#53123=CARTESIAN_POINT('',(0.5,-5.04588273603933,6.01344887848398));
#53124=CARTESIAN_POINT('Origin',(0.5,-5.04588273603933,6.01344887848398));
#53125=CARTESIAN_POINT('',(9.,-5.05606744688446,6.1996920869149));
#53126=CARTESIAN_POINT('',(4.75,-5.05606744688446,6.1996920869149));
#53127=CARTESIAN_POINT('',(9.,-5.04588273603933,6.01344887848398));
#53128=CARTESIAN_POINT('Origin',(9.,-5.11016149700799,6.09005332279587));
#53129=CARTESIAN_POINT('Origin',(9.,0.,0.));
#53130=CARTESIAN_POINT('Origin',(0.5,-4.15490381056767,6.89650450046473));
#53131=CARTESIAN_POINT('',(9.,-4.09652799237105,6.87156884617482));
#53132=CARTESIAN_POINT('',(0.499999999999999,-4.09652799237105,6.87156884617482));
#53133=CARTESIAN_POINT('',(4.75,-4.09652799237105,6.87156884617482));
#53134=CARTESIAN_POINT('',(9.,-3.925,6.79829941970784));
#53135=CARTESIAN_POINT('',(9.,-4.15490381056767,6.89650450046473));
#53136=CARTESIAN_POINT('',(0.5,-3.925,6.79829941970784));
#53137=CARTESIAN_POINT('',(0.5,-3.925,6.79829941970784));
#53138=CARTESIAN_POINT('',(0.5,-4.15490381056767,6.89650450046473));
#53139=CARTESIAN_POINT('Origin',(0.5,-3.975,6.88490196008629));
#53140=CARTESIAN_POINT('',(0.499999999999999,-3.90268918845559,6.98348173179481));
#53141=CARTESIAN_POINT('Origin',(0.5,0.,0.));
#53142=CARTESIAN_POINT('',(0.5,-3.925,6.79829941970784));
#53143=CARTESIAN_POINT('Origin',(0.5,-3.925,6.79829941970784));
#53144=CARTESIAN_POINT('',(9.,-3.90268918845559,6.98348173179481));
#53145=CARTESIAN_POINT('',(4.75,-3.90268918845559,6.98348173179481));
#53146=CARTESIAN_POINT('',(9.,-3.925,6.79829941970784));
#53147=CARTESIAN_POINT('Origin',(9.,-3.975,6.88490196008629));
#53148=CARTESIAN_POINT('Origin',(9.,0.,0.));
#53149=CARTESIAN_POINT('Origin',(0.5,-2.89421604688952,7.51322257582771));
#53150=CARTESIAN_POINT('',(9.,-2.84105711946744,7.47852889570692));
#53151=CARTESIAN_POINT('',(0.499999999999999,-2.84105711946744,7.47852889570692));
#53152=CARTESIAN_POINT('',(4.75,-2.84105711946744,7.47852889570692));
#53153=CARTESIAN_POINT('',(9.,-2.6848581251065,7.37658707316938));
#53154=CARTESIAN_POINT('',(9.,-2.89421604688952,7.51322257582771));
#53155=CARTESIAN_POINT('',(0.5,-2.6848581251065,7.37658707316938));
#53156=CARTESIAN_POINT('',(0.5,-2.6848581251065,7.37658707316938));
#53157=CARTESIAN_POINT('',(0.5,-2.89421604688952,7.51322257582771));
#53158=CARTESIAN_POINT('Origin',(0.5,-2.71906013943907,7.47055633524797));
#53159=CARTESIAN_POINT('',(0.499999999999999,-2.63072969389152,7.55508181806639));
#53160=CARTESIAN_POINT('Origin',(0.5,0.,0.));
#53161=CARTESIAN_POINT('',(0.5,-2.6848581251065,7.37658707316938));
#53162=CARTESIAN_POINT('Origin',(0.5,-2.6848581251065,7.37658707316938));
#53163=CARTESIAN_POINT('',(9.,-2.63072969389152,7.55508181806639));
#53164=CARTESIAN_POINT('',(4.75,-2.63072969389152,7.55508181806639));
#53165=CARTESIAN_POINT('',(9.,-2.6848581251065,7.37658707316938));
#53166=CARTESIAN_POINT('Origin',(9.,-2.71906013943907,7.47055633524797));
#53167=CARTESIAN_POINT('Origin',(9.,0.,0.));
#53168=CARTESIAN_POINT('Origin',(0.5,-1.54558899317062,7.90165518509824));
#53169=CARTESIAN_POINT('',(9.,-1.49926216363308,7.85825762906118));
#53170=CARTESIAN_POINT('',(0.499999999999999,-1.49926216363308,7.85825762906118));
#53171=CARTESIAN_POINT('',(4.75,-1.49926216363308,7.85825762906118));
#53172=CARTESIAN_POINT('',(9.,-1.3631381946854,7.73074086114583));
#53173=CARTESIAN_POINT('',(9.,-1.54558899317062,7.90165518509824));
#53174=CARTESIAN_POINT('',(0.5,-1.3631381946854,7.73074086114583));
#53175=CARTESIAN_POINT('',(0.5,-1.3631381946854,7.73074086114583));
#53176=CARTESIAN_POINT('',(0.5,-1.54558899317062,7.90165518509824));
#53177=CARTESIAN_POINT('Origin',(0.5,-1.3805030124521,7.82922163644705));
#53178=CARTESIAN_POINT('',(0.499999999999999,-1.27883680879202,7.8971245663519));
#53179=CARTESIAN_POINT('Origin',(0.5,0.,0.));
#53180=CARTESIAN_POINT('',(0.5,-1.3631381946854,7.73074086114583));
#53181=CARTESIAN_POINT('Origin',(0.5,-1.3631381946854,7.73074086114583));
#53182=CARTESIAN_POINT('',(9.,-1.27883680879202,7.8971245663519));
#53183=CARTESIAN_POINT('',(4.75,-1.27883680879202,7.8971245663519));
#53184=CARTESIAN_POINT('',(9.,-1.3631381946854,7.73074086114583));
#53185=CARTESIAN_POINT('Origin',(9.,-1.3805030124521,7.82922163644705));
#53186=CARTESIAN_POINT('Origin',(9.,0.,0.));
#53187=CARTESIAN_POINT('Origin',(0.5,-0.15,8.05));
#53188=CARTESIAN_POINT('',(9.,-0.111912885619985,7.99921718082665));
#53189=CARTESIAN_POINT('',(0.499999999999999,-0.111912885619985,7.99921718082665));
#53190=CARTESIAN_POINT('',(4.75,-0.111912885619985,7.99921718082665));
#53191=CARTESIAN_POINT('',(9.,4.80673868665336E-16,7.85));
#53192=CARTESIAN_POINT('',(9.,-0.15,8.05));
#53193=CARTESIAN_POINT('',(0.5,4.80673868665336E-16,7.85));
#53194=CARTESIAN_POINT('',(0.5,4.80673868665336E-16,7.85));
#53195=CARTESIAN_POINT('',(0.5,-0.15,8.05));
#53196=CARTESIAN_POINT('Origin',(0.5,4.86797102661073E-16,7.95));
#53197=CARTESIAN_POINT('',(0.499999999999999,0.111912885619987,7.99921718082665));
#53198=CARTESIAN_POINT('Origin',(0.5,0.,0.));
#53199=CARTESIAN_POINT('',(0.5,4.80673868665336E-16,7.85));
#53200=CARTESIAN_POINT('Origin',(0.5,4.80673868665336E-16,7.85));
#53201=CARTESIAN_POINT('',(9.,0.111912885619987,7.99921718082665));
#53202=CARTESIAN_POINT('',(4.75,0.111912885619987,7.99921718082665));
#53203=CARTESIAN_POINT('',(9.,4.80673868665336E-16,7.85));
#53204=CARTESIAN_POINT('Origin',(9.,4.86797102661073E-16,7.95));
#53205=CARTESIAN_POINT('Origin',(9.,0.,0.));
#53206=CARTESIAN_POINT('Origin',(0.5,1.25014666726696,7.95374963839832));
#53207=CARTESIAN_POINT('',(9.,1.27883680879202,7.8971245663519));
#53208=CARTESIAN_POINT('',(0.499999999999999,1.27883680879202,7.8971245663519));
#53209=CARTESIAN_POINT('',(4.75,1.27883680879202,7.8971245663519));
#53210=CARTESIAN_POINT('',(9.,1.3631381946854,7.73074086114583));
#53211=CARTESIAN_POINT('',(9.,1.25014666726696,7.95374963839832));
#53212=CARTESIAN_POINT('',(0.5,1.3631381946854,7.73074086114583));
#53213=CARTESIAN_POINT('',(0.5,1.3631381946854,7.73074086114583));
#53214=CARTESIAN_POINT('',(0.5,1.25014666726696,7.95374963839832));
#53215=CARTESIAN_POINT('Origin',(0.5,1.3805030124521,7.82922163644705));
#53216=CARTESIAN_POINT('',(0.499999999999999,1.49926216363308,7.85825762906118));
#53217=CARTESIAN_POINT('Origin',(0.5,0.,0.));
#53218=CARTESIAN_POINT('',(0.5,1.3631381946854,7.73074086114583));
#53219=CARTESIAN_POINT('Origin',(0.5,1.3631381946854,7.73074086114583));
#53220=CARTESIAN_POINT('',(9.,1.49926216363308,7.85825762906118));
#53221=CARTESIAN_POINT('',(4.75,1.49926216363308,7.85825762906118));
#53222=CARTESIAN_POINT('',(9.,1.3631381946854,7.73074086114583));
#53223=CARTESIAN_POINT('Origin',(9.,1.3805030124521,7.82922163644705));
#53224=CARTESIAN_POINT('Origin',(9.,0.,0.));
#53225=CARTESIAN_POINT('Origin',(0.5,2.61230826065375,7.61582861882541));
#53226=CARTESIAN_POINT('',(9.,2.63072969389153,7.55508181806639));
#53227=CARTESIAN_POINT('',(0.499999999999999,2.63072969389153,7.55508181806639));
#53228=CARTESIAN_POINT('',(4.75,2.63072969389153,7.55508181806639));
#53229=CARTESIAN_POINT('',(9.,2.6848581251065,7.37658707316938));
#53230=CARTESIAN_POINT('',(9.,2.61230826065375,7.61582861882541));
#53231=CARTESIAN_POINT('',(0.5,2.6848581251065,7.37658707316938));
#53232=CARTESIAN_POINT('',(0.5,2.6848581251065,7.37658707316938));
#53233=CARTESIAN_POINT('',(0.5,2.61230826065375,7.61582861882541));
#53234=CARTESIAN_POINT('Origin',(0.5,2.71906013943907,7.47055633524797));
#53235=CARTESIAN_POINT('',(0.499999999999999,2.84105711946744,7.47852889570692));
#53236=CARTESIAN_POINT('Origin',(0.5,0.,0.));
#53237=CARTESIAN_POINT('',(0.5,2.6848581251065,7.37658707316938));
#53238=CARTESIAN_POINT('Origin',(0.5,2.6848581251065,7.37658707316938));
#53239=CARTESIAN_POINT('',(9.,2.84105711946744,7.47852889570692));
#53240=CARTESIAN_POINT('',(4.75,2.84105711946744,7.47852889570692));
#53241=CARTESIAN_POINT('',(9.,2.6848581251065,7.37658707316938));
#53242=CARTESIAN_POINT('Origin',(9.,2.71906013943907,7.47055633524797));
#53243=CARTESIAN_POINT('Origin',(9.,0.,0.));
#53244=CARTESIAN_POINT('Origin',(0.5,3.89509618943234,7.04650450046473));
#53245=CARTESIAN_POINT('',(9.,3.9026891884556,6.98348173179481));
#53246=CARTESIAN_POINT('',(0.499999999999999,3.9026891884556,6.98348173179481));
#53247=CARTESIAN_POINT('',(4.75,3.9026891884556,6.98348173179481));
#53248=CARTESIAN_POINT('',(9.,3.925,6.79829941970784));
#53249=CARTESIAN_POINT('',(9.,3.89509618943234,7.04650450046473));
#53250=CARTESIAN_POINT('',(0.5,3.925,6.79829941970784));
#53251=CARTESIAN_POINT('',(0.5,3.925,6.79829941970784));
#53252=CARTESIAN_POINT('',(0.5,3.89509618943234,7.04650450046473));
#53253=CARTESIAN_POINT('Origin',(0.5,3.975,6.88490196008629));
#53254=CARTESIAN_POINT('',(0.499999999999999,4.09652799237105,6.87156884617482));
#53255=CARTESIAN_POINT('Origin',(0.5,0.,0.));
#53256=CARTESIAN_POINT('',(0.5,3.925,6.79829941970784));
#53257=CARTESIAN_POINT('Origin',(0.5,3.925,6.79829941970784));
#53258=CARTESIAN_POINT('',(9.,4.09652799237105,6.87156884617482));
#53259=CARTESIAN_POINT('',(4.75,4.09652799237105,6.87156884617482));
#53260=CARTESIAN_POINT('',(9.,3.925,6.79829941970784));
#53261=CARTESIAN_POINT('Origin',(9.,3.975,6.88490196008629));
#53262=CARTESIAN_POINT('Origin',(9.,0.,0.));
#53263=CARTESIAN_POINT('Origin',(0.5,5.0595335915088,6.26307590856075));
#53264=CARTESIAN_POINT('',(9.,5.05606744688446,6.1996920869149));
#53265=CARTESIAN_POINT('',(0.499999999999999,5.05606744688446,6.1996920869149));
#53266=CARTESIAN_POINT('',(4.75,5.05606744688446,6.1996920869149));
#53267=CARTESIAN_POINT('',(9.,5.04588273603933,6.01344887848398));
#53268=CARTESIAN_POINT('',(9.,5.0595335915088,6.26307590856075));
#53269=CARTESIAN_POINT('',(0.5,5.04588273603933,6.01344887848398));
#53270=CARTESIAN_POINT('',(0.5,5.04588273603933,6.01344887848398));
#53271=CARTESIAN_POINT('',(0.5,5.0595335915088,6.26307590856075));
#53272=CARTESIAN_POINT('Origin',(0.5,5.11016149700799,6.09005332279587));
#53273=CARTESIAN_POINT('',(0.499999999999999,5.22752793516966,6.05581965443332));
#53274=CARTESIAN_POINT('Origin',(0.5,0.,0.));
#53275=CARTESIAN_POINT('',(0.5,5.04588273603933,6.01344887848398));
#53276=CARTESIAN_POINT('Origin',(0.5,5.04588273603933,6.01344887848398));
#53277=CARTESIAN_POINT('',(9.,5.22752793516966,6.05581965443332));
#53278=CARTESIAN_POINT('',(4.75,5.22752793516966,6.05581965443332));
#53279=CARTESIAN_POINT('',(9.,5.04588273603933,6.01344887848398));
#53280=CARTESIAN_POINT('Origin',(9.,5.11016149700799,6.09005332279587));
#53281=CARTESIAN_POINT('Origin',(9.,0.,0.));
#53282=CARTESIAN_POINT('Origin',(0.5,6.07023962565479,5.28934692444449));
#53283=CARTESIAN_POINT('',(9.,6.05581965443332,5.22752793516966));
#53284=CARTESIAN_POINT('',(0.499999999999999,6.05581965443332,5.22752793516966));
#53285=CARTESIAN_POINT('',(4.75,6.05581965443332,5.22752793516966));
#53286=CARTESIAN_POINT('',(9.,6.01344887848398,5.04588273603933));
#53287=CARTESIAN_POINT('',(9.,6.07023962565479,5.28934692444449));
#53288=CARTESIAN_POINT('',(0.5,6.01344887848398,5.04588273603933));
#53289=CARTESIAN_POINT('',(0.5,6.01344887848398,5.04588273603933));
#53290=CARTESIAN_POINT('',(0.5,6.07023962565479,5.28934692444449));
#53291=CARTESIAN_POINT('Origin',(0.5,6.09005332279588,5.11016149700799));
#53292=CARTESIAN_POINT('',(0.499999999999999,6.1996920869149,5.05606744688446));
#53293=CARTESIAN_POINT('Origin',(0.5,0.,0.));
#53294=CARTESIAN_POINT('',(0.5,6.01344887848398,5.04588273603933));
#53295=CARTESIAN_POINT('Origin',(0.5,6.01344887848398,5.04588273603933));
#53296=CARTESIAN_POINT('',(9.,6.1996920869149,5.05606744688446));
#53297=CARTESIAN_POINT('',(4.75,6.1996920869149,5.05606744688446));
#53298=CARTESIAN_POINT('',(9.,6.01344887848398,5.04588273603933));
#53299=CARTESIAN_POINT('Origin',(9.,6.09005332279588,5.11016149700799));
#53300=CARTESIAN_POINT('Origin',(9.,0.,0.));
#53301=CARTESIAN_POINT('Origin',(0.5,6.89650450046473,4.15490381056767));
#53302=CARTESIAN_POINT('',(9.,6.87156884617482,4.09652799237105));
#53303=CARTESIAN_POINT('',(0.499999999999999,6.87156884617482,4.09652799237105));
#53304=CARTESIAN_POINT('',(4.75,6.87156884617482,4.09652799237105));
#53305=CARTESIAN_POINT('',(9.,6.79829941970784,3.925));
#53306=CARTESIAN_POINT('',(9.,6.89650450046473,4.15490381056767));
#53307=CARTESIAN_POINT('',(0.5,6.79829941970784,3.925));
#53308=CARTESIAN_POINT('',(0.5,6.79829941970784,3.925));
#53309=CARTESIAN_POINT('',(0.5,6.89650450046473,4.15490381056767));
#53310=CARTESIAN_POINT('Origin',(0.5,6.88490196008629,3.975));
#53311=CARTESIAN_POINT('',(0.499999999999999,6.98348173179481,3.90268918845559));
#53312=CARTESIAN_POINT('Origin',(0.5,0.,0.));
#53313=CARTESIAN_POINT('',(0.5,6.79829941970784,3.925));
#53314=CARTESIAN_POINT('Origin',(0.5,6.79829941970784,3.925));
#53315=CARTESIAN_POINT('',(9.,6.98348173179481,3.90268918845559));
#53316=CARTESIAN_POINT('',(4.75,6.98348173179481,3.90268918845559));
#53317=CARTESIAN_POINT('',(9.,6.79829941970784,3.925));
#53318=CARTESIAN_POINT('Origin',(9.,6.88490196008629,3.975));
#53319=CARTESIAN_POINT('Origin',(9.,0.,0.));
#53320=CARTESIAN_POINT('Origin',(0.5,7.51322257582771,2.89421604688952));
#53321=CARTESIAN_POINT('',(9.,7.47852889570692,2.84105711946744));
#53322=CARTESIAN_POINT('',(0.499999999999999,7.47852889570692,2.84105711946744));
#53323=CARTESIAN_POINT('',(4.75,7.47852889570692,2.84105711946744));
#53324=CARTESIAN_POINT('',(9.,7.37658707316938,2.6848581251065));
#53325=CARTESIAN_POINT('',(9.,7.51322257582771,2.89421604688952));
#53326=CARTESIAN_POINT('',(0.5,7.37658707316938,2.6848581251065));
#53327=CARTESIAN_POINT('',(0.5,7.37658707316938,2.6848581251065));
#53328=CARTESIAN_POINT('',(0.5,7.51322257582771,2.89421604688952));
#53329=CARTESIAN_POINT('Origin',(0.5,7.47055633524797,2.71906013943907));
#53330=CARTESIAN_POINT('',(0.499999999999999,7.55508181806639,2.63072969389152));
#53331=CARTESIAN_POINT('Origin',(0.5,0.,0.));
#53332=CARTESIAN_POINT('',(0.5,7.37658707316938,2.6848581251065));
#53333=CARTESIAN_POINT('Origin',(0.5,7.37658707316938,2.6848581251065));
#53334=CARTESIAN_POINT('',(9.,7.55508181806639,2.63072969389152));
#53335=CARTESIAN_POINT('',(4.75,7.55508181806639,2.63072969389152));
#53336=CARTESIAN_POINT('',(9.,7.37658707316938,2.6848581251065));
#53337=CARTESIAN_POINT('Origin',(9.,7.47055633524797,2.71906013943907));
#53338=CARTESIAN_POINT('Origin',(9.,0.,0.));
#53339=CARTESIAN_POINT('Origin',(0.5,7.90165518509824,1.54558899317062));
#53340=CARTESIAN_POINT('',(9.,7.85825762906118,1.49926216363308));
#53341=CARTESIAN_POINT('',(0.499999999999999,7.85825762906118,1.49926216363308));
#53342=CARTESIAN_POINT('',(4.75,7.85825762906118,1.49926216363308));
#53343=CARTESIAN_POINT('',(9.,7.73074086114583,1.3631381946854));
#53344=CARTESIAN_POINT('',(9.,7.90165518509824,1.54558899317062));
#53345=CARTESIAN_POINT('',(0.5,7.73074086114583,1.3631381946854));
#53346=CARTESIAN_POINT('',(0.5,7.73074086114583,1.3631381946854));
#53347=CARTESIAN_POINT('',(0.5,7.90165518509824,1.54558899317062));
#53348=CARTESIAN_POINT('Origin',(0.5,7.82922163644705,1.3805030124521));
#53349=CARTESIAN_POINT('',(0.499999999999999,7.8971245663519,1.27883680879202));
#53350=CARTESIAN_POINT('Origin',(0.5,0.,0.));
#53351=CARTESIAN_POINT('',(0.5,7.73074086114583,1.3631381946854));
#53352=CARTESIAN_POINT('Origin',(0.5,7.73074086114583,1.3631381946854));
#53353=CARTESIAN_POINT('',(9.,7.8971245663519,1.27883680879202));
#53354=CARTESIAN_POINT('',(4.75,7.8971245663519,1.27883680879202));
#53355=CARTESIAN_POINT('',(9.,7.73074086114583,1.3631381946854));
#53356=CARTESIAN_POINT('Origin',(9.,7.82922163644705,1.3805030124521));
#53357=CARTESIAN_POINT('Origin',(9.,0.,0.));
#53358=CARTESIAN_POINT('Origin',(0.5,8.05,0.15));
#53359=CARTESIAN_POINT('',(9.,7.99921718082665,0.111912885619985));
#53360=CARTESIAN_POINT('',(0.499999999999999,7.99921718082665,0.111912885619985));
#53361=CARTESIAN_POINT('',(4.75,7.99921718082665,0.111912885619985));
#53362=CARTESIAN_POINT('',(9.,7.85,0.));
#53363=CARTESIAN_POINT('',(9.,8.05,0.15));
#53364=CARTESIAN_POINT('',(0.5,7.85,0.));
#53365=CARTESIAN_POINT('',(0.5,7.85,0.));
#53366=CARTESIAN_POINT('',(0.5,8.05,0.15));
#53367=CARTESIAN_POINT('Origin',(0.5,7.95,0.));
#53368=CARTESIAN_POINT('',(0.499999999999999,7.99921718082665,-0.111912885619987));
#53369=CARTESIAN_POINT('Origin',(0.5,0.,0.));
#53370=CARTESIAN_POINT('',(0.5,7.85,0.));
#53371=CARTESIAN_POINT('Origin',(0.5,7.85,0.));
#53372=CARTESIAN_POINT('',(9.,7.99921718082665,-0.111912885619987));
#53373=CARTESIAN_POINT('',(4.75,7.99921718082665,-0.111912885619987));
#53374=CARTESIAN_POINT('',(9.,7.85,0.));
#53375=CARTESIAN_POINT('Origin',(9.,7.95,0.));
#53376=CARTESIAN_POINT('Origin',(9.,0.,0.));
#53377=CARTESIAN_POINT('Origin',(10.,5.55111512312578E-16,4.61880215351701));
#53378=CARTESIAN_POINT('',(10.,2.82820063659975E-16,4.61880215351701));
#53379=CARTESIAN_POINT('',(10.,4.,2.3094010767585));
#53380=CARTESIAN_POINT('',(10.,1.,4.04145188432738));
#53381=CARTESIAN_POINT('',(5.,5.55111512312578E-16,4.61880215351701));
#53382=CARTESIAN_POINT('',(10.,2.82820063659975E-16,4.61880215351701));
#53383=CARTESIAN_POINT('',(5.,4.,2.3094010767585));
#53384=CARTESIAN_POINT('',(5.,4.,2.3094010767585));
#53385=CARTESIAN_POINT('',(10.,4.,2.3094010767585));
#53386=CARTESIAN_POINT('Origin',(10.,-4.,2.3094010767585));
#53387=CARTESIAN_POINT('',(10.,-4.,2.3094010767585));
#53388=CARTESIAN_POINT('',(10.,-3.,2.88675134594813));
#53389=CARTESIAN_POINT('',(5.,-4.,2.3094010767585));
#53390=CARTESIAN_POINT('',(10.,-4.,2.3094010767585));
#53391=CARTESIAN_POINT('',(5.,2.82820063659975E-16,4.61880215351701));
#53392=CARTESIAN_POINT('Origin',(10.,-4.,-2.3094010767585));
#53393=CARTESIAN_POINT('',(10.,-4.,-2.3094010767585));
#53394=CARTESIAN_POINT('',(10.,-4.,-1.15470053837925));
#53395=CARTESIAN_POINT('',(5.,-4.,-2.3094010767585));
#53396=CARTESIAN_POINT('',(10.,-4.,-2.3094010767585));
#53397=CARTESIAN_POINT('',(5.,-4.,2.3094010767585));
#53398=CARTESIAN_POINT('Origin',(10.,-1.11022302462516E-15,-4.61880215351701));
#53399=CARTESIAN_POINT('',(10.,-8.48460190979926E-16,-4.61880215351701));
#53400=CARTESIAN_POINT('',(10.,-1.,-4.04145188432738));
#53401=CARTESIAN_POINT('',(5.,-1.11022302462516E-15,-4.61880215351701));
#53402=CARTESIAN_POINT('',(10.,-8.48460190979926E-16,-4.61880215351701));
#53403=CARTESIAN_POINT('',(5.,-4.,-2.3094010767585));
#53404=CARTESIAN_POINT('Origin',(10.,4.,-2.30940107675851));
#53405=CARTESIAN_POINT('',(10.,4.,-2.30940107675851));
#53406=CARTESIAN_POINT('',(10.,3.,-2.88675134594813));
#53407=CARTESIAN_POINT('',(5.,4.,-2.30940107675851));
#53408=CARTESIAN_POINT('',(10.,4.,-2.30940107675851));
#53409=CARTESIAN_POINT('',(5.,-8.48460190979926E-16,-4.61880215351701));
#53410=CARTESIAN_POINT('Origin',(10.,4.,2.3094010767585));
#53411=CARTESIAN_POINT('',(10.,4.,1.15470053837925));
#53412=CARTESIAN_POINT('',(5.,4.,-2.30940107675851));
#53413=CARTESIAN_POINT('Origin',(5.,0.,0.));
#53414=CARTESIAN_POINT('Origin',(-30.,4.5,0.));
#53415=CARTESIAN_POINT('',(-30.,-4.5,-5.51091059616309E-16));
#53416=CARTESIAN_POINT('Origin',(-30.,0.,0.));
#53417=CARTESIAN_POINT('Origin',(-29.75,0.,0.));
#53418=CARTESIAN_POINT('',(-29.75,-4.75,-5.81707229594993E-16));
#53419=CARTESIAN_POINT('Origin',(-14.75,0.,0.));
#53420=CARTESIAN_POINT('Origin',(0.,0.,0.));
#53421=CARTESIAN_POINT('Origin',(0.,8.,0.));
#53422=CARTESIAN_POINT('',(5.55111512312578E-16,-8.,-9.79717439317883E-16));
#53423=CARTESIAN_POINT('Origin',(0.,0.,0.));
#53424=CARTESIAN_POINT('Origin',(4.75,0.,0.));
#53425=CARTESIAN_POINT('',(9.5,-8.,-9.79717439317883E-16));
#53426=CARTESIAN_POINT('Origin',(9.5,0.,0.));
#53427=CARTESIAN_POINT('',(4.75,-8.,-9.79717439317883E-16));
#53428=CARTESIAN_POINT('',(4.75,-8.,-9.79717439317883E-16));
#53429=CARTESIAN_POINT('Origin',(9.75,0.,0.));
#53430=CARTESIAN_POINT('',(10.,-7.5,-9.18485099360515E-16));
#53431=CARTESIAN_POINT('Origin',(10.,0.,0.));
#53432=CARTESIAN_POINT('',(9.75,-7.75,-9.49101269339199E-16));
#53433=CARTESIAN_POINT('Origin',(10.,0.,0.));
#55712=UNCERTAINTY_MEASURE_WITH_UNIT(LENGTH_MEASURE(0.01),#55738,
'DISTANCE_ACCURACY_VALUE',
'Maximum model space distance between geometric entities at asserted c
onnectivities');
#55715=UNCERTAINTY_MEASURE_WITH_UNIT(LENGTH_MEASURE(0.01),#55738,
'DISTANCE_ACCURACY_VALUE',
'Maximum model space distance between geometric entities at asserted c
onnectivities');
#55734=(
GEOMETRIC_REPRESENTATION_CONTEXT(3)
GLOBAL_UNCERTAINTY_ASSIGNED_CONTEXT((#55712))
GLOBAL_UNIT_ASSIGNED_CONTEXT((#55738,#55740,#55741))
REPRESENTATION_CONTEXT('','3D')
);
#55737=(
GEOMETRIC_REPRESENTATION_CONTEXT(3)
GLOBAL_UNCERTAINTY_ASSIGNED_CONTEXT((#55715))
GLOBAL_UNIT_ASSIGNED_CONTEXT((#55738,#55740,#55741))
REPRESENTATION_CONTEXT('','3D')
);
#55738=(
LENGTH_UNIT()
NAMED_UNIT(*)
SI_UNIT(.MILLI.,.METRE.)
);
#55740=(
NAMED_UNIT(*)
PLANE_ANGLE_UNIT()
SI_UNIT($,.RADIAN.)
);
#55741=(
NAMED_UNIT(*)
SI_UNIT($,.STERADIAN.)
SOLID_ANGLE_UNIT()
);
#55760=SHAPE_DEFINITION_REPRESENTATION(#55781,#55838);
#55781=PRODUCT_DEFINITION_SHAPE('',$,#55860);
#55838=SHAPE_REPRESENTATION('',(#29560),#55734);
#55841=PRODUCT_DEFINITION_CONTEXT('part definition',#55906,'design');
#55860=PRODUCT_DEFINITION('2026-10-26-00-34-30-011',
'15_Bracket_Screw_ISO_4762_M10x30',#55881,#55841);
#55881=PRODUCT_DEFINITION_FORMATION('',$,#55926);
#55906=APPLICATION_CONTEXT(
'Core Data for Automotive Mechanical Design Process');
#55907=PRODUCT_CONTEXT('part definition',#55906,'mechanical');
#55926=PRODUCT('2026-10-26-00-34-30-011',
'15_Bracket_Screw_ISO_4762_M10x30',$,(#55907));
#55992=COLOUR_RGB('Black',0.12,0.14,0.17);
#55993=FILL_AREA_STYLE_COLOUR('',#55992);
#55994=FILL_AREA_STYLE('',(#55993));
#55995=SURFACE_STYLE_FILL_AREA(#55994);
#55996=SURFACE_SIDE_STYLE('',(#55995));
#55997=SURFACE_STYLE_USAGE(.BOTH.,#55996);
#55998=PRESENTATION_STYLE_ASSIGNMENT((#55997));
ENDSEC;
END-ISO-10303-21;
